ISO-10303-21;
HEADER;
FILE_DESCRIPTION (('STEP AP214'),
    '1' );
FILE_NAME ('hex flange bolt_din_DIN 6921 - M8 x 40 x 40-S.step',
    '2026-10-09T14:04:53',
    ( '' ),
    ( '' ),
    'SwSTEP 2.0',
    'SolidWorks 2021',
    '' );
FILE_SCHEMA (( 'AUTOMOTIVE_DESIGN' ));
ENDSEC;

DATA;
#18=VERTEX_POINT ( 'NONE', #35795 ) ;
#37=DIRECTION ( 'NONE',  ( -1.000000000000000000, -1.224606353822377258E-16, -0.000000000000000000 ) ) ;
#116=LINE ( 'NONE', #82122, #11300 ) ;
#157=CIRCLE ( 'NONE', #101825, 3.309500000000001663 ) ;
#252=DIRECTION ( 'NONE',  ( 0.000000000000000000, -1.000000000000000000, 0.000000000000000000 ) ) ;
#264=CARTESIAN_POINT ( 'NONE',  ( 34.83349330513379982, -4.000000000000000000, 4.898587196589415787E-16 ) ) ;
#267=VECTOR ( 'NONE', #35746, 1000.000000000000000 ) ;
#272=CARTESIAN_POINT ( 'NONE',  ( 0.2573354458087858676, -4.368923434677200568, -5.432802636760778903 ) ) ;
#285=EDGE_CURVE ( 'NONE', #95564, #63670, #35892, .T. ) ;
#314=UNCERTAINTY_MEASURE_WITH_UNIT (LENGTH_MEASURE( 1.000000000000000082E-05 ), #86417, 'distance_accuracy_value', 'NONE');
#324=DIRECTION ( 'NONE',  ( -1.000000000000000000, -0.000000000000000000, -0.000000000000000000 ) ) ;
#326=ORIENTED_EDGE ( 'NONE', *, *, #60102, .F. ) ;
#334=EDGE_CURVE ( 'NONE', #34125, #93985, #84713, .T. ) ;
#360=DIRECTION ( 'NONE',  ( -1.000000000000000000, -1.224606353822377258E-16, -0.000000000000000000 ) ) ;
#364=FACE_OUTER_BOUND ( 'NONE', #54905, .T. ) ;
#373=CYLINDRICAL_SURFACE ( 'NONE', #62496, 4.000000000000000000 ) ;
#381=EDGE_CURVE ( 'NONE', #74067, #18, #102497, .T. ) ;
#386=ADVANCED_FACE ( 'NONE', ( #53417 ), #96135, .T. ) ;
#399=DIRECTION ( 'NONE',  ( 0.000000000000000000, 1.000000000000000000, 0.000000000000000000 ) ) ;
#411=ORIENTED_EDGE ( 'NONE', *, *, #79860, .T. ) ;
#419=EDGE_LOOP ( 'NONE', ( #2090, #86427, #72217, #95516, #41988, #25906 ) ) ;
#444=VERTEX_POINT ( 'NONE', #60986 ) ;
#447=CARTESIAN_POINT ( 'NONE',  ( 29.34999999999999787, 1.533819458162526451E-15, 0.000000000000000000 ) ) ;
#476=EDGE_CURVE ( 'NONE', #67441, #75440, #73711, .T. ) ;
#478=VERTEX_POINT ( 'NONE', #19497 ) ;
#532=ORIENTED_EDGE ( 'NONE', *, *, #38834, .T. ) ;
#549=CARTESIAN_POINT ( 'NONE',  ( 33.58349330513379982, 4.898587196589405926E-16, -4.000000000000001776 ) ) ;
#569=CARTESIAN_POINT ( 'NONE',  ( 8.866506694866188809, -3.851859888774471706E-31, 4.000000000000000888 ) ) ;
#573=ORIENTED_EDGE ( 'NONE', *, *, #17362, .F. ) ;
#575=VECTOR ( 'NONE', #68936, 1000.000000000000000 ) ;
#596=VERTEX_POINT ( 'NONE', #87383 ) ;
#616=FACE_OUTER_BOUND ( 'NONE', #76040, .T. ) ;
#657=ORIENTED_EDGE ( 'NONE', *, *, #20920, .F. ) ;
#664=DIRECTION ( 'NONE',  ( 0.000000000000000000, 1.000000000000000000, 0.000000000000000000 ) ) ;
#673=VERTEX_POINT ( 'NONE', #17212 ) ;
#702=FACE_OUTER_BOUND ( 'NONE', #86765, .T. ) ;
#731=EDGE_LOOP ( 'NONE', ( #16688, #7338, #6417, #75018, #97240 ) ) ;
#736=EDGE_CURVE ( 'NONE', #77337, #18, #99663, .T. ) ;
#744=CARTESIAN_POINT ( 'NONE',  ( 0.1061556211655322601, 4.836380039389416297, -4.623144047065555817 ) ) ;
#766=CARTESIAN_POINT ( 'NONE',  ( 6.683837171061809634, -7.911893696991943337, -3.558927330633863411E-17 ) ) ;
#785=ORIENTED_EDGE ( 'NONE', *, *, #53839, .F. ) ;
#795=CONICAL_SURFACE ( 'NONE', #45601, 4.000000000000001776, 0.9599310885968808105 ) ;
#859=DIRECTION ( 'NONE',  ( -1.000000000000000000, -1.224606353822377258E-16, -0.000000000000000000 ) ) ;
#863=EDGE_CURVE ( 'NONE', #34518, #96063, #84597, .T. ) ;
#866=VERTEX_POINT ( 'NONE', #68417 ) ;
#871=CONICAL_SURFACE ( 'NONE', #93935, 4.000000000000001776, 0.9599310885968808105 ) ;
#875=EDGE_LOOP ( 'NONE', ( #30568, #3242, #63435, #105804, #87512, #94154 ) ) ;
#879=CARTESIAN_POINT ( 'NONE',  ( 6.585468679846623985, 7.640532685286893333, 0.2337908078075569274 ) ) ;
#883=AXIS2_PLACEMENT_3D ( 'NONE', #55097, #96645, #4442 ) ;
#892=DIRECTION ( 'NONE',  ( 0.000000000000000000, 0.000000000000000000, 1.000000000000000000 ) ) ;
#898=DIRECTION ( 'NONE',  ( 1.000000000000000000, 1.224606353822377258E-16, 0.000000000000000000 ) ) ;
#903=DIRECTION ( 'NONE',  ( 0.000000000000000000, 0.000000000000000000, 1.000000000000000000 ) ) ;
#906=CARTESIAN_POINT ( 'NONE',  ( 28.86650669486618881, 1.474610560812782335E-15, 0.000000000000000000 ) ) ;
#908=CARTESIAN_POINT ( 'NONE',  ( 0.4033376246892471650, 4.059728990630802947, 5.968343123267131567 ) ) ;
#925=DIRECTION ( 'NONE',  ( 0.5735764363510466035, -0.8191520442889914655, 1.003171929053524500E-16 ) ) ;
#932=CIRCLE ( 'NONE', #49162, 4.000000000000001776 ) ;
#936=ORIENTED_EDGE ( 'NONE', *, *, #34599, .F. ) ;
#946=CIRCLE ( 'NONE', #7833, 3.309500000000001663 ) ;
#958=VERTEX_POINT ( 'NONE', #86733 ) ;
#960=CARTESIAN_POINT ( 'NONE',  ( 6.463481858019714643, 4.600809706232196206, 5.711197301637623625 ) ) ;
#979=CARTESIAN_POINT ( 'NONE',  ( 17.33349330513380337, 1.593028355512270567E-15, 0.000000000000000000 ) ) ;
#1004=CARTESIAN_POINT ( 'NONE',  ( 6.562934840145643101, 7.579717272840336584, -0.5631738335430742648 ) ) ;
#1007=CONICAL_SURFACE ( 'NONE', #81951, 4.000000000000001776, 0.9599310885968808105 ) ;
#1025=VECTOR ( 'NONE', #69707, 1000.000000000000000 ) ;
#1095=DIRECTION ( 'NONE',  ( 0.000000000000000000, 0.000000000000000000, -1.000000000000000000 ) ) ;
#1099=DIRECTION ( 'NONE',  ( 0.000000000000000000, -1.000000000000000000, 0.000000000000000000 ) ) ;
#1122=DIRECTION ( 'NONE',  ( 0.000000000000000000, -1.000000000000000000, 0.000000000000000000 ) ) ;
#1148=CIRCLE ( 'NONE', #70087, 4.000000000000000888 ) ;
#1155=VERTEX_POINT ( 'NONE', #58600 ) ;
#1179=VECTOR ( 'NONE', #23307, 1000.000000000000000 ) ;
#1220=ORIENTED_EDGE ( 'NONE', *, *, #17572, .F. ) ;
#1227=DIRECTION ( 'NONE',  ( -1.000000000000000000, -1.224606353822377258E-16, -0.000000000000000000 ) ) ;
#1241=DIRECTION ( 'NONE',  ( -1.000000000000000000, -1.224606353822377258E-16, -0.000000000000000000 ) ) ;
#1244=CARTESIAN_POINT ( 'NONE',  ( 16.08349330513380337, 1.593028355512270567E-15, 0.000000000000000000 ) ) ;
#1250=LINE ( 'NONE', #64569, #70140 ) ;
#1257=CIRCLE ( 'NONE', #20291, 4.000000000000001776 ) ;
#1281=VECTOR ( 'NONE', #20460, 1000.000000000000000 ) ;
#1285=DIRECTION ( 'NONE',  ( 0.000000000000000000, -1.000000000000000000, 0.000000000000000000 ) ) ;
#1288=CARTESIAN_POINT ( 'NONE',  ( -4.573977915173229720E-15, 5.469921996229796690, -3.525817189091416282 ) ) ;
#1294=ORIENTED_EDGE ( 'NONE', *, *, #89470, .F. ) ;
#1298=VECTOR ( 'NONE', #77870, 1000.000000000000000 ) ;
#1340=CARTESIAN_POINT ( 'NONE',  ( 23.86650669486618881, -3.851859888774471706E-31, 4.000000000000000888 ) ) ;
#1344=CARTESIAN_POINT ( 'NONE',  ( 27.33349330513380337, 1.593028355512270567E-15, 0.000000000000000000 ) ) ;
#1392=PRODUCT_DEFINITION_CONTEXT ( 'detailed design', #6631, 'design' ) ;
#1398=CARTESIAN_POINT ( 'NONE',  ( 47.33349330513379982, -7.703719777548943412E-31, 4.000000000000001776 ) ) ;
#1404=VECTOR ( 'NONE', #20579, 1000.000000000000114 ) ;
#1432=ORIENTED_EDGE ( 'NONE', *, *, #71720, .T. ) ;
#1441=ORIENTED_EDGE ( 'NONE', *, *, #60385, .T. ) ;
#1495=ORIENTED_EDGE ( 'NONE', *, *, #35490, .T. ) ;
#1498=LINE ( 'NONE', #3117, #83897 ) ;
#1526=DIRECTION ( 'NONE',  ( 0.000000000000000000, -1.000000000000000000, 0.000000000000000000 ) ) ;
#1530=AXIS2_PLACEMENT_3D ( 'NONE', #103824, #70931, #88185 ) ;
#1570=DIRECTION ( 'NONE',  ( -1.000000000000000000, -1.224606353822377258E-16, -0.000000000000000000 ) ) ;
#1592=LINE ( 'NONE', #34553, #4317 ) ;
#1620=CARTESIAN_POINT ( 'NONE',  ( 0.000000000000000000, 4.898587196589412829E-16, -4.000000000000000000 ) ) ;
#1632=CONICAL_SURFACE ( 'NONE', #70583, 3.309500000000001663, 0.9599310885968770357 ) ;
#1636=VERTEX_POINT ( 'NONE', #27608 ) ;
#1662=FACE_OUTER_BOUND ( 'NONE', #43469, .T. ) ;
#1702=CARTESIAN_POINT ( 'NONE',  ( 38.58349330513380693, 1.593028355512270567E-15, 0.000000000000000000 ) ) ;
#1762=ORIENTED_EDGE ( 'NONE', *, *, #53785, .F. ) ;
#1771=CIRCLE ( 'NONE', #8639, 3.309500000000001663 ) ;
#1789=CONICAL_SURFACE ( 'NONE', #101672, 4.000000000000001776, 0.9599310885968808105 ) ;
#1818=ORIENTED_EDGE ( 'NONE', *, *, #44327, .T. ) ;
#1820=FACE_OUTER_BOUND ( 'NONE', #14130, .T. ) ;
#1821=CARTESIAN_POINT ( 'NONE',  ( 5.947762761376478302, -4.378239541354659536, 5.416666666666666075 ) ) ;
#1822=CARTESIAN_POINT ( 'NONE',  ( 13.09999999999999787, 1.533819458162526451E-15, 0.000000000000000000 ) ) ;
#1832=CARTESIAN_POINT ( 'NONE',  ( 6.169949891408690767, -4.949864754179921889, -4.426582755168041672 ) ) ;
#1833=CARTESIAN_POINT ( 'NONE',  ( 0.2578475836320682779, 4.367703157927327773, -5.434916218090833695 ) ) ;
#1864=CARTESIAN_POINT ( 'NONE',  ( 11.08349330513380160, 1.593028355512270567E-15, 0.000000000000000000 ) ) ;
#1876=EDGE_CURVE ( 'NONE', #596, #98741, #106344, .T. ) ;
#1878=EDGE_LOOP ( 'NONE', ( #32027, #39229, #67122, #48724, #5383, #100745 ) ) ;
#1930=VECTOR ( 'NONE', #65836, 1000.000000000000000 ) ;
#1944=CYLINDRICAL_SURFACE ( 'NONE', #70223, 4.000000000000000000 ) ;
#1983=EDGE_CURVE ( 'NONE', #10582, #79906, #56452, .T. ) ;
#1984=CARTESIAN_POINT ( 'NONE',  ( 29.83349330513380337, 1.593028355512270567E-15, 0.000000000000000000 ) ) ;
#2011=CARTESIAN_POINT ( 'NONE',  ( 0.000000000000000000, 0.000000000000000000, 4.000000000000000000 ) ) ;
#2034=CARTESIAN_POINT ( 'NONE',  ( 15.11650669486618881, 4.000000000000003553, 4.898587196589414801E-16 ) ) ;
#2038=DIRECTION ( 'NONE',  ( 1.000000000000000000, 0.000000000000000000, 0.000000000000000000 ) ) ;
#2039=DIRECTION ( 'NONE',  ( -0.5735764363510494901, -0.8191520442889894671, 0.000000000000000000 ) ) ;
#2046=B_SPLINE_CURVE_WITH_KNOTS ( 'NONE', 3,
 ( #20307, #53154, #69867, #55764, #23460, #25048, #40140, #88699 ),
 .UNSPECIFIED., .F., .F.,
 ( 4, 2, 2, 4 ),
 ( 0.003797433802554431997, 0.004743183970586230952, 0.005688934138618029906, 0.007580434474681626948 ),
 .UNSPECIFIED. ) ;
#2049=ORIENTED_EDGE ( 'NONE', *, *, #21354, .T. ) ;
#2052=DIRECTION ( 'NONE',  ( 0.000000000000000000, -1.000000000000000000, 0.000000000000000000 ) ) ;
#2073=DIRECTION ( 'NONE',  ( 0.000000000000000000, -1.000000000000000000, 0.000000000000000000 ) ) ;
#2090=ORIENTED_EDGE ( 'NONE', *, *, #7883, .F. ) ;
#2097=CARTESIAN_POINT ( 'NONE',  ( 24.83349330513380337, 1.593028355512270567E-15, 0.000000000000000000 ) ) ;
#2105=DIRECTION ( 'NONE',  ( -0.5735764363510494901, -0.8191520442889894671, 0.000000000000000000 ) ) ;
#2115=VERTEX_POINT ( 'NONE', #82480 ) ;
#2149=VERTEX_POINT ( 'NONE', #19396 ) ;
#2152=AXIS2_PLACEMENT_3D ( 'NONE', #14691, #6080, #81021 ) ;
#2154=CARTESIAN_POINT ( 'NONE',  ( 20.11650669486618881, -3.851859888774471706E-31, 4.000000000000000888 ) ) ;
#2156=DIRECTION ( 'NONE',  ( -1.000000000000000000, -0.000000000000000000, -0.000000000000000000 ) ) ;
#2167=ORIENTED_EDGE ( 'NONE', *, *, #61657, .F. ) ;
#2169=DIRECTION ( 'NONE',  ( 0.000000000000000000, 0.000000000000000000, 1.000000000000000000 ) ) ;
#2181=DIRECTION ( 'NONE',  ( 0.000000000000000000, 0.000000000000000000, 1.000000000000000000 ) ) ;
#2193=CARTESIAN_POINT ( 'NONE',  ( 31.84999999999999787, 1.533819458162526451E-15, 0.000000000000000000 ) ) ;
#2224=CARTESIAN_POINT ( 'NONE',  ( 43.86650669486618881, -3.999999999999998224, 0.000000000000000000 ) ) ;
#2227=CARTESIAN_POINT ( 'NONE',  ( 6.692588830498432451, -7.935834885954439422, -0.04058884017440578251 ) ) ;
#2241=EDGE_CURVE ( 'NONE', #60237, #86927, #22079, .T. ) ;
#2248=ORIENTED_EDGE ( 'NONE', *, *, #15481, .F. ) ;
#2263=FACE_OUTER_BOUND ( 'NONE', #39040, .T. ) ;
#2319=EDGE_CURVE ( 'NONE', #8756, #59177, #42694, .T. ) ;
#2326=ORIENTED_EDGE ( 'NONE', *, *, #10621, .T. ) ;
#2379=CARTESIAN_POINT ( 'NONE',  ( 20.59999999999999787, 3.309500000000003439, 4.052968581778167743E-16 ) ) ;
#2384=CARTESIAN_POINT ( 'NONE',  ( 6.936184427528457874, 0.000000000000000000, -8.605212085995399107 ) ) ;
#2403=EDGE_CURVE ( 'NONE', #26186, #57765, #8261, .T. ) ;
#2442=DIRECTION ( 'NONE',  ( -1.000000000000000000, -1.224606353822377258E-16, -0.000000000000000000 ) ) ;
#2460=EDGE_CURVE ( 'NONE', #83253, #25084, #68584, .T. ) ;
#2461=ORIENTED_EDGE ( 'NONE', *, *, #98829, .F. ) ;
#2501=ORIENTED_EDGE ( 'NONE', *, *, #66634, .F. ) ;
#2507=ORIENTED_EDGE ( 'NONE', *, *, #54982, .T. ) ;
#2532=CIRCLE ( 'NONE', #28374, 4.000000000000000888 ) ;
#2565=CARTESIAN_POINT ( 'NONE',  ( 18.58349330513380337, -7.703719777548943412E-31, 4.000000000000001776 ) ) ;
#2568=CARTESIAN_POINT ( 'NONE',  ( 5.817833032102704749, -1.364745674339625570, -6.499999999999999112 ) ) ;
#2573=DIRECTION ( 'NONE',  ( 0.000000000000000000, 0.000000000000000000, -1.000000000000000000 ) ) ;
#2588=DIRECTION ( 'NONE',  ( -1.000000000000000000, -1.224606353822377258E-16, -0.000000000000000000 ) ) ;
#2593=LINE ( 'NONE', #58178, #99366 ) ;
#2595=AXIS2_PLACEMENT_3D ( 'NONE', #8469, #23094, #55928 ) ;
#2603=DIRECTION ( 'NONE',  ( -1.000000000000000000, -0.000000000000000000, -0.000000000000000000 ) ) ;
#2607=ORIENTED_EDGE ( 'NONE', *, *, #58675, .F. ) ;
#2626=EDGE_CURVE ( 'NONE', #36026, #35969, #34172, .T. ) ;
#2648=DIRECTION ( 'NONE',  ( -1.000000000000000000, -1.224606353822377258E-16, -0.000000000000000000 ) ) ;
#2649=DIRECTION ( 'NONE',  ( -1.000000000000000000, -0.000000000000000000, -0.000000000000000000 ) ) ;
#2657=CIRCLE ( 'NONE', #87073, 4.000000000000000888 ) ;
#2719=DIRECTION ( 'NONE',  ( 0.000000000000000000, 1.000000000000000000, 0.000000000000000000 ) ) ;
#2752=CARTESIAN_POINT ( 'NONE',  ( 12.33349330513380337, 1.593028355512270567E-15, 0.000000000000000000 ) ) ;
#2798=LINE ( 'NONE', #17412, #267 ) ;
#2810=CARTESIAN_POINT ( 'NONE',  ( 43.86650669486618881, 1.474610560812782335E-15, 0.000000000000000000 ) ) ;
#2814=VERTEX_POINT ( 'NONE', #48778 ) ;
#2815=DIRECTION ( 'NONE',  ( -0.5735764363510497121, 0.8191520442889892450, 1.003171929053521665E-16 ) ) ;
#2818=CARTESIAN_POINT ( 'NONE',  ( 21.84999999999999787, 1.533819458162526451E-15, 0.000000000000000000 ) ) ;
#2831=AXIS2_PLACEMENT_3D ( 'NONE', #25998, #60988, #2181 ) ;
#2883=DIRECTION ( 'NONE',  ( 0.000000000000000000, -1.000000000000000000, 0.000000000000000000 ) ) ;
#2888=CIRCLE ( 'NONE', #37354, 4.000000000000001776 ) ;
#2893=EDGE_CURVE ( 'NONE', #59552, #21594, #61508, .T. ) ;
#2919=ADVANCED_FACE ( 'NONE', ( #71882 ), #87035, .T. ) ;
#2971=ADVANCED_FACE ( 'NONE', ( #96701 ), #25647, .T. ) ;
#2980=EDGE_CURVE ( 'NONE', #76213, #10553, #71785, .T. ) ;
#2988=DIRECTION ( 'NONE',  ( -1.000000000000000000, -1.224606353822377258E-16, -0.000000000000000000 ) ) ;
#2997=DIRECTION ( 'NONE',  ( -1.000000000000000000, -1.224606353822377258E-16, -0.000000000000000000 ) ) ;
#3017=AXIS2_PLACEMENT_3D ( 'NONE', #2097, #52252, #60381 ) ;
#3037=EDGE_CURVE ( 'NONE', #74863, #65506, #37973, .T. ) ;
#3046=CARTESIAN_POINT ( 'NONE',  ( 0.000000000000000000, 4.898587196589412829E-16, -4.000000000000000000 ) ) ;
#3056=CIRCLE ( 'NONE', #63352, 4.000000000000001776 ) ;
#3080=ORIENTED_EDGE ( 'NONE', *, *, #71874, .T. ) ;
#3084=CARTESIAN_POINT ( 'NONE',  ( 22.33349330513380337, 4.000000000000003553, 0.000000000000000000 ) ) ;
#3102=CIRCLE ( 'NONE', #63417, 4.000000000000001776 ) ;
#3112=CARTESIAN_POINT ( 'NONE',  ( 6.172076129340175576, 1.395179846525673950, -6.500000000000603073 ) ) ;
#3115=EDGE_CURVE ( 'NONE', #80889, #83253, #65394, .T. ) ;
#3117=CARTESIAN_POINT ( 'NONE',  ( 0.000000000000000000, 0.000000000000000000, 4.000000000000000000 ) ) ;
#3118=LINE ( 'NONE', #61370, #54375 ) ;
#3121=CARTESIAN_POINT ( 'NONE',  ( 11.84999999999999787, 3.309500000000003439, 4.052968581778167743E-16 ) ) ;
#3139=CARTESIAN_POINT ( 'NONE',  ( 0.000000000000000000, 0.000000000000000000, 4.000000000000000000 ) ) ;
#3146=CARTESIAN_POINT ( 'NONE',  ( 36.08349330513379982, 4.000000000000003553, 0.000000000000000000 ) ) ;
#3181=CARTESIAN_POINT ( 'NONE',  ( 26.36650669486618881, 1.474610560812782335E-15, 0.000000000000000000 ) ) ;
#3185=CARTESIAN_POINT ( 'NONE',  ( 0.000000000000000000, 0.000000000000000000, 0.000000000000000000 ) ) ;
#3231=CARTESIAN_POINT ( 'NONE',  ( 8.099999999999999645, 3.752776749732561257, -6.499999999999999112 ) ) ;
#3236=EDGE_CURVE ( 'NONE', #2115, #35969, #58908, .T. ) ;
#3242=ORIENTED_EDGE ( 'NONE', *, *, #38802, .T. ) ;
#3282=ADVANCED_FACE ( 'NONE', ( #9791 ), #49405, .T. ) ;
#3283=CARTESIAN_POINT ( 'NONE',  ( 31.84999999999999787, 3.309500000000003439, 4.052968581778167743E-16 ) ) ;
#3311=CARTESIAN_POINT ( 'NONE',  ( 27.61650669486618881, 4.000000000000003553, 4.898587196589414801E-16 ) ) ;
#3316=ADVANCED_FACE ( 'NONE', ( #59984 ), #71296, .F. ) ;
#3343=CARTESIAN_POINT ( 'NONE',  ( 0.000000000000000000, 0.000000000000000000, 4.000000000000000000 ) ) ;
#3350=SHAPE_REPRESENTATION_RELATIONSHIP ( 'NONE' , 'NONE' ,  #88164, #88554 ) ;
#3353=DIRECTION ( 'NONE',  ( -1.000000000000000000, -0.000000000000000000, -0.000000000000000000 ) ) ;
#3375=CARTESIAN_POINT ( 'NONE',  ( 8.099999999999999645, 0.000000000000000000, 4.000000000000000000 ) ) ;
#3408=AXIS2_PLACEMENT_3D ( 'NONE', #36883, #4477, #70279 ) ;
#3442=CIRCLE ( 'NONE', #86152, 4.000000000000000000 ) ;
#3448=ORIENTED_EDGE ( 'NONE', *, *, #3473, .T. ) ;
#3450=VERTEX_POINT ( 'NONE', #6887 ) ;
#3464=ORIENTED_EDGE ( 'NONE', *, *, #88915, .F. ) ;
#3473=EDGE_CURVE ( 'NONE', #4931, #60457, #56245, .T. ) ;
#3497=CIRCLE ( 'NONE', #74066, 4.000000000000001776 ) ;
#3525=LINE ( 'NONE', #76867, #72255 ) ;
#3570=ORIENTED_EDGE ( 'NONE', *, *, #49537, .T. ) ;
#3630=CARTESIAN_POINT ( 'NONE',  ( 0.000000000000000000, 0.000000000000000000, 0.000000000000000000 ) ) ;
#3654=CIRCLE ( 'NONE', #29552, 4.000000000000000888 ) ;
#3655=CARTESIAN_POINT ( 'NONE',  ( 6.332254158185223858, -2.698766916914401737, -6.499999999999998224 ) ) ;
#3662=CARTESIAN_POINT ( 'NONE',  ( 0.000000000000000000, 0.000000000000000000, 0.000000000000000000 ) ) ;
#3683=CIRCLE ( 'NONE', #82901, 4.000000000000001776 ) ;
#3687=FACE_OUTER_BOUND ( 'NONE', #57216, .T. ) ;
#3694=VERTEX_POINT ( 'NONE', #74988 ) ;
#3764=LINE ( 'NONE', #42609, #44597 ) ;
#3795=ORIENTED_EDGE ( 'NONE', *, *, #13580, .F. ) ;
#3825=DIRECTION ( 'NONE',  ( 1.000000000000000000, 1.224606353822377258E-16, 0.000000000000000000 ) ) ;
#3920=EDGE_CURVE ( 'NONE', #77684, #98423, #4778, .T. ) ;
#3942=LINE ( 'NONE', #19640, #81969 ) ;
#3943=ORIENTED_EDGE ( 'NONE', *, *, #25237, .T. ) ;
#3949=EDGE_CURVE ( 'NONE', #45750, #44463, #39199, .T. ) ;
#3952=DIRECTION ( 'NONE',  ( -1.000000000000000000, -1.224606353822377258E-16, -0.000000000000000000 ) ) ;
#3965=DIRECTION ( 'NONE',  ( 0.5735764363510462704, 0.8191520442889915765, 0.000000000000000000 ) ) ;
#3977=DIRECTION ( 'NONE',  ( -1.000000000000000000, -1.224606353822377258E-16, -0.000000000000000000 ) ) ;
#3996=ADVANCED_FACE ( 'NONE', ( #14495 ), #54964, .F. ) ;
#4000=ORIENTED_EDGE ( 'NONE', *, *, #2893, .F. ) ;
#4009=ADVANCED_FACE ( 'NONE', ( #71161 ), #62557, .T. ) ;
#4033=DIRECTION ( 'NONE',  ( 0.000000000000000000, -1.000000000000000000, 0.000000000000000000 ) ) ;
#4048=DIRECTION ( 'NONE',  ( -1.000000000000000000, -1.224606353822377258E-16, -0.000000000000000000 ) ) ;
#4086=EDGE_LOOP ( 'NONE', ( #40381, #17061, #81597, #89946, #27974 ) ) ;
#4128=CARTESIAN_POINT ( 'NONE',  ( 6.463481858019718196, -4.600809706232205087, -5.711197301637625401 ) ) ;
#4135=LINE ( 'NONE', #30551, #97119 ) ;
#4179=ORIENTED_EDGE ( 'NONE', *, *, #58104, .F. ) ;
#4214=ORIENTED_EDGE ( 'NONE', *, *, #66504, .T. ) ;
#4228=AXIS2_PLACEMENT_3D ( 'NONE', #67235, #59674, #59139 ) ;
#4243=CARTESIAN_POINT ( 'NONE',  ( 5.975663821525200703, -4.257391242883789673, 5.625982059626458032 ) ) ;
#4248=DIRECTION ( 'NONE',  ( -1.000000000000000000, -1.224606353822377258E-16, -0.000000000000000000 ) ) ;
#4253=ORIENTED_EDGE ( 'NONE', *, *, #63596, .T. ) ;
#4258=ORIENTED_EDGE ( 'NONE', *, *, #21466, .F. ) ;
#4317=VECTOR ( 'NONE', #9159, 1000.000000000000114 ) ;
#4335=ORIENTED_EDGE ( 'NONE', *, *, #86266, .T. ) ;
#4341=ORIENTED_EDGE ( 'NONE', *, *, #82819, .F. ) ;
#4391=VERTEX_POINT ( 'NONE', #26909 ) ;
#4394=CONICAL_SURFACE ( 'NONE', #91998, 4.000000000000001776, 0.9599310885968808105 ) ;
#4396=ORIENTED_EDGE ( 'NONE', *, *, #95242, .T. ) ;
#4420=AXIS2_PLACEMENT_3D ( 'NONE', #13735, #95736, #15338 ) ;
#4438=EDGE_LOOP ( 'NONE', ( #105282, #97923, #82329, #52310, #58613 ) ) ;
#4440=EDGE_CURVE ( 'NONE', #20019, #32527, #94329, .T. ) ;
#4442=DIRECTION ( 'NONE',  ( 0.000000000000000000, -1.000000000000000000, 0.000000000000000000 ) ) ;
#4444=FACE_OUTER_BOUND ( 'NONE', #55660, .T. ) ;
#4477=DIRECTION ( 'NONE',  ( -1.000000000000000000, -1.224606353822377258E-16, -0.000000000000000000 ) ) ;
#4481=DIRECTION ( 'NONE',  ( 1.000000000000000000, 0.000000000000000000, 0.000000000000000000 ) ) ;
#4492=DIRECTION ( 'NONE',  ( -1.000000000000000000, -1.224606353822377258E-16, -0.000000000000000000 ) ) ;
#4503=AXIS2_PLACEMENT_3D ( 'NONE', #16811, #65885, #64827 ) ;
#4566=CARTESIAN_POINT ( 'NONE',  ( 37.61650669486618881, 4.000000000000003553, 4.898587196589414801E-16 ) ) ;
#4615=DIRECTION ( 'NONE',  ( -1.000000000000000000, -1.224606353822377258E-16, -0.000000000000000000 ) ) ;
#4649=DIRECTION ( 'NONE',  ( 0.000000000000000000, -1.000000000000000000, 0.000000000000000000 ) ) ;
#4660=CARTESIAN_POINT ( 'NONE',  ( 41.36650669486618881, 4.000000000000003553, 4.898587196589414801E-16 ) ) ;
#4665=ORIENTED_EDGE ( 'NONE', *, *, #37443, .T. ) ;
#4669=DIRECTION ( 'NONE',  ( -1.000000000000000000, -1.224606353822377258E-16, -0.000000000000000000 ) ) ;
#4671=EDGE_CURVE ( 'NONE', #88549, #34518, #59761, .T. ) ;
#4677=CARTESIAN_POINT ( 'NONE',  ( 0.000000000000000000, 0.000000000000000000, 0.000000000000000000 ) ) ;
#4693=CARTESIAN_POINT ( 'NONE',  ( 24.34999999999999787, 3.309500000000003439, 0.000000000000000000 ) ) ;
#4708=AXIS2_PLACEMENT_3D ( 'NONE', #66378, #47536, #57738 ) ;
#4710=DIRECTION ( 'NONE',  ( 0.000000000000000000, -1.000000000000000000, 0.000000000000000000 ) ) ;
#4712=EDGE_LOOP ( 'NONE', ( #27252, #30873, #4253, #22693, #23481, #104507 ) ) ;
#4741=CARTESIAN_POINT ( 'NONE',  ( 10.11650669486618881, 1.474610560812782335E-15, 0.000000000000000000 ) ) ;
#4770=EDGE_LOOP ( 'NONE', ( #47668, #104722, #83540, #51663, #71167 ) ) ;
#4778=CIRCLE ( 'NONE', #30672, 4.000000000000001776 ) ;
#4847=DIRECTION ( 'NONE',  ( -1.000000000000000000, -1.224606353822377258E-16, -0.000000000000000000 ) ) ;
#4875=AXIS2_PLACEMENT_3D ( 'NONE', #93778, #19937, #52779 ) ;
#4877=EDGE_LOOP ( 'NONE', ( #40534, #54617, #19042, #93179, #41359, #42500 ) ) ;
#4882=CARTESIAN_POINT ( 'NONE',  ( 6.281178480976146616, -3.752776749732557704, 6.500000000000006217 ) ) ;
#4886=ADVANCED_FACE ( 'NONE', ( #92534 ), #51102, .T. ) ;
#4921=DIRECTION ( 'NONE',  ( 0.000000000000000000, 0.000000000000000000, -1.000000000000000000 ) ) ;
#4929=DIRECTION ( 'NONE',  ( 1.000000000000000000, 1.224606353822377258E-16, 0.000000000000000000 ) ) ;
#4931=VERTEX_POINT ( 'NONE', #61798 ) ;
#4935=ORIENTED_EDGE ( 'NONE', *, *, #59344, .F. ) ;
#4941=EDGE_CURVE ( 'NONE', #55265, #20019, #5649, .T. ) ;
#4956=ORIENTED_EDGE ( 'NONE', *, *, #80192, .F. ) ;
#4958=DIRECTION ( 'NONE',  ( -1.000000000000000000, -1.224606353822377258E-16, -0.000000000000000000 ) ) ;
#4968=EDGE_CURVE ( 'NONE', #46481, #29099, #2046, .T. ) ;
#4977=EDGE_CURVE ( 'NONE', #11792, #21079, #85632, .T. ) ;
#4990=CARTESIAN_POINT ( 'NONE',  ( 11.08349330513380160, 1.593028355512270567E-15, 0.000000000000000000 ) ) ;
#5042=DIRECTION ( 'NONE',  ( -1.000000000000000000, -1.224606353822377258E-16, -0.000000000000000000 ) ) ;
#5087=DIRECTION ( 'NONE',  ( -1.000000000000000000, -1.224606353822377258E-16, -0.000000000000000000 ) ) ;
#5090=CARTESIAN_POINT ( 'NONE',  ( 39.83349330513380693, 1.593028355512270567E-15, 0.000000000000000000 ) ) ;
#5137=DIRECTION ( 'NONE',  ( 1.000000000000000000, 1.224606353822377258E-16, 0.000000000000000000 ) ) ;
#5184=ORIENTED_EDGE ( 'NONE', *, *, #42895, .T. ) ;
#5207=LINE ( 'NONE', #37071, #46099 ) ;
#5225=DIRECTION ( 'NONE',  ( 0.000000000000000000, 0.000000000000000000, -1.000000000000000000 ) ) ;
#5235=ORIENTED_EDGE ( 'NONE', *, *, #102815, .T. ) ;
#5247=EDGE_CURVE ( 'NONE', #48174, #39800, #78535, .T. ) ;
#5251=DIRECTION ( 'NONE',  ( 0.000000000000000000, 0.000000000000000000, 1.000000000000000000 ) ) ;
#5252=AXIS2_PLACEMENT_3D ( 'NONE', #43173, #11308, #84692 ) ;
#5253=CARTESIAN_POINT ( 'NONE',  ( 19.83349330513379982, 4.000000000000002665, 0.000000000000000000 ) ) ;
#5257=ORIENTED_EDGE ( 'NONE', *, *, #51467, .T. ) ;
#5262=CARTESIAN_POINT ( 'NONE',  ( 32.61650669486618881, 4.898587196589411843E-16, -4.000000000000000888 ) ) ;
#5272=LINE ( 'NONE', #22003, #35686 ) ;
#5292=DIRECTION ( 'NONE',  ( 0.000000000000000000, 0.000000000000000000, 1.000000000000000000 ) ) ;
#5300=ORIENTED_EDGE ( 'NONE', *, *, #49935, .F. ) ;
#5303=VECTOR ( 'NONE', #57715, 1000.000000000000000 ) ;
#5308=ORIENTED_EDGE ( 'NONE', *, *, #39887, .T. ) ;
#5319=ORIENTED_EDGE ( 'NONE', *, *, #48836, .F. ) ;
#5320=CARTESIAN_POINT ( 'NONE',  ( 5.691929483231186637, 5.629165124598853431, 3.249999999999998668 ) ) ;
#5374=CARTESIAN_POINT ( 'NONE',  ( 10.59999999999999609, 1.533819458162526451E-15, 0.000000000000000000 ) ) ;
#5376=ORIENTED_EDGE ( 'NONE', *, *, #81041, .T. ) ;
#5383=ORIENTED_EDGE ( 'NONE', *, *, #32507, .F. ) ;
#5387=DIRECTION ( 'NONE',  ( -1.000000000000000000, -1.224606353822377258E-16, -0.000000000000000000 ) ) ;
#5402=ORIENTED_EDGE ( 'NONE', *, *, #2241, .F. ) ;
#5403=DIRECTION ( 'NONE',  ( -1.000000000000000000, -0.000000000000000000, -0.000000000000000000 ) ) ;
#5444=ORIENTED_EDGE ( 'NONE', *, *, #32507, .T. ) ;
#5476=EDGE_CURVE ( 'NONE', #77149, #70292, #93432, .T. ) ;
#5490=CARTESIAN_POINT ( 'NONE',  ( 30.11650669486618881, 1.474610560812782335E-15, 0.000000000000000000 ) ) ;
#5491=CARTESIAN_POINT ( 'NONE',  ( 45.59999999999999432, 1.533819458162526451E-15, 0.000000000000000000 ) ) ;
#5497=CARTESIAN_POINT ( 'NONE',  ( 6.585304930659546585, 4.021878819315965359, -6.499999999999999112 ) ) ;
#5518=ORIENTED_EDGE ( 'NONE', *, *, #14262, .F. ) ;
#5545=DIRECTION ( 'NONE',  ( -0.000000000000000000, 0.000000000000000000, 1.000000000000000000 ) ) ;
#5550=CARTESIAN_POINT ( 'NONE',  ( 6.643884894376898664, -3.901062859470944222, -6.756839076126442301 ) ) ;
#5570=CARTESIAN_POINT ( 'NONE',  ( 13.58349330513380160, 1.593028355512270567E-15, 0.000000000000000000 ) ) ;
#5589=AXIS2_PLACEMENT_3D ( 'NONE', #69479, #30628, #96927 ) ;
#5602=CARTESIAN_POINT ( 'NONE',  ( 39.34999999999999432, 1.533819458162526451E-15, 0.000000000000000000 ) ) ;
#5607=DIRECTION ( 'NONE',  ( 0.000000000000000000, -1.000000000000000000, 0.000000000000000000 ) ) ;
#5608=CARTESIAN_POINT ( 'NONE',  ( 24.83349330513380337, 1.593028355512270567E-15, 0.000000000000000000 ) ) ;
#5649=LINE ( 'NONE', #62843, #18427 ) ;
#5668=ORIENTED_EDGE ( 'NONE', *, *, #80635, .F. ) ;
#5676=ORIENTED_EDGE ( 'NONE', *, *, #32257, .F. ) ;
#5688=CARTESIAN_POINT ( 'NONE',  ( 0.000000000000000000, 0.000000000000000000, 4.000000000000000000 ) ) ;
#5691=EDGE_LOOP ( 'NONE', ( #56261, #67960, #35808, #75072, #79133 ) ) ;
#5697=FILL_AREA_STYLE_COLOUR ( '', #57869 ) ;
#5698=CARTESIAN_POINT ( 'NONE',  ( 6.683837171061809634, -7.911893696991943337, -3.558927330633863411E-17 ) ) ;
#5703=DIRECTION ( 'NONE',  ( -1.000000000000000000, -1.224606353822377258E-16, -0.000000000000000000 ) ) ;
#5729=ORIENTED_EDGE ( 'NONE', *, *, #103598, .T. ) ;
#5738=AXIS2_PLACEMENT_3D ( 'NONE', #24706, #23642, #41393 ) ;
#5758=ORIENTED_EDGE ( 'NONE', *, *, #39102, .F. ) ;
#5796=CARTESIAN_POINT ( 'NONE',  ( 23.09999999999999432, 1.533819458162526451E-15, 0.000000000000000000 ) ) ;
#5808=ORIENTED_EDGE ( 'NONE', *, *, #102858, .T. ) ;
#5823=DIRECTION ( 'NONE',  ( 1.000000000000000000, 1.224606353822377258E-16, 0.000000000000000000 ) ) ;
#5843=AXIS2_PLACEMENT_3D ( 'NONE', #8796, #64920, #66505 ) ;
#5846=CARTESIAN_POINT ( 'NONE',  ( 15.59999999999999787, -3.309499999999999886, 4.475777889183790779E-16 ) ) ;
#5865=AXIS2_PLACEMENT_3D ( 'NONE', #43018, #27412, #66760 ) ;
#5881=DIRECTION ( 'NONE',  ( -1.000000000000000000, -1.224606353822377258E-16, -0.000000000000000000 ) ) ;
#5891=LINE ( 'NONE', #38823, #58706 ) ;
#5913=AXIS2_PLACEMENT_3D ( 'NONE', #36186, #69054, #60963 ) ;
#5915=ORIENTED_EDGE ( 'NONE', *, *, #96902, .F. ) ;
#5929=ORIENTED_EDGE ( 'NONE', *, *, #37624, .F. ) ;
#5930=ORIENTED_EDGE ( 'NONE', *, *, #76250, .F. ) ;
#5935=VERTEX_POINT ( 'NONE', #88914 ) ;
#5949=CIRCLE ( 'NONE', #33545, 4.000000000000001776 ) ;
#5954=CARTESIAN_POINT ( 'NONE',  ( 29.34999999999999787, 1.533819458162526451E-15, 0.000000000000000000 ) ) ;
#5969=CARTESIAN_POINT ( 'NONE',  ( 37.33349330513379982, 1.593028355512270567E-15, 0.000000000000000000 ) ) ;
#5983=EDGE_CURVE ( 'NONE', #73940, #78785, #11847, .T. ) ;
#5996=EDGE_CURVE ( 'NONE', #70259, #65781, #68709, .T. ) ;
#6016=ORIENTED_EDGE ( 'NONE', *, *, #23113, .T. ) ;
#6055=CONICAL_SURFACE ( 'NONE', #23338, 3.309500000000001663, 0.9599310885968770357 ) ;
#6072=CARTESIAN_POINT ( 'NONE',  ( 6.281175601187043434, -3.752776749732576356, -6.500000000000000000 ) ) ;
#6075=CYLINDRICAL_SURFACE ( 'NONE', #106139, 4.000000000000000000 ) ;
#6080=DIRECTION ( 'NONE',  ( -1.000000000000000000, -0.000000000000000000, -0.000000000000000000 ) ) ;
#6084=CARTESIAN_POINT ( 'NONE',  ( 0.4042117618284671865, -3.141900367810038119, 6.500000000000000888 ) ) ;
#6091=ORIENTED_EDGE ( 'NONE', *, *, #47129, .T. ) ;
#6098=DIRECTION ( 'NONE',  ( 1.000000000000000000, 1.224606353822377258E-16, 0.000000000000000000 ) ) ;
#6125=ORIENTED_EDGE ( 'NONE', *, *, #10434, .T. ) ;
#6156=ORIENTED_EDGE ( 'NONE', *, *, #5476, .F. ) ;
#6164=VERTEX_POINT ( 'NONE', #58130 ) ;
#6201=DIRECTION ( 'NONE',  ( -1.000000000000000000, -1.224606353822377258E-16, -0.000000000000000000 ) ) ;
#6211=CONICAL_SURFACE ( 'NONE', #20062, 4.000000000000001776, 0.9599310885968808105 ) ;
#6230=DIRECTION ( 'NONE',  ( -1.000000000000000000, -1.224606353822377258E-16, -0.000000000000000000 ) ) ;
#6236=DIRECTION ( 'NONE',  ( -1.000000000000000000, -0.000000000000000000, -0.000000000000000000 ) ) ;
#6241=AXIS2_PLACEMENT_3D ( 'NONE', #45075, #2997, #19242 ) ;
#6248=AXIS2_PLACEMENT_3D ( 'NONE', #55121, #47565, #72379 ) ;
#6265=ORIENTED_EDGE ( 'NONE', *, *, #99016, .F. ) ;
#6271=CIRCLE ( 'NONE', #33636, 3.309500000000001663 ) ;
#6283=CARTESIAN_POINT ( 'NONE',  ( 18.09999999999999787, 3.309500000000003439, 4.052968581778167743E-16 ) ) ;
#6290=VERTEX_POINT ( 'NONE', #11152 ) ;
#6316=CARTESIAN_POINT ( 'NONE',  ( 39.83349330513380693, 4.000000000000002665, 0.000000000000000000 ) ) ;
#6327=ORIENTED_EDGE ( 'NONE', *, *, #30920, .T. ) ;
#6333=ORIENTED_EDGE ( 'NONE', *, *, #47887, .F. ) ;
#6357=CARTESIAN_POINT ( 'NONE',  ( 47.40949999999999420, 0.000000000000000000, 0.000000000000000000 ) ) ;
#6409=DIRECTION ( 'NONE',  ( -1.000000000000000000, -1.224606353822377258E-16, -0.000000000000000000 ) ) ;
#6416=EDGE_LOOP ( 'NONE', ( #89677, #90438, #785, #66998, #84441 ) ) ;
#6417=ORIENTED_EDGE ( 'NONE', *, *, #28581, .T. ) ;
#6449=CARTESIAN_POINT ( 'NONE',  ( 43.10000000000000142, 1.533819458162526451E-15, 0.000000000000000000 ) ) ;
#6454=CARTESIAN_POINT ( 'NONE',  ( 32.61650669486618881, 1.474610560812782335E-15, 0.000000000000000000 ) ) ;
#6455=ADVANCED_FACE ( 'NONE', ( #56915 ), #18908, .T. ) ;
#6459=ORIENTED_EDGE ( 'NONE', *, *, #40008, .T. ) ;
#6499=ORIENTED_EDGE ( 'NONE', *, *, #97094, .T. ) ;
#6504=CARTESIAN_POINT ( 'NONE',  ( 0.000000000000000000, 0.000000000000000000, 0.000000000000000000 ) ) ;
#6530=DIRECTION ( 'NONE',  ( 0.000000000000000000, -1.000000000000000000, 0.000000000000000000 ) ) ;
#6531=ORIENTED_EDGE ( 'NONE', *, *, #64000, .F. ) ;
#6539=CARTESIAN_POINT ( 'NONE',  ( 15.11650669486618881, 1.474610560812782335E-15, 0.000000000000000000 ) ) ;
#6544=ORIENTED_EDGE ( 'NONE', *, *, #78306, .F. ) ;
#6556=VECTOR ( 'NONE', #71348, 1000.000000000000114 ) ;
#6610=ADVANCED_FACE ( 'NONE', ( #83862 ), #93013, .T. ) ;
#6631=APPLICATION_CONTEXT ( 'automotive_design' ) ;
#6683=ORIENTED_EDGE ( 'NONE', *, *, #46491, .T. ) ;
#6685=ORIENTED_EDGE ( 'NONE', *, *, #41821, .F. ) ;
#6694=CARTESIAN_POINT ( 'NONE',  ( 0.000000000000000000, 4.898587196589412829E-16, -4.000000000000000000 ) ) ;
#6711=VERTEX_POINT ( 'NONE', #44486 ) ;
#6754=DIRECTION ( 'NONE',  ( -1.000000000000000000, -1.224606353822377258E-16, -0.000000000000000000 ) ) ;
#6773=CARTESIAN_POINT ( 'NONE',  ( 0.2578475836320761050, -6.890627091270383531, -1.065083781909173632 ) ) ;
#6806=ADVANCED_FACE ( 'NONE', ( #62791 ), #44245, .T. ) ;
#6812=FACE_OUTER_BOUND ( 'NONE', #85185, .T. ) ;
#6822=ORIENTED_EDGE ( 'NONE', *, *, #80311, .F. ) ;
#6856=CARTESIAN_POINT ( 'NONE',  ( 0.05533025579362120527, 6.264553569211842365, -2.149474931388136945 ) ) ;
#6887=CARTESIAN_POINT ( 'NONE',  ( 6.683837171061805194, -3.955946848495972556, -6.851900933636989599 ) ) ;
#6895=CARTESIAN_POINT ( 'NONE',  ( 11.84999999999999787, 1.533819458162526451E-15, 0.000000000000000000 ) ) ;
#6901=FACE_OUTER_BOUND ( 'NONE', #47116, .T. ) ;
#6908=ADVANCED_FACE ( 'NONE', ( #32023 ), #66486, .T. ) ;
#6915=DIRECTION ( 'NONE',  ( 0.000000000000000000, -1.000000000000000000, 0.000000000000000000 ) ) ;
#6924=VERTEX_POINT ( 'NONE', #89184 ) ;
#6956=ORIENTED_EDGE ( 'NONE', *, *, #82391, .F. ) ;
#6965=CARTESIAN_POINT ( 'NONE',  ( 25.59999999999999787, 3.309500000000003439, 0.000000000000000000 ) ) ;
#6968=CARTESIAN_POINT ( 'NONE',  ( 27.33349330513380337, -4.000000000000000000, 4.898587196589415787E-16 ) ) ;
#6982=DIRECTION ( 'NONE',  ( 0.000000000000000000, 0.000000000000000000, 1.000000000000000000 ) ) ;
#6993=VERTEX_POINT ( 'NONE', #75094 ) ;
#7024=LINE ( 'NONE', #39941, #25427 ) ;
#7031=ADVANCED_FACE ( 'NONE', ( #35768 ), #54609, .T. ) ;
#7059=EDGE_CURVE ( 'NONE', #26216, #48231, #14972, .T. ) ;
#7064=CARTESIAN_POINT ( 'NONE',  ( 26.08349330513380337, -4.000000000000000888, 4.898587196589416773E-16 ) ) ;
#7089=CIRCLE ( 'NONE', #43292, 4.000000000000001776 ) ;
#7131=ORIENTED_EDGE ( 'NONE', *, *, #24281, .T. ) ;
#7146=ORIENTED_EDGE ( 'NONE', *, *, #64988, .T. ) ;
#7150=DIRECTION ( 'NONE',  ( 0.000000000000000000, 0.000000000000000000, 1.000000000000000000 ) ) ;
#7194=VECTOR ( 'NONE', #72759, 1000.000000000000000 ) ;
#7218=DIRECTION ( 'NONE',  ( 0.000000000000000000, 0.000000000000000000, 1.000000000000000000 ) ) ;
#7230=DIRECTION ( 'NONE',  ( 0.000000000000000000, -1.000000000000000000, 0.000000000000000000 ) ) ;
#7232=LINE ( 'NONE', #80590, #75225 ) ;
#7235=AXIS2_PLACEMENT_3D ( 'NONE', #17943, #68629, #67021 ) ;
#7270=CYLINDRICAL_SURFACE ( 'NONE', #58967, 4.000000000000000000 ) ;
#7338=ORIENTED_EDGE ( 'NONE', *, *, #102153, .T. ) ;
#7361=DIRECTION ( 'NONE',  ( -1.000000000000000000, -0.000000000000000000, -0.000000000000000000 ) ) ;
#7388=CIRCLE ( 'NONE', #84859, 4.000000000000000888 ) ;
#7447=AXIS2_PLACEMENT_3D ( 'NONE', #86497, #99576, #49968 ) ;
#7453=CIRCLE ( 'NONE', #35078, 4.000000000000000888 ) ;
#7461=DIRECTION ( 'NONE',  ( 0.000000000000000000, -1.000000000000000000, 0.000000000000000000 ) ) ;
#7462=DIRECTION ( 'NONE',  ( -1.000000000000000000, -1.224606353822377258E-16, -0.000000000000000000 ) ) ;
#7464=VERTEX_POINT ( 'NONE', #106554 ) ;
#7465=CARTESIAN_POINT ( 'NONE',  ( 0.000000000000000000, -5.629165124598843661, 3.250000000000012879 ) ) ;
#7474=ORIENTED_EDGE ( 'NONE', *, *, #92468, .F. ) ;
#7492=ADVANCED_FACE ( 'NONE', ( #49912 ), #58560, .T. ) ;
#7519=ORIENTED_EDGE ( 'NONE', *, *, #69952, .T. ) ;
#7536=EDGE_CURVE ( 'NONE', #25659, #82981, #3056, .T. ) ;
#7563=CYLINDRICAL_SURFACE ( 'NONE', #80148, 4.000000000000000000 ) ;
#7590=CONICAL_SURFACE ( 'NONE', #28529, 4.000000000000001776, 0.9599310885968808105 ) ;
#7607=DIRECTION ( 'NONE',  ( -1.000000000000000000, -1.224606353822377258E-16, -0.000000000000000000 ) ) ;
#7650=ORIENTED_EDGE ( 'NONE', *, *, #36643, .F. ) ;
#7659=DIRECTION ( 'NONE',  ( 0.000000000000000000, -1.000000000000000000, 0.000000000000000000 ) ) ;
#7688=VERTEX_POINT ( 'NONE', #4566 ) ;
#7690=DIRECTION ( 'NONE',  ( 0.000000000000000000, -1.000000000000000000, 0.000000000000000000 ) ) ;
#7741=AXIS2_PLACEMENT_3D ( 'NONE', #88085, #23365, #14165 ) ;
#7742=DIRECTION ( 'NONE',  ( -1.000000000000000000, -0.000000000000000000, -0.000000000000000000 ) ) ;
#7744=FACE_OUTER_BOUND ( 'NONE', #99770, .T. ) ;
#7763=DIRECTION ( 'NONE',  ( 0.000000000000000000, -1.000000000000000000, 0.000000000000000000 ) ) ;
#7765=CIRCLE ( 'NONE', #100775, 3.309500000000001663 ) ;
#7789=VERTEX_POINT ( 'NONE', #82692 ) ;
#7819=EDGE_LOOP ( 'NONE', ( #101008, #25574, #97499 ) ) ;
#7833=AXIS2_PLACEMENT_3D ( 'NONE', #40799, #50875, #56436 ) ;
#7881=DIRECTION ( 'NONE',  ( -1.000000000000000000, -0.000000000000000000, -0.000000000000000000 ) ) ;
#7883=EDGE_CURVE ( 'NONE', #70259, #4931, #29283, .T. ) ;
#7889=EDGE_LOOP ( 'NONE', ( #29118, #28576, #11638, #100553, #86715 ) ) ;
#7910=AXIS2_PLACEMENT_3D ( 'NONE', #42163, #17912, #83674 ) ;
#7929=ORIENTED_EDGE ( 'NONE', *, *, #66113, .F. ) ;
#7948=AXIS2_PLACEMENT_3D ( 'NONE', #1244, #100499, #58995 ) ;
#7951=DIRECTION ( 'NONE',  ( -1.000000000000000000, -1.224606353822377258E-16, -0.000000000000000000 ) ) ;
#8006=EDGE_LOOP ( 'NONE', ( #45604, #27234, #103690, #61023, #39753 ) ) ;
#8020=CARTESIAN_POINT ( 'NONE',  ( 31.08349330513380337, -7.703719777548943412E-31, 4.000000000000001776 ) ) ;
#8056=CONICAL_SURFACE ( 'NONE', #16691, 3.309500000000001663, 0.9599310885968770357 ) ;
#8063=ORIENTED_EDGE ( 'NONE', *, *, #89598, .F. ) ;
#8080=ORIENTED_EDGE ( 'NONE', *, *, #103768, .F. ) ;
#8092=CARTESIAN_POINT ( 'NONE',  ( 6.289692432696784685, -1.240516797660047330E-13, -6.828989928337167115 ) ) ;
#8115=AXIS2_PLACEMENT_3D ( 'NONE', #65937, #6098, #97236 ) ;
#8124=EDGE_LOOP ( 'NONE', ( #17862, #35310, #103852, #28932, #19631 ) ) ;
#8128=CIRCLE ( 'NONE', #87387, 4.000000000000000888 ) ;
#8166=FACE_OUTER_BOUND ( 'NONE', #88022, .T. ) ;
#8210=ORIENTED_EDGE ( 'NONE', *, *, #38510, .T. ) ;
#8225=AXIS2_PLACEMENT_3D ( 'NONE', #44438, #3977, #56067 ) ;
#8227=ORIENTED_EDGE ( 'NONE', *, *, #99870, .F. ) ;
#8255=EDGE_CURVE ( 'NONE', #100726, #74863, #98240, .T. ) ;
#8261=CIRCLE ( 'NONE', #34111, 3.309500000000001663 ) ;
#8284=AXIS2_PLACEMENT_3D ( 'NONE', #50459, #82305, #40782 ) ;
#8299=DIRECTION ( 'NONE',  ( -1.000000000000000000, -1.224606353822377258E-16, -0.000000000000000000 ) ) ;
#8300=ORIENTED_EDGE ( 'NONE', *, *, #28946, .F. ) ;
#8311=ORIENTED_EDGE ( 'NONE', *, *, #69339, .F. ) ;
#8318=VECTOR ( 'NONE', #47721, 1000.000000000000114 ) ;
#8322=CARTESIAN_POINT ( 'NONE',  ( 39.34999999999999432, 1.533819458162526451E-15, 0.000000000000000000 ) ) ;
#8327=AXIS2_PLACEMENT_3D ( 'NONE', #79707, #30662, #87285 ) ;
#8391=AXIS2_PLACEMENT_3D ( 'NONE', #5608, #5087, #38020 ) ;
#8423=DIRECTION ( 'NONE',  ( 0.000000000000000000, -1.000000000000000000, 0.000000000000000000 ) ) ;
#8430=VERTEX_POINT ( 'NONE', #105638 ) ;
#8467=ORIENTED_EDGE ( 'NONE', *, *, #38306, .F. ) ;
#8469=CARTESIAN_POINT ( 'NONE',  ( 23.58349330513380337, 1.593028355512270567E-15, 0.000000000000000000 ) ) ;
#8474=AXIS2_PLACEMENT_3D ( 'NONE', #94505, #86422, #68639 ) ;
#8475=ORIENTED_EDGE ( 'NONE', *, *, #76436, .F. ) ;
#8490=VERTEX_POINT ( 'NONE', #19751 ) ;
#8522=VECTOR ( 'NONE', #27763, 1000.000000000000000 ) ;
#8531=ORIENTED_EDGE ( 'NONE', *, *, #29602, .T. ) ;
#8541=CARTESIAN_POINT ( 'NONE',  ( 0.06682554136338023087, -4.993536075455418555, 4.350941807883115686 ) ) ;
#8547=EDGE_CURVE ( 'NONE', #6290, #79598, #11055, .T. ) ;
#8574=AXIS2_PLACEMENT_3D ( 'NONE', #40128, #65994, #97825 ) ;
#8633=CIRCLE ( 'NONE', #60560, 3.309500000000001663 ) ;
#8639=AXIS2_PLACEMENT_3D ( 'NONE', #77776, #10365, #76696 ) ;
#8670=CARTESIAN_POINT ( 'NONE',  ( 6.326416241096633364, 1.324101276589543907, 6.831531844319975733 ) ) ;
#8677=ORIENTED_EDGE ( 'NONE', *, *, #56086, .T. ) ;
#8685=AXIS2_PLACEMENT_3D ( 'NONE', #37824, #22150, #39391 ) ;
#8687=DIRECTION ( 'NONE',  ( -1.000000000000000000, -1.224606353822377258E-16, -0.000000000000000000 ) ) ;
#8695=EDGE_LOOP ( 'NONE', ( #29852, #52762, #66387 ) ) ;
#8710=CIRCLE ( 'NONE', #20874, 4.000000000000000888 ) ;
#8725=ADVANCED_FACE ( 'NONE', ( #84066 ), #26407, .T. ) ;
#8756=VERTEX_POINT ( 'NONE', #42533 ) ;
#8761=ORIENTED_EDGE ( 'NONE', *, *, #57096, .T. ) ;
#8785=CARTESIAN_POINT ( 'NONE',  ( 18.09999999999999787, 3.309500000000003439, 0.000000000000000000 ) ) ;
#8796=CARTESIAN_POINT ( 'NONE',  ( 10.11650669486618881, 1.474610560812782335E-15, 0.000000000000000000 ) ) ;
#8811=FACE_OUTER_BOUND ( 'NONE', #419, .T. ) ;
#8838=CARTESIAN_POINT ( 'NONE',  ( 9.833493305133801599, 4.000000000000003553, 0.000000000000000000 ) ) ;
#8841=ORIENTED_EDGE ( 'NONE', *, *, #47129, .F. ) ;
#8856=ORIENTED_EDGE ( 'NONE', *, *, #23714, .F. ) ;
#8872=DIRECTION ( 'NONE',  ( 0.000000000000000000, -1.000000000000000000, 0.000000000000000000 ) ) ;
#8887=ADVANCED_FACE ( 'NONE', ( #94837 ), #15082, .T. ) ;
#8892=EDGE_CURVE ( 'NONE', #49207, #26696, #70011, .T. ) ;
#8925=CIRCLE ( 'NONE', #17579, 4.000000000000000888 ) ;
#8936=ORIENTED_EDGE ( 'NONE', *, *, #18048, .F. ) ;
#8954=CARTESIAN_POINT ( 'NONE',  ( 36.36650669486618881, 4.000000000000003553, 4.898587196589414801E-16 ) ) ;
#8969=DIRECTION ( 'NONE',  ( 1.000000000000000000, 0.000000000000000000, 0.000000000000000000 ) ) ;
#9004=ORIENTED_EDGE ( 'NONE', *, *, #83556, .F. ) ;
#9007=CARTESIAN_POINT ( 'NONE',  ( 6.585468679846620432, 3.617797563910807312, -6.733790807807556789 ) ) ;
#9018=CARTESIAN_POINT ( 'NONE',  ( 18.86650669486618881, -3.999999999999998224, 0.000000000000000000 ) ) ;
#9024=FACE_OUTER_BOUND ( 'NONE', #92995, .T. ) ;
#9043=DIRECTION ( 'NONE',  ( -1.000000000000000000, -1.224606353822377258E-16, -0.000000000000000000 ) ) ;
#9047=DIRECTION ( 'NONE',  ( -1.000000000000000000, -1.224606353822377258E-16, -0.000000000000000000 ) ) ;
#9049=CARTESIAN_POINT ( 'NONE',  ( 14.34999999999999787, -3.309499999999999886, 4.475777889183790779E-16 ) ) ;
#9052=DIRECTION ( 'NONE',  ( 0.000000000000000000, -1.000000000000000000, 0.000000000000000000 ) ) ;
#9080=DIRECTION ( 'NONE',  ( 0.5735764363510462704, 0.8191520442889915765, 0.000000000000000000 ) ) ;
#9104=CARTESIAN_POINT ( 'NONE',  ( 15.11650669486618881, 1.474610560812782335E-15, 0.000000000000000000 ) ) ;
#9136=ADVANCED_FACE ( 'NONE', ( #17629 ), #1944, .T. ) ;
#9159=DIRECTION ( 'NONE',  ( 0.5735764363510462704, 0.8191520442889915765, 0.000000000000000000 ) ) ;
#9171=VECTOR ( 'NONE', #87564, 1000.000000000000114 ) ;
#9180=AXIS2_PLACEMENT_3D ( 'NONE', #6895, #360, #91032 ) ;
#9183=DIRECTION ( 'NONE',  ( -1.000000000000000000, -0.000000000000000000, -0.000000000000000000 ) ) ;
#9200=CARTESIAN_POINT ( 'NONE',  ( 28.86650669486618881, -3.999999999999998224, 0.000000000000000000 ) ) ;
#9207=CARTESIAN_POINT ( 'NONE',  ( 39.83349330513380693, 1.593028355512270567E-15, 0.000000000000000000 ) ) ;
#9260=B_SPLINE_CURVE_WITH_KNOTS ( 'NONE', 3,
 ( #46402, #4882, #81267, #40292, #64582, #12949 ),
 .UNSPECIFIED., .F., .F.,
 ( 4, 2, 4 ),
 ( 0.000000000000000000, 0.0003491763592121701330, 0.0006983527184243402660 ),
 .UNSPECIFIED. ) ;
#9263=CARTESIAN_POINT ( 'NONE',  ( 30.59999999999999787, 1.533819458162526451E-15, 0.000000000000000000 ) ) ;
#9270=CARTESIAN_POINT ( 'NONE',  ( 0.000000000000000000, 0.000000000000000000, 0.000000000000000000 ) ) ;
#9273=AXIS2_PLACEMENT_3D ( 'NONE', #57695, #74420, #42060 ) ;
#9279=VERTEX_POINT ( 'NONE', #60105 ) ;
#9295=DIRECTION ( 'NONE',  ( 1.000000000000000000, 1.224606353822377258E-16, 0.000000000000000000 ) ) ;
#9297=LINE ( 'NONE', #33612, #90499 ) ;
#9318=CARTESIAN_POINT ( 'NONE',  ( 44.83349330513380693, 4.898587196589405926E-16, -4.000000000000001776 ) ) ;
#9324=CARTESIAN_POINT ( 'NONE',  ( 45.59999999999999432, -3.309499999999999886, 4.475777889183790779E-16 ) ) ;
#9329=CYLINDRICAL_SURFACE ( 'NONE', #63293, 4.000000000000000000 ) ;
#9339=ORIENTED_EDGE ( 'NONE', *, *, #18724, .T. ) ;
#9345=EDGE_CURVE ( 'NONE', #65882, #94111, #37430, .T. ) ;
#9368=CARTESIAN_POINT ( 'NONE',  ( 0.5805565836007701153, -7.505553499465148271, -1.383738442504732931E-16 ) ) ;
#9414=DIRECTION ( 'NONE',  ( 0.000000000000000000, -1.000000000000000000, 0.000000000000000000 ) ) ;
#9429=VECTOR ( 'NONE', #95370, 1000.000000000000000 ) ;
#9435=ADVANCED_FACE ( 'NONE', ( #103194 ), #103715, .T. ) ;
#9442=AXIS2_PLACEMENT_3D ( 'NONE', #53530, #54564, #36853 ) ;
#9474=EDGE_CURVE ( 'NONE', #88304, #6711, #64658, .T. ) ;
#9480=DIRECTION ( 'NONE',  ( 1.000000000000000000, 1.224606353822377258E-16, 0.000000000000000000 ) ) ;
#9532=DIRECTION ( 'NONE',  ( 1.000000000000000000, 1.224606353822377258E-16, 0.000000000000000000 ) ) ;
#9540=CARTESIAN_POINT ( 'NONE',  ( 43.58349330513380693, 4.000000000000002665, 0.000000000000000000 ) ) ;
#9563=CARTESIAN_POINT ( 'NONE',  ( -3.482999479109682994E-15, 5.309483803148794756, 3.803704290982253600 ) ) ;
#9566=DIRECTION ( 'NONE',  ( -1.000000000000000000, -1.224606353822377258E-16, -0.000000000000000000 ) ) ;
#9571=DIRECTION ( 'NONE',  ( 0.000000000000000000, -1.000000000000000000, 0.000000000000000000 ) ) ;
#9586=ADVANCED_FACE ( 'NONE', ( #63007 ), #871, .T. ) ;
#9600=VERTEX_POINT ( 'NONE', #35710 ) ;
#9605=EDGE_CURVE ( 'NONE', #30104, #18278, #40481, .T. ) ;
#9609=DIRECTION ( 'NONE',  ( 0.000000000000000000, -1.000000000000000000, 0.000000000000000000 ) ) ;
#9610=CARTESIAN_POINT ( 'NONE',  ( 6.683837171061802529, 3.955946848495962787, 6.851900933636986935 ) ) ;
#9634=CONICAL_SURFACE ( 'NONE', #6248, 4.000000000000001776, 0.9599310885968808105 ) ;
#9637=CARTESIAN_POINT ( 'NONE',  ( 21.08349330513380337, 4.000000000000003553, 0.000000000000000000 ) ) ;
#9640=ORIENTED_EDGE ( 'NONE', *, *, #59985, .F. ) ;
#9648=DIRECTION ( 'NONE',  ( 0.000000000000000000, -1.000000000000000000, 0.000000000000000000 ) ) ;
#9663=AXIS2_PLACEMENT_3D ( 'NONE', #106670, #64125, #6915 ) ;
#9711=ORIENTED_EDGE ( 'NONE', *, *, #98224, .T. ) ;
#9737=DIRECTION ( 'NONE',  ( 0.000000000000000000, -1.000000000000000000, 0.000000000000000000 ) ) ;
#9744=VERTEX_POINT ( 'NONE', #105572 ) ;
#9747=CIRCLE ( 'NONE', #83837, 6.500000000000000888 ) ;
#9752=CARTESIAN_POINT ( 'NONE',  ( 6.162888688655347558, 7.505553499465140277, 0.000000000000000000 ) ) ;
#9755=DIRECTION ( 'NONE',  ( -1.000000000000000000, -1.224606353822377258E-16, -0.000000000000000000 ) ) ;
#9760=CARTESIAN_POINT ( 'NONE',  ( 31.08349330513380337, -4.000000000000000000, 4.898587196589415787E-16 ) ) ;
#9776=VERTEX_POINT ( 'NONE', #24687 ) ;
#9789=VECTOR ( 'NONE', #31553, 1000.000000000000000 ) ;
#9791=FACE_OUTER_BOUND ( 'NONE', #41223, .T. ) ;
#9827=EDGE_CURVE ( 'NONE', #14924, #25868, #33647, .T. ) ;
#9911=AXIS2_PLACEMENT_3D ( 'NONE', #15832, #81602, #40635 ) ;
#9912=CARTESIAN_POINT ( 'NONE',  ( 11.08349330513380160, 1.593028355512270567E-15, 0.000000000000000000 ) ) ;
#9927=CARTESIAN_POINT ( 'NONE',  ( 43.58349330513380693, -4.000000000000000888, 4.898587196589416773E-16 ) ) ;
#9930=CARTESIAN_POINT ( 'NONE',  ( 21.36650669486618881, 1.474610560812782335E-15, 0.000000000000000000 ) ) ;
#9935=DIRECTION ( 'NONE',  ( -1.000000000000000000, -1.224606353822377258E-16, -0.000000000000000000 ) ) ;
#9936=DIRECTION ( 'NONE',  ( 0.000000000000000000, -1.000000000000000000, 0.000000000000000000 ) ) ;
#9941=VERTEX_POINT ( 'NONE', #52644 ) ;
#9946=CARTESIAN_POINT ( 'NONE',  ( 44.83349330513380693, -7.703719777548943412E-31, 4.000000000000001776 ) ) ;
#9969=CARTESIAN_POINT ( 'NONE',  ( 40.11650669486618881, -3.999999999999998224, 0.000000000000000000 ) ) ;
#9972=CONICAL_SURFACE ( 'NONE', #51312, 4.000000000000001776, 0.9599310885968808105 ) ;
#10006=EDGE_LOOP ( 'NONE', ( #83353, #104840, #41816, #98617, #86006 ) ) ;
#10019=FACE_OUTER_BOUND ( 'NONE', #53870, .T. ) ;
#10044=AXIS2_PLACEMENT_3D ( 'NONE', #29349, #39539, #70308 ) ;
#10061=CARTESIAN_POINT ( 'NONE',  ( 41.08349330513380693, -7.703719777548943412E-31, 4.000000000000001776 ) ) ;
#10084=CARTESIAN_POINT ( 'NONE',  ( 21.08349330513380337, 4.000000000000002665, 0.000000000000000000 ) ) ;
#10095=CARTESIAN_POINT ( 'NONE',  ( 32.33349330513379982, -4.000000000000000888, 4.898587196589416773E-16 ) ) ;
#10121=DIRECTION ( 'NONE',  ( 0.000000000000000000, -1.000000000000000000, 0.000000000000000000 ) ) ;
#10128=CARTESIAN_POINT ( 'NONE',  ( 16.36650669486618881, 4.898587196589411843E-16, -4.000000000000000888 ) ) ;
#10208=ORIENTED_EDGE ( 'NONE', *, *, #69262, .T. ) ;
#10224=FACE_OUTER_BOUND ( 'NONE', #18021, .T. ) ;
#10254=AXIS2_PLACEMENT_3D ( 'NONE', #65429, #9295, #98323 ) ;
#10275=CARTESIAN_POINT ( 'NONE',  ( 26.36650669486618881, -3.851859888774471706E-31, 4.000000000000000888 ) ) ;
#10285=ADVANCED_FACE ( 'NONE', ( #72026 ), #7270, .T. ) ;
#10329=CARTESIAN_POINT ( 'NONE',  ( 5.819846122303831137, -4.937269551422888370, 4.448398286272754909 ) ) ;
#10339=CARTESIAN_POINT ( 'NONE',  ( 34.83349330513379982, 1.593028355512270567E-15, 0.000000000000000000 ) ) ;
#10360=DIRECTION ( 'NONE',  ( 0.000000000000000000, -1.000000000000000000, 0.000000000000000000 ) ) ;
#10365=DIRECTION ( 'NONE',  ( -1.000000000000000000, -1.224606353822377258E-16, -0.000000000000000000 ) ) ;
#10374=LINE ( 'NONE', #43289, #63585 ) ;
#10376=ORIENTED_EDGE ( 'NONE', *, *, #74414, .T. ) ;
#10392=AXIS2_PLACEMENT_3D ( 'NONE', #92441, #74660, #34255 ) ;
#10434=EDGE_CURVE ( 'NONE', #92260, #74342, #93463, .T. ) ;
#10459=EDGE_LOOP ( 'NONE', ( #31431, #72869, #82775, #99577, #6333, #16627 ) ) ;
#10464=CARTESIAN_POINT ( 'NONE',  ( 0.01372220897661637073, 5.309964801958114933, -3.802871176606130277 ) ) ;
#10481=LINE ( 'NONE', #99040, #43870 ) ;
#10490=CARTESIAN_POINT ( 'NONE',  ( 6.281175601187043434, -7.505553499465149159, -1.184821369511938456E-16 ) ) ;
#10495=AXIS2_PLACEMENT_3D ( 'NONE', #11938, #36797, #29761 ) ;
#10516=DIRECTION ( 'NONE',  ( -1.000000000000000000, -1.224606353822377258E-16, -0.000000000000000000 ) ) ;
#10527=CYLINDRICAL_SURFACE ( 'NONE', #39462, 4.000000000000000000 ) ;
#10546=DIRECTION ( 'NONE',  ( 0.000000000000000000, -1.000000000000000000, 0.000000000000000000 ) ) ;
#10553=VERTEX_POINT ( 'NONE', #19679 ) ;
#10561=CIRCLE ( 'NONE', #36418, 3.309500000000001663 ) ;
#10567=FACE_OUTER_BOUND ( 'NONE', #43000, .T. ) ;
#10574=CARTESIAN_POINT ( 'NONE',  ( 0.000000000000000000, 0.000000000000000000, 0.000000000000000000 ) ) ;
#10579=CARTESIAN_POINT ( 'NONE',  ( 6.692588830498425345, 3.932766476276031486, 6.892929031562513131 ) ) ;
#10582=VERTEX_POINT ( 'NONE', #89680 ) ;
#10600=VECTOR ( 'NONE', #78051, 1000.000000000000000 ) ;
#10613=ORIENTED_EDGE ( 'NONE', *, *, #22675, .F. ) ;
#10614=DIRECTION ( 'NONE',  ( 0.000000000000000000, 0.8660254037844375974, -0.5000000000000019984 ) ) ;
#10616=CARTESIAN_POINT ( 'NONE',  ( 11.36650669486618881, 1.474610560812782335E-15, 0.000000000000000000 ) ) ;
#10621=EDGE_CURVE ( 'NONE', #40315, #54371, #72936, .T. ) ;
#10626=ORIENTED_EDGE ( 'NONE', *, *, #36730, .T. ) ;
#10657=CONICAL_SURFACE ( 'NONE', #64058, 4.000000000000001776, 0.9599310885968808105 ) ;
#10686=DIRECTION ( 'NONE',  ( 0.000000000000000000, -1.000000000000000000, 0.000000000000000000 ) ) ;
#10696=CARTESIAN_POINT ( 'NONE',  ( 9.349999999999997868, 1.533819458162526451E-15, 0.000000000000000000 ) ) ;
#10704=VERTEX_POINT ( 'NONE', #56208 ) ;
#10728=AXIS2_PLACEMENT_3D ( 'NONE', #14983, #57033, #47878 ) ;
#10734=CYLINDRICAL_SURFACE ( 'NONE', #12806, 4.000000000000000000 ) ;
#10742=CARTESIAN_POINT ( 'NONE',  ( 34.35000000000000142, -3.309499999999999886, 4.475777889183790779E-16 ) ) ;
#10773=ORIENTED_EDGE ( 'NONE', *, *, #57096, .F. ) ;
#10777=CARTESIAN_POINT ( 'NONE',  ( 27.33349330513380337, -4.000000000000000888, 4.898587196589416773E-16 ) ) ;
#10800=CARTESIAN_POINT ( 'NONE',  ( 12.33349330513380337, 4.000000000000003553, 0.000000000000000000 ) ) ;
#10834=ORIENTED_EDGE ( 'NONE', *, *, #15481, .T. ) ;
#10848=CARTESIAN_POINT ( 'NONE',  ( 6.333820801334183237, -4.275724398228409662, 5.594228103108734196 ) ) ;
#10852=ORIENTED_EDGE ( 'NONE', *, *, #18048, .T. ) ;
#10867=CARTESIAN_POINT ( 'NONE',  ( 0.000000000000000000, -5.629165124598848990, -3.250000000000003553 ) ) ;
#10889=DIRECTION ( 'NONE',  ( 0.000000000000000000, -1.000000000000000000, 0.000000000000000000 ) ) ;
#10903=CARTESIAN_POINT ( 'NONE',  ( 41.85000000000000142, 3.309500000000003439, 4.052968581778167743E-16 ) ) ;
#10946=DIRECTION ( 'NONE',  ( -1.000000000000000000, -1.224606353822377258E-16, -0.000000000000000000 ) ) ;
#10947=AXIS2_PLACEMENT_3D ( 'NONE', #77343, #94609, #45521 ) ;
#10988=CARTESIAN_POINT ( 'NONE',  ( 6.445370176741509916, -4.584736124522773792, -5.738941594273985203 ) ) ;
#10996=ORIENTED_EDGE ( 'NONE', *, *, #1876, .F. ) ;
#10998=ORIENTED_EDGE ( 'NONE', *, *, #43431, .F. ) ;
#11035=ORIENTED_EDGE ( 'NONE', *, *, #2241, .T. ) ;
#11055=LINE ( 'NONE', #12653, #47788 ) ;
#11075=ORIENTED_EDGE ( 'NONE', *, *, #24444, .F. ) ;
#11111=CONICAL_SURFACE ( 'NONE', #71401, 4.000000000000001776, 0.9599310885968808105 ) ;
#11117=CARTESIAN_POINT ( 'NONE',  ( 47.40949999999999420, 4.898587196589412829E-16, -4.000000000000000000 ) ) ;
#11128=VERTEX_POINT ( 'NONE', #90609 ) ;
#11134=ORIENTED_EDGE ( 'NONE', *, *, #59096, .F. ) ;
#11152=CARTESIAN_POINT ( 'NONE',  ( 44.35000000000000142, 3.309500000000003439, 0.000000000000000000 ) ) ;
#11156=VECTOR ( 'NONE', #40605, 1000.000000000000000 ) ;
#11168=LINE ( 'NONE', #58688, #11532 ) ;
#11178=EDGE_CURVE ( 'NONE', #1155, #105753, #74285, .T. ) ;
#11183=FACE_OUTER_BOUND ( 'NONE', #8695, .T. ) ;
#11191=ORIENTED_EDGE ( 'NONE', *, *, #76380, .T. ) ;
#11197=CARTESIAN_POINT ( 'NONE',  ( 11.36650669486618881, 1.474610560812782335E-15, 0.000000000000000000 ) ) ;
#11200=AXIS2_PLACEMENT_3D ( 'NONE', #77743, #11383, #102541 ) ;
#11231=ADVANCED_FACE ( 'NONE', ( #96465 ), #88371, .T. ) ;
#11254=ORIENTED_EDGE ( 'NONE', *, *, #31122, .T. ) ;
#11258=EDGE_LOOP ( 'NONE', ( #59528, #64672, #5808, #93860, #4341 ) ) ;
#11299=CARTESIAN_POINT ( 'NONE',  ( 16.84999999999999787, 1.533819458162526451E-15, 0.000000000000000000 ) ) ;
#11300=VECTOR ( 'NONE', #24988, 1000.000000000000000 ) ;
#11302=DIRECTION ( 'NONE',  ( -1.000000000000000000, -1.224606353822377258E-16, -0.000000000000000000 ) ) ;
#11308=DIRECTION ( 'NONE',  ( -1.000000000000000000, -1.224606353822377258E-16, -0.000000000000000000 ) ) ;
#11309=DIRECTION ( 'NONE',  ( 0.000000000000000000, 1.000000000000000000, 0.000000000000000000 ) ) ;
#11331=DIRECTION ( 'NONE',  ( 1.000000000000000000, 1.224606353822377258E-16, 0.000000000000000000 ) ) ;
#11382=AXIS2_PLACEMENT_3D ( 'NONE', #41168, #22889, #16899 ) ;
#11383=DIRECTION ( 'NONE',  ( -1.000000000000000000, -1.224606353822377258E-16, -0.000000000000000000 ) ) ;
#11436=AXIS2_PLACEMENT_3D ( 'NONE', #61500, #94391, #11309 ) ;
#11442=VECTOR ( 'NONE', #95255, 1000.000000000000114 ) ;
#11466=ORIENTED_EDGE ( 'NONE', *, *, #32565, .F. ) ;
#11473=ORIENTED_EDGE ( 'NONE', *, *, #14774, .T. ) ;
#11510=CARTESIAN_POINT ( 'NONE',  ( 9.833493305133801599, 4.898587196589405926E-16, -4.000000000000001776 ) ) ;
#11532=VECTOR ( 'NONE', #93174, 1000.000000000000000 ) ;
#11543=EDGE_CURVE ( 'NONE', #89196, #106610, #24610, .T. ) ;
#11551=DIRECTION ( 'NONE',  ( -1.000000000000000000, -0.000000000000000000, -0.000000000000000000 ) ) ;
#11571=EDGE_CURVE ( 'NONE', #47451, #9744, #10481, .T. ) ;
#11580=CONICAL_SURFACE ( 'NONE', #85683, 4.000000000000001776, 0.9599310885968808105 ) ;
#11636=CARTESIAN_POINT ( 'NONE',  ( 0.000000000000000000, 4.898587196589412829E-16, -4.000000000000000000 ) ) ;
#11638=ORIENTED_EDGE ( 'NONE', *, *, #17136, .F. ) ;
#11681=AXIS2_PLACEMENT_3D ( 'NONE', #30076, #79660, #86194 ) ;
#11725=CONICAL_SURFACE ( 'NONE', #32410, 3.309500000000001663, 0.9599310885968770357 ) ;
#11732=DIRECTION ( 'NONE',  ( -1.000000000000000000, -1.224606353822377258E-16, -0.000000000000000000 ) ) ;
#11735=CARTESIAN_POINT ( 'NONE',  ( 11.08349330513380160, 1.593028355512270567E-15, 0.000000000000000000 ) ) ;
#11741=CARTESIAN_POINT ( 'NONE',  ( 6.394337469123803075, 3.776351736504755863, -6.540833074877203224 ) ) ;
#11747=EDGE_CURVE ( 'NONE', #44445, #84797, #64746, .T. ) ;
#11760=ORIENTED_EDGE ( 'NONE', *, *, #105357, .F. ) ;
#11772=ORIENTED_EDGE ( 'NONE', *, *, #50787, .F. ) ;
#11792=VERTEX_POINT ( 'NONE', #41882 ) ;
#11795=CARTESIAN_POINT ( 'NONE',  ( 12.61650669486618881, 1.474610560812782335E-15, 0.000000000000000000 ) ) ;
#11798=AXIS2_PLACEMENT_3D ( 'NONE', #103522, #62545, #57472 ) ;
#11847=CIRCLE ( 'NONE', #96265, 4.000000000000000888 ) ;
#11849=CONICAL_SURFACE ( 'NONE', #99708, 4.000000000000001776, 0.9599310885968808105 ) ;
#11856=CARTESIAN_POINT ( 'NONE',  ( 6.683837171061802529, -3.955946848495957457, 6.851900933636990487 ) ) ;
#11890=CARTESIAN_POINT ( 'NONE',  ( 5.947762761376474749, 6.880090707843042885, -1.083333333333332593 ) ) ;
#11915=LINE ( 'NONE', #26559, #55456 ) ;
#11927=AXIS2_PLACEMENT_3D ( 'NONE', #98087, #6409, #39347 ) ;
#11933=CARTESIAN_POINT ( 'NONE',  ( 11.36650669486618881, 4.000000000000003553, 4.898587196589414801E-16 ) ) ;
#11938=CARTESIAN_POINT ( 'NONE',  ( 44.83349330513380693, 1.593028355512270567E-15, 0.000000000000000000 ) ) ;
#11957=EDGE_CURVE ( 'NONE', #8490, #59552, #56781, .T. ) ;
#12065=VECTOR ( 'NONE', #70873, 1000.000000000000000 ) ;
#12139=EDGE_LOOP ( 'NONE', ( #49016, #102623, #62677, #70598, #88685 ) ) ;
#12141=DIRECTION ( 'NONE',  ( -1.000000000000000000, -1.224606353822377258E-16, -0.000000000000000000 ) ) ;
#12187=ORIENTED_EDGE ( 'NONE', *, *, #67408, .T. ) ;
#12211=EDGE_LOOP ( 'NONE', ( #100735, #55417, #103120, #53084, #23845, #69797 ) ) ;
#12213=DIRECTION ( 'NONE',  ( -1.000000000000000000, -1.224606353822377258E-16, -0.000000000000000000 ) ) ;
#12231=DIRECTION ( 'NONE',  ( -1.000000000000000000, -0.000000000000000000, -0.000000000000000000 ) ) ;
#12233=EDGE_CURVE ( 'NONE', #26186, #99054, #97869, .T. ) ;
#12251=DIRECTION ( 'NONE',  ( 1.000000000000000000, 1.224606353822377258E-16, 0.000000000000000000 ) ) ;
#12277=DIRECTION ( 'NONE',  ( 0.000000000000000000, 1.000000000000000000, 0.000000000000000000 ) ) ;
#12283=DIRECTION ( 'NONE',  ( -1.000000000000000000, -1.224606353822377258E-16, -0.000000000000000000 ) ) ;
#12290=ORIENTED_EDGE ( 'NONE', *, *, #46788, .F. ) ;
#12317=ORIENTED_EDGE ( 'NONE', *, *, #32550, .F. ) ;
#12352=CARTESIAN_POINT ( 'NONE',  ( 26.08349330513380337, 1.593028355512270567E-15, 0.000000000000000000 ) ) ;
#12376=DIRECTION ( 'NONE',  ( -1.000000000000000000, -1.224606353822377258E-16, -0.000000000000000000 ) ) ;
#12382=ORIENTED_EDGE ( 'NONE', *, *, #73314, .F. ) ;
#12383=DIRECTION ( 'NONE',  ( -1.000000000000000000, -1.224606353822377258E-16, -0.000000000000000000 ) ) ;
#12391=ORIENTED_EDGE ( 'NONE', *, *, #68412, .T. ) ;
#12463=CARTESIAN_POINT ( 'NONE',  ( 18.58349330513380337, 1.593028355512270567E-15, 0.000000000000000000 ) ) ;
#12492=DIRECTION ( 'NONE',  ( -1.000000000000000000, -0.000000000000000000, -0.000000000000000000 ) ) ;
#12496=DIRECTION ( 'NONE',  ( 0.000000000000000000, -1.000000000000000000, 0.000000000000000000 ) ) ;
#12520=DIRECTION ( 'NONE',  ( 0.000000000000000000, -1.000000000000000000, 0.000000000000000000 ) ) ;
#12540=ORIENTED_EDGE ( 'NONE', *, *, #23345, .F. ) ;
#12553=ADVANCED_FACE ( 'NONE', ( #20197 ), #54473, .T. ) ;
#12562=ORIENTED_EDGE ( 'NONE', *, *, #55159, .T. ) ;
#12567=CARTESIAN_POINT ( 'NONE',  ( 0.000000000000000000, 0.000000000000000000, 0.000000000000000000 ) ) ;
#12569=FACE_OUTER_BOUND ( 'NONE', #100330, .T. ) ;
#12578=ADVANCED_FACE ( 'NONE', ( #105314 ), #6075, .T. ) ;
#12586=LINE ( 'NONE', #37448, #79869 ) ;
#12595=CARTESIAN_POINT ( 'NONE',  ( 26.08349330513380337, 1.593028355512270567E-15, 0.000000000000000000 ) ) ;
#12627=DIRECTION ( 'NONE',  ( 1.000000000000000000, 1.224606353822377258E-16, 0.000000000000000000 ) ) ;
#12653=CARTESIAN_POINT ( 'NONE',  ( 44.35000000000000142, 3.309500000000003439, 4.052968581778167743E-16 ) ) ;
#12659=CARTESIAN_POINT ( 'NONE',  ( 46.08349330513379982, -7.703719777548943412E-31, 4.000000000000001776 ) ) ;
#12682=DIRECTION ( 'NONE',  ( 0.000000000000000000, -1.000000000000000000, 0.000000000000000000 ) ) ;
#12711=DIRECTION ( 'NONE',  ( 0.000000000000000000, -1.000000000000000000, 0.000000000000000000 ) ) ;
#12716=ORIENTED_EDGE ( 'NONE', *, *, #104489, .F. ) ;
#12719=DIRECTION ( 'NONE',  ( -1.000000000000000000, -1.224606353822377258E-16, -0.000000000000000000 ) ) ;
#12743=DIRECTION ( 'NONE',  ( -1.000000000000000000, -0.000000000000000000, -0.000000000000000000 ) ) ;
#12749=DIRECTION ( 'NONE',  ( 1.000000000000000000, 1.224606353822377258E-16, 0.000000000000000000 ) ) ;
#12754=DIRECTION ( 'NONE',  ( 0.000000000000000000, -1.000000000000000000, 0.000000000000000000 ) ) ;
#12773=ORIENTED_EDGE ( 'NONE', *, *, #35328, .T. ) ;
#12779=CARTESIAN_POINT ( 'NONE',  ( 0.000000000000000000, 0.000000000000000000, 0.000000000000000000 ) ) ;
#12780=ORIENTED_EDGE ( 'NONE', *, *, #26095, .F. ) ;
#12804=CARTESIAN_POINT ( 'NONE',  ( 25.59999999999999787, 3.309500000000003439, 4.052968581778167743E-16 ) ) ;
#12806=AXIS2_PLACEMENT_3D ( 'NONE', #52263, #85177, #17798 ) ;
#12831=CIRCLE ( 'NONE', #21502, 4.000000000000000888 ) ;
#12876=CARTESIAN_POINT ( 'NONE',  ( 47.33349330513379982, -4.000000000000000888, 4.898587196589416773E-16 ) ) ;
#12879=DIRECTION ( 'NONE',  ( 0.000000000000000000, -1.000000000000000000, 0.000000000000000000 ) ) ;
#12892=ORIENTED_EDGE ( 'NONE', *, *, #63025, .T. ) ;
#12900=CARTESIAN_POINT ( 'NONE',  ( 0.5805565836007643421, -3.752776749732575468, -6.499999999999999112 ) ) ;
#12922=VECTOR ( 'NONE', #42197, 1000.000000000000000 ) ;
#12947=DIRECTION ( 'NONE',  ( 0.000000000000000000, -1.000000000000000000, 0.000000000000000000 ) ) ;
#12949=CARTESIAN_POINT ( 'NONE',  ( 6.683837171061802529, -3.955946848495957457, 6.851900933636990487 ) ) ;
#12958=VERTEX_POINT ( 'NONE', #11117 ) ;
#12959=ORIENTED_EDGE ( 'NONE', *, *, #2626, .F. ) ;
#13048=DIRECTION ( 'NONE',  ( 1.000000000000000000, 1.224606353822377258E-16, 0.000000000000000000 ) ) ;
#13060=CIRCLE ( 'NONE', #30347, 3.309500000000001663 ) ;
#13069=ORIENTED_EDGE ( 'NONE', *, *, #39543, .F. ) ;
#13070=DIRECTION ( 'NONE',  ( 0.000000000000000000, -1.000000000000000000, 0.000000000000000000 ) ) ;
#13104=CARTESIAN_POINT ( 'NONE',  ( 24.83349330513380337, 4.000000000000003553, 0.000000000000000000 ) ) ;
#13105=VECTOR ( 'NONE', #68142, 1000.000000000000000 ) ;
#13107=CARTESIAN_POINT ( 'NONE',  ( 42.61650669486618881, 1.474610560812782335E-15, 0.000000000000000000 ) ) ;
#13108=EDGE_LOOP ( 'NONE', ( #5319, #28807, #56157, #95901, #21461 ) ) ;
#13128=EDGE_LOOP ( 'NONE', ( #55173, #34032, #28595, #43085, #37741 ) ) ;
#13129=CARTESIAN_POINT ( 'NONE',  ( 14.83349330513380337, -4.000000000000000000, 4.898587196589415787E-16 ) ) ;
#13151=AXIS2_PLACEMENT_3D ( 'NONE', #76747, #75688, #50341 ) ;
#13159=ADVANCED_FACE ( 'NONE', ( #33714 ), #51991, .F. ) ;
#13199=CARTESIAN_POINT ( 'NONE',  ( 14.34999999999999787, -3.309499999999999886, 0.000000000000000000 ) ) ;
#13216=CIRCLE ( 'NONE', #83828, 4.000000000000001776 ) ;
#13230=CARTESIAN_POINT ( 'NONE',  ( 5.691929483231188414, -5.629165124598859649, -3.250000000000000000 ) ) ;
#13232=EDGE_LOOP ( 'NONE', ( #83488, #82351, #104105, #76348, #86745, #49815 ) ) ;
#13246=DIRECTION ( 'NONE',  ( -1.000000000000000000, -1.224606353822377258E-16, -0.000000000000000000 ) ) ;
#13249=DIRECTION ( 'NONE',  ( 0.000000000000000000, -1.000000000000000000, 0.000000000000000000 ) ) ;
#13282=AXIS2_PLACEMENT_3D ( 'NONE', #92652, #2038, #2573 ) ;
#13295=CARTESIAN_POINT ( 'NONE',  ( 0.000000000000000000, 0.000000000000000000, 4.000000000000000000 ) ) ;
#13309=VERTEX_POINT ( 'NONE', #10095 ) ;
#13315=ORIENTED_EDGE ( 'NONE', *, *, #29658, .T. ) ;
#13334=CARTESIAN_POINT ( 'NONE',  ( 27.61650669486618881, 1.474610560812782335E-15, 0.000000000000000000 ) ) ;
#13342=CARTESIAN_POINT ( 'NONE',  ( 28.86650669486618881, -3.851859888774471706E-31, 4.000000000000000888 ) ) ;
#13352=DIRECTION ( 'NONE',  ( 0.000000000000000000, 1.000000000000000000, 0.000000000000000000 ) ) ;
#13357=FACE_OUTER_BOUND ( 'NONE', #75662, .T. ) ;
#13361=CIRCLE ( 'NONE', #22027, 4.000000000000000888 ) ;
#13384=ADVANCED_FACE ( 'NONE', ( #51612 ), #36017, .T. ) ;
#13392=FACE_OUTER_BOUND ( 'NONE', #98686, .T. ) ;
#13412=AXIS2_PLACEMENT_3D ( 'NONE', #79163, #54876, #87806 ) ;
#13436=ADVANCED_FACE ( 'NONE', ( #57303 ), #14327, .F. ) ;
#13448=ORIENTED_EDGE ( 'NONE', *, *, #17572, .T. ) ;
#13466=EDGE_CURVE ( 'NONE', #48174, #52776, #57835, .T. ) ;
#13494=DIRECTION ( 'NONE',  ( -1.000000000000000000, -1.224606353822377258E-16, -0.000000000000000000 ) ) ;
#13504=CARTESIAN_POINT ( 'NONE',  ( 18.58349330513380337, 4.898587196589405926E-16, -4.000000000000001776 ) ) ;
#13527=AXIS2_PLACEMENT_3D ( 'NONE', #49622, #82530, #41009 ) ;
#13528=CARTESIAN_POINT ( 'NONE',  ( 9.349999999999997868, -3.309499999999999886, 0.000000000000000000 ) ) ;
#13530=ORIENTED_EDGE ( 'NONE', *, *, #56516, .T. ) ;
#13532=DIRECTION ( 'NONE',  ( 0.000000000000000000, -1.000000000000000000, 0.000000000000000000 ) ) ;
#13533=DIRECTION ( 'NONE',  ( 0.000000000000000000, -1.000000000000000000, 0.000000000000000000 ) ) ;
#13536=EDGE_CURVE ( 'NONE', #74863, #866, #100432, .T. ) ;
#13541=VERTEX_POINT ( 'NONE', #75080 ) ;
#13559=EDGE_CURVE ( 'NONE', #39684, #59572, #68075, .T. ) ;
#13560=CARTESIAN_POINT ( 'NONE',  ( 6.162888688655344005, 3.752776749732565253, 6.499999999999997335 ) ) ;
#13567=DIRECTION ( 'NONE',  ( 0.5735764363510466035, -0.8191520442889914655, 1.003171929053524500E-16 ) ) ;
#13580=EDGE_CURVE ( 'NONE', #69803, #67441, #42264, .T. ) ;
#13605=DIRECTION ( 'NONE',  ( -1.000000000000000000, -1.224606353822377258E-16, -0.000000000000000000 ) ) ;
#13616=CIRCLE ( 'NONE', #86033, 3.309500000000001663 ) ;
#13629=CARTESIAN_POINT ( 'NONE',  ( 18.09999999999999787, 1.533819458162526451E-15, 0.000000000000000000 ) ) ;
#13640=FACE_OUTER_BOUND ( 'NONE', #50609, .T. ) ;
#13665=DIRECTION ( 'NONE',  ( 0.5735764363510466035, -0.8191520442889914655, 1.003171929053524500E-16 ) ) ;
#13676=DIRECTION ( 'NONE',  ( -1.000000000000000000, -1.224606353822377258E-16, -0.000000000000000000 ) ) ;
#13680=CARTESIAN_POINT ( 'NONE',  ( 14.83349330513380337, -4.000000000000000888, 4.898587196589416773E-16 ) ) ;
#13713=ADVANCED_FACE ( 'NONE', ( #14591 ), #7563, .T. ) ;
#13722=ADVANCED_FACE ( 'NONE', ( #24333 ), #30834, .T. ) ;
#13735=CARTESIAN_POINT ( 'NONE',  ( 0.000000000000000000, 0.000000000000000000, 0.000000000000000000 ) ) ;
#13746=EDGE_LOOP ( 'NONE', ( #80081, #83090, #34403, #95995, #3448 ) ) ;
#13767=CARTESIAN_POINT ( 'NONE',  ( 17.33349330513380337, -4.000000000000000888, 4.898587196589416773E-16 ) ) ;
#13771=ORIENTED_EDGE ( 'NONE', *, *, #46719, .F. ) ;
#13775=LINE ( 'NONE', #94190, #94813 ) ;
#13778=CARTESIAN_POINT ( 'NONE',  ( 6.683837171061802529, -3.955946848495957457, 6.851900933636990487 ) ) ;
#13786=CARTESIAN_POINT ( 'NONE',  ( 32.61650669486618881, -3.999999999999998224, 0.000000000000000000 ) ) ;
#13799=AXIS2_PLACEMENT_3D ( 'NONE', #52960, #84268, #35212 ) ;
#13823=EDGE_CURVE ( 'NONE', #2814, #68944, #1592, .T. ) ;
#13855=EDGE_LOOP ( 'NONE', ( #42750, #8531, #23802, #20332, #8080, #100520 ) ) ;
#13873=DIRECTION ( 'NONE',  ( 0.000000000000000000, -1.000000000000000000, 0.000000000000000000 ) ) ;
#13884=DIRECTION ( 'NONE',  ( -1.000000000000000000, -1.224606353822377258E-16, -0.000000000000000000 ) ) ;
#13904=CARTESIAN_POINT ( 'NONE',  ( 14.83349330513380337, 1.593028355512270567E-15, 0.000000000000000000 ) ) ;
#13909=LINE ( 'NONE', #103470, #79192 ) ;
#13920=DIRECTION ( 'NONE',  ( 0.000000000000000000, 0.000000000000000000, 1.000000000000000000 ) ) ;
#13934=AXIS2_PLACEMENT_3D ( 'NONE', #18337, #99758, #35059 ) ;
#13961=CIRCLE ( 'NONE', #91532, 4.000000000000000888 ) ;
#13998=VERTEX_POINT ( 'NONE', #65951 ) ;
#14015=CARTESIAN_POINT ( 'NONE',  ( 8.099999999999999645, 0.000000000000000000, 0.000000000000000000 ) ) ;
#14016=AXIS2_PLACEMENT_3D ( 'NONE', #87756, #47789, #4710 ) ;
#14038=ORIENTED_EDGE ( 'NONE', *, *, #18377, .F. ) ;
#14040=EDGE_CURVE ( 'NONE', #103934, #102391, #116, .T. ) ;
#14092=AXIS2_PLACEMENT_3D ( 'NONE', #21955, #46732, #70489 ) ;
#14094=CARTESIAN_POINT ( 'NONE',  ( 6.338255145484064990, 2.729868969638910681, -6.500000000000574651 ) ) ;
#14130=EDGE_LOOP ( 'NONE', ( #39997, #9004, #83688, #100107, #102610 ) ) ;
#14150=PLANE ( 'NONE',  #66776 ) ;
#14165=DIRECTION ( 'NONE',  ( 0.000000000000000000, 0.000000000000000000, 1.000000000000000000 ) ) ;
#14167=ORIENTED_EDGE ( 'NONE', *, *, #53785, .T. ) ;
#14179=CARTESIAN_POINT ( 'NONE',  ( 14.34999999999999787, 3.309500000000003439, 4.052968581778167743E-16 ) ) ;
#14219=EDGE_CURVE ( 'NONE', #35426, #58076, #58395, .T. ) ;
#14220=DIRECTION ( 'NONE',  ( -1.000000000000000000, -1.224606353822377258E-16, -0.000000000000000000 ) ) ;
#14259=DIRECTION ( 'NONE',  ( -0.5735764363510497121, 0.8191520442889892450, 1.003171929053521665E-16 ) ) ;
#14262=EDGE_CURVE ( 'NONE', #32527, #72439, #75055, .T. ) ;
#14277=CARTESIAN_POINT ( 'NONE',  ( 8.099999999999999645, 0.000000000000000000, 0.000000000000000000 ) ) ;
#14288=ORIENTED_EDGE ( 'NONE', *, *, #51124, .F. ) ;
#14294=DIRECTION ( 'NONE',  ( -1.000000000000000000, -1.224606353822377258E-16, -0.000000000000000000 ) ) ;
#14306=CARTESIAN_POINT ( 'NONE',  ( 6.463344223170840230, -4.601472318010336515, 5.710032555828793654 ) ) ;
#14318=ORIENTED_EDGE ( 'NONE', *, *, #31122, .F. ) ;
#14327=PLANE ( 'NONE',  #54193 ) ;
#14348=CARTESIAN_POINT ( 'NONE',  ( 36.08349330513379982, -4.000000000000000000, 4.898587196589415787E-16 ) ) ;
#14370=ORIENTED_EDGE ( 'NONE', *, *, #66560, .T. ) ;
#14378=CIRCLE ( 'NONE', #100556, 4.000000000000000888 ) ;
#14404=ORIENTED_EDGE ( 'NONE', *, *, #74546, .F. ) ;
#14418=CIRCLE ( 'NONE', #66096, 4.000000000000001776 ) ;
#14427=EDGE_LOOP ( 'NONE', ( #98575, #40594, #41584, #99596, #40924 ) ) ;
#14432=DIRECTION ( 'NONE',  ( 0.000000000000000000, 1.000000000000000000, 0.000000000000000000 ) ) ;
#14485=ORIENTED_EDGE ( 'NONE', *, *, #17646, .T. ) ;
#14495=FACE_OUTER_BOUND ( 'NONE', #81348, .T. ) ;
#14499=ADVANCED_FACE ( 'NONE', ( #39594 ), #32572, .T. ) ;
#14508=CIRCLE ( 'NONE', #78287, 4.000000000000000888 ) ;
#14522=CIRCLE ( 'NONE', #81728, 4.000000000000000888 ) ;
#14527=DIRECTION ( 'NONE',  ( -1.000000000000000000, -1.224606353822377258E-16, -0.000000000000000000 ) ) ;
#14532=DIRECTION ( 'NONE',  ( 0.000000000000000000, -1.000000000000000000, 0.000000000000000000 ) ) ;
#14588=CARTESIAN_POINT ( 'NONE',  ( 23.58349330513380337, 1.593028355512270567E-15, 0.000000000000000000 ) ) ;
#14591=FACE_OUTER_BOUND ( 'NONE', #90066, .T. ) ;
#14613=ORIENTED_EDGE ( 'NONE', *, *, #74414, .F. ) ;
#14620=DIRECTION ( 'NONE',  ( -1.000000000000000000, -1.224606353822377258E-16, -0.000000000000000000 ) ) ;
#14636=DIRECTION ( 'NONE',  ( -1.000000000000000000, -1.224606353822377258E-16, -0.000000000000000000 ) ) ;
#14684=CARTESIAN_POINT ( 'NONE',  ( 22.33349330513380337, 4.898587196589405926E-16, -4.000000000000001776 ) ) ;
#14691=CARTESIAN_POINT ( 'NONE',  ( 0.000000000000000000, 0.000000000000000000, 0.000000000000000000 ) ) ;
#14697=CARTESIAN_POINT ( 'NONE',  ( 12.33349330513380337, 4.898587196589405926E-16, -4.000000000000001776 ) ) ;
#14712=ORIENTED_EDGE ( 'NONE', *, *, #30508, .F. ) ;
#14747=DIRECTION ( 'NONE',  ( 0.000000000000000000, -1.000000000000000000, 0.000000000000000000 ) ) ;
#14770=ADVANCED_FACE ( 'NONE', ( #93839 ), #92307, .T. ) ;
#14774=EDGE_CURVE ( 'NONE', #75040, #103547, #102718, .T. ) ;
#14841=CARTESIAN_POINT ( 'NONE',  ( 6.463481858019720860, -7.246446802359431949, 1.128819432756288599 ) ) ;
#14842=ORIENTED_EDGE ( 'NONE', *, *, #96907, .T. ) ;
#14848=DIRECTION ( 'NONE',  ( -1.000000000000000000, -1.224606353822377258E-16, -0.000000000000000000 ) ) ;
#14855=ORIENTED_EDGE ( 'NONE', *, *, #32565, .T. ) ;
#14861=ORIENTED_EDGE ( 'NONE', *, *, #5983, .F. ) ;
#14865=DIRECTION ( 'NONE',  ( -1.000000000000000000, -1.224606353822377258E-16, -0.000000000000000000 ) ) ;
#14875=DIRECTION ( 'NONE',  ( 1.000000000000000000, 0.000000000000000000, -0.000000000000000000 ) ) ;
#14898=ORIENTED_EDGE ( 'NONE', *, *, #1983, .T. ) ;
#14911=AXIS2_PLACEMENT_3D ( 'NONE', #2193, #9755, #68011 ) ;
#14920=ORIENTED_EDGE ( 'NONE', *, *, #48323, .T. ) ;
#14924=VERTEX_POINT ( 'NONE', #55992 ) ;
#14955=ADVANCED_FACE ( 'NONE', ( #24748 ), #82429, .T. ) ;
#14972=CIRCLE ( 'NONE', #99416, 4.000000000000001776 ) ;
#14983=CARTESIAN_POINT ( 'NONE',  ( 0.000000000000000000, 0.000000000000000000, 0.000000000000000000 ) ) ;
#14995=VECTOR ( 'NONE', #73285, 1000.000000000000000 ) ;
#15008=DIRECTION ( 'NONE',  ( 0.000000000000000000, -1.000000000000000000, 0.000000000000000000 ) ) ;
#15017=CARTESIAN_POINT ( 'NONE',  ( 45.11650669486618881, -3.999999999999998224, 0.000000000000000000 ) ) ;
#15019=AXIS2_PLACEMENT_3D ( 'NONE', #87920, #14527, #29713 ) ;
#15041=CARTESIAN_POINT ( 'NONE',  ( 36.84999999999999432, 1.533819458162526451E-15, 0.000000000000000000 ) ) ;
#15048=DIRECTION ( 'NONE',  ( 0.000000000000000000, -1.000000000000000000, 0.000000000000000000 ) ) ;
#15082=CONICAL_SURFACE ( 'NONE', #87408, 3.309500000000001663, 0.9599310885968770357 ) ;
#15088=ORIENTED_EDGE ( 'NONE', *, *, #285, .F. ) ;
#15091=DIRECTION ( 'NONE',  ( -0.5735764363510497121, 0.8191520442889892450, 1.003171929053521665E-16 ) ) ;
#15134=CARTESIAN_POINT ( 'NONE',  ( 6.463647488011505793, -2.646730816809989228, 6.840026438643557860 ) ) ;
#15142=AXIS2_PLACEMENT_3D ( 'NONE', #100753, #102357, #44135 ) ;
#15160=AXIS2_PLACEMENT_3D ( 'NONE', #82957, #25838, #68383 ) ;
#15162=DIRECTION ( 'NONE',  ( -1.000000000000000000, -1.224606353822377258E-16, -0.000000000000000000 ) ) ;
#15175=CIRCLE ( 'NONE', #75468, 4.000000000000001776 ) ;
#15204=CARTESIAN_POINT ( 'NONE',  ( 0.000000000000000000, 0.000000000000000000, 4.000000000000000000 ) ) ;
#15225=CIRCLE ( 'NONE', #44738, 4.000000000000001776 ) ;
#15264=CARTESIAN_POINT ( 'NONE',  ( 0.000000000000000000, 4.898587196589412829E-16, -4.000000000000000000 ) ) ;
#15265=ORIENTED_EDGE ( 'NONE', *, *, #71479, .F. ) ;
#15291=LINE ( 'NONE', #32029, #102540 ) ;
#15317=CARTESIAN_POINT ( 'NONE',  ( 6.326622418652846136, 1.327077765692999733, -6.831545684615175418 ) ) ;
#15328=ORIENTED_EDGE ( 'NONE', *, *, #4440, .F. ) ;
#15335=CARTESIAN_POINT ( 'NONE',  ( 0.05458999538792581874, -1.264741368075138706, -6.499999999999999112 ) ) ;
#15338=DIRECTION ( 'NONE',  ( 0.000000000000000000, 0.000000000000000000, -1.000000000000000000 ) ) ;
#15353=ORIENTED_EDGE ( 'NONE', *, *, #2460, .F. ) ;
#15372=VERTEX_POINT ( 'NONE', #9318 ) ;
#15381=CARTESIAN_POINT ( 'NONE',  ( 31.08349330513380337, 1.593028355512270567E-15, 0.000000000000000000 ) ) ;
#15412=DIRECTION ( 'NONE',  ( 0.5735764363510466035, -0.8191520442889914655, 1.003171929053524500E-16 ) ) ;
#15416=AXIS2_PLACEMENT_3D ( 'NONE', #75488, #69018, #60923 ) ;
#15430=ORIENTED_EDGE ( 'NONE', *, *, #100437, .T. ) ;
#15434=CARTESIAN_POINT ( 'NONE',  ( 1.107919095008624844E-15, -5.309483803148806302, -3.803704290982252711 ) ) ;
#15438=CARTESIAN_POINT ( 'NONE',  ( 35.11650669486618170, 1.474610560812782335E-15, 0.000000000000000000 ) ) ;
#15449=CONICAL_SURFACE ( 'NONE', #47922, 3.309500000000001663, 0.9599310885968770357 ) ;
#15481=EDGE_CURVE ( 'NONE', #45468, #95564, #18519, .T. ) ;
#15501=ORIENTED_EDGE ( 'NONE', *, *, #77459, .T. ) ;
#15508=ORIENTED_EDGE ( 'NONE', *, *, #33199, .F. ) ;
#15523=CARTESIAN_POINT ( 'NONE',  ( 37.61650669486618881, 1.474610560812782335E-15, 0.000000000000000000 ) ) ;
#15545=AXIS2_PLACEMENT_3D ( 'NONE', #67709, #100590, #26750 ) ;
#15548=ADVANCED_FACE ( 'NONE', ( #71286 ), #75284, .T. ) ;
#15562=CARTESIAN_POINT ( 'NONE',  ( 18.86650669486618881, 4.898587196589411843E-16, -4.000000000000000888 ) ) ;
#15567=ORIENTED_EDGE ( 'NONE', *, *, #44424, .T. ) ;
#15637=ORIENTED_EDGE ( 'NONE', *, *, #67931, .F. ) ;
#15653=AXIS2_PLACEMENT_3D ( 'NONE', #88503, #57691, #48547 ) ;
#15665=DIRECTION ( 'NONE',  ( -1.000000000000000000, -0.000000000000000000, -0.000000000000000000 ) ) ;
#15685=AXIS2_PLACEMENT_3D ( 'NONE', #71601, #48386, #65111 ) ;
#15687=B_SPLINE_CURVE_WITH_KNOTS ( 'NONE', 3,
 ( #99256, #27029, #82566, #8670, #59912, #84168 ),
 .UNSPECIFIED., .F., .F.,
 ( 4, 2, 4 ),
 ( 0.000000000000000000, 0.001995463903526787514, 0.003990927807053575027 ),
 .UNSPECIFIED. ) ;
#15716=CARTESIAN_POINT ( 'NONE',  ( 35.59999999999999432, 1.533819458162526451E-15, 0.000000000000000000 ) ) ;
#15723=EDGE_CURVE ( 'NONE', #9744, #76326, #106228, .T. ) ;
#15726=ORIENTED_EDGE ( 'NONE', *, *, #31715, .T. ) ;
#15778=CARTESIAN_POINT ( 'NONE',  ( 0.000000000000000000, 0.000000000000000000, 4.000000000000000000 ) ) ;
#15786=EDGE_CURVE ( 'NONE', #20310, #75040, #20239, .T. ) ;
#15791=ORIENTED_EDGE ( 'NONE', *, *, #34418, .T. ) ;
#15809=DIRECTION ( 'NONE',  ( 0.5735764363510462704, 0.8191520442889915765, 0.000000000000000000 ) ) ;
#15815=EDGE_CURVE ( 'NONE', #6164, #86885, #37470, .T. ) ;
#15832=CARTESIAN_POINT ( 'NONE',  ( 25.59999999999999787, 1.533819458162526451E-15, 0.000000000000000000 ) ) ;
#15843=CARTESIAN_POINT ( 'NONE',  ( 34.35000000000000142, 1.533819458162526451E-15, 0.000000000000000000 ) ) ;
#15847=DIRECTION ( 'NONE',  ( 0.000000000000000000, -1.000000000000000000, 0.000000000000000000 ) ) ;
#15849=CARTESIAN_POINT ( 'NONE',  ( 6.683837171061802529, 3.955946848495958346, -6.851900933636989599 ) ) ;
#15867=ORIENTED_EDGE ( 'NONE', *, *, #37443, .F. ) ;
#15873=ADVANCED_FACE ( 'NONE', ( #69062 ), #54644, .T. ) ;
#15903=CIRCLE ( 'NONE', #100283, 4.000000000000001776 ) ;
#15963=LINE ( 'NONE', #81733, #101987 ) ;
#16001=CARTESIAN_POINT ( 'NONE',  ( 0.000000000000000000, 0.000000000000000000, 0.000000000000000000 ) ) ;
#16042=CARTESIAN_POINT ( 'NONE',  ( 6.222742520105469133, 3.584500230190539316, -6.791463481567638460 ) ) ;
#16066=EDGE_CURVE ( 'NONE', #63698, #26216, #77069, .T. ) ;
#16109=ORIENTED_EDGE ( 'NONE', *, *, #15786, .F. ) ;
#16114=EDGE_CURVE ( 'NONE', #54299, #81845, #14418, .T. ) ;
#16136=ORIENTED_EDGE ( 'NONE', *, *, #41821, .T. ) ;
#16143=DIRECTION ( 'NONE',  ( 0.000000000000000000, -1.000000000000000000, 0.000000000000000000 ) ) ;
#16154=VERTEX_POINT ( 'NONE', #19022 ) ;
#16166=VECTOR ( 'NONE', #13567, 1000.000000000000000 ) ;
#16167=CARTESIAN_POINT ( 'NONE',  ( 6.562974947121710478, 4.277474787035884241, -6.282829635893496523 ) ) ;
#16173=ORIENTED_EDGE ( 'NONE', *, *, #23274, .F. ) ;
#16192=CARTESIAN_POINT ( 'NONE',  ( 6.563035550597769330, -3.302680408004400991, 6.845819698387220598 ) ) ;
#16200=ADVANCED_FACE ( 'NONE', ( #50783 ), #98868, .T. ) ;
#16210=ORIENTED_EDGE ( 'NONE', *, *, #62542, .F. ) ;
#16211=EDGE_CURVE ( 'NONE', #27527, #7464, #83695, .T. ) ;
#16238=ORIENTED_EDGE ( 'NONE', *, *, #58104, .T. ) ;
#16255=ORIENTED_EDGE ( 'NONE', *, *, #104668, .F. ) ;
#16264=ORIENTED_EDGE ( 'NONE', *, *, #40608, .F. ) ;
#16284=ORIENTED_EDGE ( 'NONE', *, *, #79485, .T. ) ;
#16287=ORIENTED_EDGE ( 'NONE', *, *, #74546, .T. ) ;
#16315=AXIS2_PLACEMENT_3D ( 'NONE', #48230, #23474, #31043 ) ;
#16354=VERTEX_POINT ( 'NONE', #95010 ) ;
#16416=ORIENTED_EDGE ( 'NONE', *, *, #8892, .T. ) ;
#16483=( BOUNDED_SURFACE ( )  B_SPLINE_SURFACE ( 3, 2, ( 
 ( #35583, #43637, #101350 ),
 ( #36129, #68997, #101872 ),
 ( #28032, #60903, #44719 ),
 ( #77607, #36656, #69520 ),
 ( #62461, #18845, #85680 ),
 ( #94298, #52760, #68968 ),
 ( #19389, #52221, #70014 ),
 ( #61946, #86749, #68429 ) ),
 .UNSPECIFIED., .F., .F., .F. ) 
 B_SPLINE_SURFACE_WITH_KNOTS ( ( 4, 2, 2, 4 ),
 ( 3, 3 ),
 ( 0.03205733154476830132, 0.03606343422293256662, 0.03806648556201469580, 0.04006953690109683192 ),
 ( 0.000000000000000000, 1.000000000000000000 ),
 .UNSPECIFIED. ) 
 GEOMETRIC_REPRESENTATION_ITEM ( )  RATIONAL_B_SPLINE_SURFACE ( (
 ( 1.000000000000000000, 0.8047781205924506853, 1.000000000000000000),
 ( 1.000000000000000000, 0.8123783054473237009, 1.000000000000000000),
 ( 1.000000000000000000, 0.8190665327891030190, 1.000000000000000000),
 ( 1.000000000000000000, 0.8191934993920665375, 1.000000000000000000),
 ( 1.000000000000000000, 0.8176088856299702501, 1.000000000000000000),
 ( 1.000000000000000000, 0.8122958243107715193, 1.000000000000000000),
 ( 1.000000000000000000, 0.8086309198479471050, 1.000000000000000000),
 ( 1.000000000000000000, 0.8047712443299024354, 1.000000000000000000) ) ) 
 REPRESENTATION_ITEM ( '' )  SURFACE ( )  );
#16496=ORIENTED_EDGE ( 'NONE', *, *, #47816, .T. ) ;
#16518=CARTESIAN_POINT ( 'NONE',  ( 23.86650669486618881, 1.474610560812782335E-15, 0.000000000000000000 ) ) ;
#16529=EDGE_LOOP ( 'NONE', ( #39971, #24978, #105122, #77480, #54463, #83624 ) ) ;
#16546=CONICAL_SURFACE ( 'NONE', #57872, 3.309500000000001663, 0.9599310885968770357 ) ;
#16567=ORIENTED_EDGE ( 'NONE', *, *, #28385, .T. ) ;
#16569=ORIENTED_EDGE ( 'NONE', *, *, #81711, .F. ) ;
#16580=CARTESIAN_POINT ( 'NONE',  ( 5.975663821523083286, 4.257391242883784344, -5.625982059626467802 ) ) ;
#16584=DIRECTION ( 'NONE',  ( 0.000000000000000000, -1.000000000000000000, 0.000000000000000000 ) ) ;
#16589=CARTESIAN_POINT ( 'NONE',  ( 6.683837171061806082, 7.911893696991934455, 7.436622852660996417E-19 ) ) ;
#16597=DIRECTION ( 'NONE',  ( 0.000000000000000000, 1.000000000000000000, 0.000000000000000000 ) ) ;
#16618=DIRECTION ( 'NONE',  ( 0.000000000000000000, -1.000000000000000000, 0.000000000000000000 ) ) ;
#16621=DIRECTION ( 'NONE',  ( -1.000000000000000000, -1.224606353822377258E-16, -0.000000000000000000 ) ) ;
#16623=CONICAL_SURFACE ( 'NONE', #52808, 3.309500000000001663, 0.9599310885968770357 ) ;
#16627=ORIENTED_EDGE ( 'NONE', *, *, #45301, .F. ) ;
#16631=DIRECTION ( 'NONE',  ( -1.000000000000000000, -0.000000000000000000, -0.000000000000000000 ) ) ;
#16651=ORIENTED_EDGE ( 'NONE', *, *, #4968, .T. ) ;
#16656=ORIENTED_EDGE ( 'NONE', *, *, #21272, .T. ) ;
#16684=ADVANCED_FACE ( 'NONE', ( #92729 ), #10734, .T. ) ;
#16688=ORIENTED_EDGE ( 'NONE', *, *, #44488, .F. ) ;
#16691=AXIS2_PLACEMENT_3D ( 'NONE', #5374, #38293, #47400 ) ;
#16732=FACE_OUTER_BOUND ( 'NONE', #70923, .T. ) ;
#16740=EDGE_CURVE ( 'NONE', #33104, #43441, #43649, .T. ) ;
#16749=VERTEX_POINT ( 'NONE', #27517 ) ;
#16754=DIRECTION ( 'NONE',  ( 0.000000000000000000, -1.000000000000000000, 0.000000000000000000 ) ) ;
#16782=EDGE_CURVE ( 'NONE', #55816, #79598, #55830, .T. ) ;
#16806=ORIENTED_EDGE ( 'NONE', *, *, #37517, .F. ) ;
#16811=CARTESIAN_POINT ( 'NONE',  ( 0.000000000000000000, 0.000000000000000000, 0.000000000000000000 ) ) ;
#16822=DIRECTION ( 'NONE',  ( 0.000000000000000000, -1.000000000000000000, 0.000000000000000000 ) ) ;
#16835=ORIENTED_EDGE ( 'NONE', *, *, #105556, .T. ) ;
#16840=EDGE_CURVE ( 'NONE', #25868, #96063, #76555, .T. ) ;
#16854=ORIENTED_EDGE ( 'NONE', *, *, #56086, .F. ) ;
#16873=EDGE_LOOP ( 'NONE', ( #12716, #60138, #58162, #94005, #34673 ) ) ;
#16880=EDGE_CURVE ( 'NONE', #8756, #30104, #69533, .T. ) ;
#16899=DIRECTION ( 'NONE',  ( 0.000000000000000000, 0.000000000000000000, 1.000000000000000000 ) ) ;
#16903=AXIS2_PLACEMENT_3D ( 'NONE', #27820, #87085, #53113 ) ;
#16908=ADVANCED_FACE ( 'NONE', ( #6901 ), #11111, .T. ) ;
#16916=B_SPLINE_CURVE_WITH_KNOTS ( 'NONE', 3,
 ( #87548, #5550, #96172, #22302, #6072, #72409 ),
 .UNSPECIFIED., .F., .F.,
 ( 4, 2, 4 ),
 ( -4.698498716301142229E-06, 0.0003457374136927998383, 0.0006961733261019008171 ),
 .UNSPECIFIED. ) ;
#16925=CARTESIAN_POINT ( 'NONE',  ( 0.000000000000000000, 0.000000000000000000, 0.000000000000000000 ) ) ;
#16929=CARTESIAN_POINT ( 'NONE',  ( 36.08349330513379982, -7.703719777548943412E-31, 4.000000000000001776 ) ) ;
#16944=CARTESIAN_POINT ( 'NONE',  ( 43.86650669486618881, 4.898587196589411843E-16, -4.000000000000000888 ) ) ;
#16953=EDGE_CURVE ( 'NONE', #42491, #80498, #98953, .T. ) ;
#16955=CIRCLE ( 'NONE', #84080, 3.309500000000001663 ) ;
#16983=ORIENTED_EDGE ( 'NONE', *, *, #46780, .T. ) ;
#16985=DIRECTION ( 'NONE',  ( -1.000000000000000000, -1.224606353822377258E-16, -0.000000000000000000 ) ) ;
#17011=CARTESIAN_POINT ( 'NONE',  ( 6.643884894376894223, -7.802125718944335375, 4.061124033062993374E-12 ) ) ;
#17025=CARTESIAN_POINT ( 'NONE',  ( 10.59999999999999609, 1.533819458162526451E-15, 0.000000000000000000 ) ) ;
#17060=DIRECTION ( 'NONE',  ( 0.000000000000000000, 1.000000000000000000, 0.000000000000000000 ) ) ;
#17061=ORIENTED_EDGE ( 'NONE', *, *, #86349, .T. ) ;
#17072=ORIENTED_EDGE ( 'NONE', *, *, #56000, .F. ) ;
#17076=EDGE_CURVE ( 'NONE', #12958, #40315, #102198, .T. ) ;
#17127=CARTESIAN_POINT ( 'NONE',  ( 6.289692432696804225, 5.239086202715451002, -4.583616368338175207 ) ) ;
#17136=EDGE_CURVE ( 'NONE', #4391, #81365, #41917, .T. ) ;
#17144=DIRECTION ( 'NONE',  ( -1.000000000000000000, -1.224606353822377258E-16, -0.000000000000000000 ) ) ;
#17159=CARTESIAN_POINT ( 'NONE',  ( 0.5805565836007605673, 3.752776749732565253, 6.499999999999997335 ) ) ;
#17171=DIRECTION ( 'NONE',  ( -1.000000000000000000, -1.224606353822377258E-16, -0.000000000000000000 ) ) ;
#17180=DIRECTION ( 'NONE',  ( 0.000000000000000000, 0.000000000000000000, 1.000000000000000000 ) ) ;
#17186=ORIENTED_EDGE ( 'NONE', *, *, #66634, .T. ) ;
#17191=ORIENTED_EDGE ( 'NONE', *, *, #93644, .F. ) ;
#17212=CARTESIAN_POINT ( 'NONE',  ( 28.58349330513380337, 4.000000000000002665, 0.000000000000000000 ) ) ;
#17222=ORIENTED_EDGE ( 'NONE', *, *, #62626, .F. ) ;
#17244=DIRECTION ( 'NONE',  ( -1.000000000000000000, -1.224606353822377258E-16, -0.000000000000000000 ) ) ;
#17271=LINE ( 'NONE', #97622, #27946 ) ;
#17272=CIRCLE ( 'NONE', #15545, 4.000000000000001776 ) ;
#17274=DIRECTION ( 'NONE',  ( -1.000000000000000000, -1.224606353822377258E-16, -0.000000000000000000 ) ) ;
#17287=AXIS2_PLACEMENT_3D ( 'NONE', #69771, #61702, #94594 ) ;
#17298=FACE_OUTER_BOUND ( 'NONE', #31600, .T. ) ;
#17311=ORIENTED_EDGE ( 'NONE', *, *, #80192, .T. ) ;
#17331=EDGE_LOOP ( 'NONE', ( #85703, #14920, #65742, #56077, #58794 ) ) ;
#17332=CONICAL_SURFACE ( 'NONE', #34602, 6.500000000000000000, 1.047197551196600296 ) ;
#17333=DIRECTION ( 'NONE',  ( 0.000000000000000000, 0.000000000000000000, -1.000000000000000000 ) ) ;
#17345=EDGE_LOOP ( 'NONE', ( #11191, #95108, #54883 ) ) ;
#17362=EDGE_CURVE ( 'NONE', #2115, #74776, #93686, .T. ) ;
#17402=CIRCLE ( 'NONE', #27825, 4.000000000000001776 ) ;
#17412=CARTESIAN_POINT ( 'NONE',  ( 21.84999999999999787, -3.309499999999999886, 0.000000000000000000 ) ) ;
#17432=DIRECTION ( 'NONE',  ( -0.5735764363510497121, 0.8191520442889892450, 1.003171929053521665E-16 ) ) ;
#17478=EDGE_LOOP ( 'NONE', ( #67641, #35875, #77440, #55530, #68792 ) ) ;
#17493=CIRCLE ( 'NONE', #27840, 4.000000000000001776 ) ;
#17495=ORIENTED_EDGE ( 'NONE', *, *, #50787, .T. ) ;
#17572=EDGE_CURVE ( 'NONE', #43166, #59552, #57309, .T. ) ;
#17574=DIRECTION ( 'NONE',  ( -1.000000000000000000, -0.000000000000000000, -0.000000000000000000 ) ) ;
#17579=AXIS2_PLACEMENT_3D ( 'NONE', #35475, #24467, #106385 ) ;
#17581=VERTEX_POINT ( 'NONE', #67149 ) ;
#17591=LINE ( 'NONE', #41841, #27051 ) ;
#17595=CONICAL_SURFACE ( 'NONE', #14092, 3.309500000000001663, 0.9599310885968770357 ) ;
#17614=DIRECTION ( 'NONE',  ( -1.000000000000000000, -1.224606353822377258E-16, -0.000000000000000000 ) ) ;
#17619=AXIS2_PLACEMENT_3D ( 'NONE', #27213, #53574, #94032 ) ;
#17627=CARTESIAN_POINT ( 'NONE',  ( 34.83349330513379982, -4.000000000000000888, 4.898587196589416773E-16 ) ) ;
#17629=FACE_OUTER_BOUND ( 'NONE', #13855, .T. ) ;
#17634=CARTESIAN_POINT ( 'NONE',  ( 6.222742520105470021, 3.584500230190543313, 6.791463481567635796 ) ) ;
#17646=EDGE_CURVE ( 'NONE', #92260, #103853, #49348, .T. ) ;
#17662=AXIS2_PLACEMENT_3D ( 'NONE', #57071, #66779, #399 ) ;
#17689=DIRECTION ( 'NONE',  ( 0.000000000000000000, -1.000000000000000000, 0.000000000000000000 ) ) ;
#17696=DIRECTION ( 'NONE',  ( -1.000000000000000000, -0.000000000000000000, -0.000000000000000000 ) ) ;
#17734=DIRECTION ( 'NONE',  ( -1.000000000000000000, -0.000000000000000000, -0.000000000000000000 ) ) ;
#17735=CARTESIAN_POINT ( 'NONE',  ( 6.463344223170841119, 7.245769408789096921, 1.129975644293424786 ) ) ;
#17798=DIRECTION ( 'NONE',  ( 0.000000000000000000, 0.000000000000000000, 1.000000000000000000 ) ) ;
#17850=CYLINDRICAL_SURFACE ( 'NONE', #59157, 4.000000000000000000 ) ;
#17860=CARTESIAN_POINT ( 'NONE',  ( 0.000000000000000000, 0.000000000000000000, 0.000000000000000000 ) ) ;
#17862=ORIENTED_EDGE ( 'NONE', *, *, #85143, .F. ) ;
#17863=AXIS2_PLACEMENT_3D ( 'NONE', #36877, #13605, #46000 ) ;
#17868=DIRECTION ( 'NONE',  ( 0.5735764363510462704, 0.8191520442889915765, 0.000000000000000000 ) ) ;
#17886=ORIENTED_EDGE ( 'NONE', *, *, #79646, .T. ) ;
#17912=DIRECTION ( 'NONE',  ( -1.000000000000000000, -1.224606353822377258E-16, -0.000000000000000000 ) ) ;
#17919=CARTESIAN_POINT ( 'NONE',  ( 6.289692432696756264, -5.239086202715467877, 4.583616368337884772 ) ) ;
#17922=DIRECTION ( 'NONE',  ( 0.000000000000000000, -1.000000000000000000, 0.000000000000000000 ) ) ;
#17923=ORIENTED_EDGE ( 'NONE', *, *, #73053, .F. ) ;
#17943=CARTESIAN_POINT ( 'NONE',  ( 40.59999999999999432, 1.533819458162526451E-15, 0.000000000000000000 ) ) ;
#17949=CARTESIAN_POINT ( 'NONE',  ( 45.59999999999999432, -3.309499999999999886, 0.000000000000000000 ) ) ;
#18021=EDGE_LOOP ( 'NONE', ( #94815, #33461, #71888, #100627, #103453 ) ) ;
#18048=EDGE_CURVE ( 'NONE', #61302, #89958, #21040, .T. ) ;
#18049=CARTESIAN_POINT ( 'NONE',  ( 23.09999999999999432, -3.309499999999999886, 4.475777889183790779E-16 ) ) ;
#18053=ORIENTED_EDGE ( 'NONE', *, *, #18444, .F. ) ;
#18062=ORIENTED_EDGE ( 'NONE', *, *, #97181, .T. ) ;
#18071=EDGE_CURVE ( 'NONE', #92046, #57881, #88575, .T. ) ;
#18072=ORIENTED_EDGE ( 'NONE', *, *, #71479, .T. ) ;
#18084=CARTESIAN_POINT ( 'NONE',  ( 18.58349330513380337, 4.000000000000003553, 0.000000000000000000 ) ) ;
#18097=AXIS2_PLACEMENT_3D ( 'NONE', #2752, #86368, #93907 ) ;
#18120=FACE_OUTER_BOUND ( 'NONE', #86847, .T. ) ;
#18121=DIRECTION ( 'NONE',  ( -1.000000000000000000, -1.224606353822377258E-16, -0.000000000000000000 ) ) ;
#18124=ORIENTED_EDGE ( 'NONE', *, *, #23747, .F. ) ;
#18130=DIRECTION ( 'NONE',  ( -1.000000000000000000, -1.224606353822377258E-16, -0.000000000000000000 ) ) ;
#18134=ORIENTED_EDGE ( 'NONE', *, *, #65217, .F. ) ;
#18146=VECTOR ( 'NONE', #43939, 1000.000000000000000 ) ;
#18180=CONICAL_SURFACE ( 'NONE', #64655, 3.309500000000001663, 0.9599310885968770357 ) ;
#18181=ORIENTED_EDGE ( 'NONE', *, *, #381, .T. ) ;
#18190=DIRECTION ( 'NONE',  ( -0.5735764363510494901, -0.8191520442889894671, 0.000000000000000000 ) ) ;
#18196=CARTESIAN_POINT ( 'NONE',  ( 6.333820801331835781, 4.275724398228168965, -5.594228103108450867 ) ) ;
#18252=ADVANCED_FACE ( 'NONE', ( #81322 ), #50659, .T. ) ;
#18264=CIRCLE ( 'NONE', #90618, 4.000000000000001776 ) ;
#18267=VECTOR ( 'NONE', #19087, 1000.000000000000000 ) ;
#18276=CARTESIAN_POINT ( 'NONE',  ( 34.83349330513379982, 4.898587196589405926E-16, -4.000000000000001776 ) ) ;
#18278=VERTEX_POINT ( 'NONE', #34429 ) ;
#18287=CARTESIAN_POINT ( 'NONE',  ( 37.61650669486618881, 1.474610560812782335E-15, 0.000000000000000000 ) ) ;
#18291=CARTESIAN_POINT ( 'NONE',  ( 30.11650669486618881, 1.474610560812782335E-15, 0.000000000000000000 ) ) ;
#18318=ORIENTED_EDGE ( 'NONE', *, *, #65176, .T. ) ;
#18328=LINE ( 'NONE', #18878, #56075 ) ;
#18337=CARTESIAN_POINT ( 'NONE',  ( 13.58349330513380160, 1.593028355512270567E-15, 0.000000000000000000 ) ) ;
#18340=AXIS2_PLACEMENT_3D ( 'NONE', #98693, #82531, #32945 ) ;
#18377=EDGE_CURVE ( 'NONE', #70516, #19922, #24846, .T. ) ;
#18383=LINE ( 'NONE', #1620, #23127 ) ;
#18388=LINE ( 'NONE', #49658, #57342 ) ;
#18395=VECTOR ( 'NONE', #19164, 1000.000000000000114 ) ;
#18405=DIRECTION ( 'NONE',  ( 0.000000000000000000, -1.000000000000000000, 0.000000000000000000 ) ) ;
#18421=AXIS2_PLACEMENT_3D ( 'NONE', #77156, #26521, #27588 ) ;
#18427=VECTOR ( 'NONE', #86604, 1000.000000000000000 ) ;
#18437=EDGE_CURVE ( 'NONE', #54223, #27527, #98860, .T. ) ;
#18444=EDGE_CURVE ( 'NONE', #53830, #32527, #92618, .T. ) ;
#18446=EDGE_LOOP ( 'NONE', ( #62869, #20363, #25232, #26374, #91386 ) ) ;
#18447=DIRECTION ( 'NONE',  ( -1.000000000000000000, -0.000000000000000000, -0.000000000000000000 ) ) ;
#18453=DIRECTION ( 'NONE',  ( -1.000000000000000000, -1.224606353822377258E-16, -0.000000000000000000 ) ) ;
#18485=LINE ( 'NONE', #44883, #34850 ) ;
#18501=ORIENTED_EDGE ( 'NONE', *, *, #41539, .T. ) ;
#18505=AXIS2_PLACEMENT_3D ( 'NONE', #91637, #2603, #100768 ) ;
#18519=LINE ( 'NONE', #101003, #82139 ) ;
#18533=LINE ( 'NONE', #91869, #95856 ) ;
#18550=AXIS2_PLACEMENT_3D ( 'NONE', #44342, #3353, #60020 ) ;
#18604=ORIENTED_EDGE ( 'NONE', *, *, #3236, .T. ) ;
#18610=DIRECTION ( 'NONE',  ( -0.5735764363510497121, 0.8191520442889892450, 1.003171929053521665E-16 ) ) ;
#18662=EDGE_LOOP ( 'NONE', ( #12317, #51319, #70386, #76712, #86545 ) ) ;
#18665=DIRECTION ( 'NONE',  ( 0.000000000000000000, 0.000000000000000000, 1.000000000000000000 ) ) ;
#18668=DIRECTION ( 'NONE',  ( 0.000000000000000000, 0.000000000000000000, 1.000000000000000000 ) ) ;
#18695=CIRCLE ( 'NONE', #73773, 4.000000000000000888 ) ;
#18717=VERTEX_POINT ( 'NONE', #55843 ) ;
#18724=EDGE_CURVE ( 'NONE', #48174, #25868, #47244, .T. ) ;
#18741=CARTESIAN_POINT ( 'NONE',  ( 36.84999999999999432, -3.309499999999999886, 0.000000000000000000 ) ) ;
#18807=ORIENTED_EDGE ( 'NONE', *, *, #85584, .F. ) ;
#18843=DIRECTION ( 'NONE',  ( -1.000000000000000000, -1.224606353822377258E-16, -0.000000000000000000 ) ) ;
#18845=CARTESIAN_POINT ( 'NONE',  ( 6.207999833770304399, 1.336757187206296660, 6.499999999999700684 ) ) ;
#18858=ORIENTED_EDGE ( 'NONE', *, *, #76250, .T. ) ;
#18874=DIRECTION ( 'NONE',  ( 0.000000000000000000, -1.000000000000000000, 0.000000000000000000 ) ) ;
#18878=CARTESIAN_POINT ( 'NONE',  ( 6.936184427528457874, 1.053834543709838281E-15, 8.605212085995399107 ) ) ;
#18883=DIRECTION ( 'NONE',  ( 0.000000000000000000, -1.000000000000000000, 0.000000000000000000 ) ) ;
#18908=CONICAL_SURFACE ( 'NONE', #80916, 3.309500000000001663, 0.9599310885968770357 ) ;
#18966=ORIENTED_EDGE ( 'NONE', *, *, #39887, .F. ) ;
#19004=DIRECTION ( 'NONE',  ( 0.000000000000000000, 1.000000000000000000, 0.000000000000000000 ) ) ;
#19008=CARTESIAN_POINT ( 'NONE',  ( 6.289692432696817548, -6.589071317540659223, 2.245373559999283231 ) ) ;
#19022=CARTESIAN_POINT ( 'NONE',  ( 13.86650669486618881, -3.999999999999998224, 0.000000000000000000 ) ) ;
#19025=CIRCLE ( 'NONE', #67271, 4.000000000000001776 ) ;
#19042=ORIENTED_EDGE ( 'NONE', *, *, #37624, .T. ) ;
#19047=CARTESIAN_POINT ( 'NONE',  ( 18.09999999999999787, -3.309499999999999886, 0.000000000000000000 ) ) ;
#19054=DIRECTION ( 'NONE',  ( 0.000000000000000000, 1.000000000000000000, 0.000000000000000000 ) ) ;
#19057=FACE_OUTER_BOUND ( 'NONE', #95103, .T. ) ;
#19058=ADVANCED_FACE ( 'NONE', ( #37302 ), #55677, .T. ) ;
#19064=VERTEX_POINT ( 'NONE', #62101 ) ;
#19069=LINE ( 'NONE', #10903, #1025 ) ;
#19081=CARTESIAN_POINT ( 'NONE',  ( 41.08349330513380693, 1.593028355512270567E-15, 0.000000000000000000 ) ) ;
#19087=DIRECTION ( 'NONE',  ( -1.000000000000000000, -0.000000000000000000, -0.000000000000000000 ) ) ;
#19112=CARTESIAN_POINT ( 'NONE',  ( 23.09999999999999432, 3.309500000000003439, 4.052968581778167743E-16 ) ) ;
#19134=CARTESIAN_POINT ( 'NONE',  ( 34.83349330513379982, 1.593028355512270567E-15, 0.000000000000000000 ) ) ;
#19136=ORIENTED_EDGE ( 'NONE', *, *, #98957, .F. ) ;
#19164=DIRECTION ( 'NONE',  ( 0.5735764363510462704, 0.8191520442889915765, 0.000000000000000000 ) ) ;
#19183=DIRECTION ( 'NONE',  ( -1.000000000000000000, -1.224606353822377258E-16, -0.000000000000000000 ) ) ;
#19195=AXIS2_PLACEMENT_3D ( 'NONE', #25720, #65595, #58580 ) ;
#19197=EDGE_CURVE ( 'NONE', #80498, #44793, #5891, .T. ) ;
#19200=AXIS2_PLACEMENT_3D ( 'NONE', #73023, #66546, #83257 ) ;
#19203=ADVANCED_FACE ( 'NONE', ( #30750 ), #98342, .T. ) ;
#19223=VERTEX_POINT ( 'NONE', #58721 ) ;
#19226=DIRECTION ( 'NONE',  ( -0.5735764363510497121, 0.8191520442889892450, 1.003171929053521665E-16 ) ) ;
#19228=DIRECTION ( 'NONE',  ( 0.5735764363510466035, -0.8191520442889914655, 1.003171929053524500E-16 ) ) ;
#19242=DIRECTION ( 'NONE',  ( 0.000000000000000000, -1.000000000000000000, 0.000000000000000000 ) ) ;
#19249=ORIENTED_EDGE ( 'NONE', *, *, #13580, .T. ) ;
#19265=DIRECTION ( 'NONE',  ( -1.000000000000000000, -1.224606353822377258E-16, -0.000000000000000000 ) ) ;
#19280=ORIENTED_EDGE ( 'NONE', *, *, #39543, .T. ) ;
#19288=ORIENTED_EDGE ( 'NONE', *, *, #88722, .T. ) ;
#19301=CARTESIAN_POINT ( 'NONE',  ( 37.33349330513379982, 1.593028355512270567E-15, 0.000000000000000000 ) ) ;
#19317=CARTESIAN_POINT ( 'NONE',  ( 0.000000000000000000, 0.000000000000000000, 0.000000000000000000 ) ) ;
#19328=DIRECTION ( 'NONE',  ( 0.000000000000000000, -1.000000000000000000, 0.000000000000000000 ) ) ;
#19342=DIRECTION ( 'NONE',  ( 0.000000000000000000, -1.000000000000000000, 0.000000000000000000 ) ) ;
#19356=CIRCLE ( 'NONE', #33107, 4.000000000000001776 ) ;
#19367=ORIENTED_EDGE ( 'NONE', *, *, #80978, .T. ) ;
#19375=DIRECTION ( 'NONE',  ( -1.000000000000000000, -1.224606353822377258E-16, -0.000000000000000000 ) ) ;
#19382=EDGE_CURVE ( 'NONE', #28486, #15372, #70867, .T. ) ;
#19389=CARTESIAN_POINT ( 'NONE',  ( 6.098403338276324526, 3.412123303361987325, 6.499999999999997335 ) ) ;
#19390=ORIENTED_EDGE ( 'NONE', *, *, #97343, .F. ) ;
#19396=CARTESIAN_POINT ( 'NONE',  ( 33.86650669486618881, 4.000000000000003553, 4.898587196589414801E-16 ) ) ;
#19399=AXIS2_PLACEMENT_3D ( 'NONE', #62781, #40081, #63841 ) ;
#19408=CARTESIAN_POINT ( 'NONE',  ( 37.33349330513379982, -4.000000000000000888, 4.898587196589416773E-16 ) ) ;
#19424=EDGE_CURVE ( 'NONE', #64980, #86482, #96739, .T. ) ;
#19432=CARTESIAN_POINT ( 'NONE',  ( 21.36650669486618881, 1.474610560812782335E-15, 0.000000000000000000 ) ) ;
#19471=DIRECTION ( 'NONE',  ( 0.000000000000000000, -1.000000000000000000, 0.000000000000000000 ) ) ;
#19474=EDGE_CURVE ( 'NONE', #9776, #102391, #84653, .T. ) ;
#19494=CARTESIAN_POINT ( 'NONE',  ( 24.83349330513380337, 1.593028355512270567E-15, 0.000000000000000000 ) ) ;
#19497=CARTESIAN_POINT ( 'NONE',  ( 14.34999999999999787, 3.309500000000003439, 0.000000000000000000 ) ) ;
#19509=ORIENTED_EDGE ( 'NONE', *, *, #98874, .T. ) ;
#19513=EDGE_CURVE ( 'NONE', #7688, #76929, #69183, .T. ) ;
#19519=CARTESIAN_POINT ( 'NONE',  ( 41.85000000000000142, 1.533819458162526451E-15, 0.000000000000000000 ) ) ;
#19533=ORIENTED_EDGE ( 'NONE', *, *, #87071, .F. ) ;
#19543=CARTESIAN_POINT ( 'NONE',  ( 0.000000000000000000, 0.000000000000000000, 0.000000000000000000 ) ) ;
#19547=FACE_OUTER_BOUND ( 'NONE', #55005, .T. ) ;
#19557=DIRECTION ( 'NONE',  ( 1.000000000000000000, 1.224606353822377258E-16, 0.000000000000000000 ) ) ;
#19569=ADVANCED_FACE ( 'NONE', ( #39759 ), #56975, .T. ) ;
#19580=ORIENTED_EDGE ( 'NONE', *, *, #41468, .F. ) ;
#19594=CARTESIAN_POINT ( 'NONE',  ( 46.84999999999999432, -3.309499999999999886, 0.000000000000000000 ) ) ;
#19605=CARTESIAN_POINT ( 'NONE',  ( 46.36650669486618881, -3.999999999999998224, 0.000000000000000000 ) ) ;
#19631=ORIENTED_EDGE ( 'NONE', *, *, #85297, .F. ) ;
#19640=CARTESIAN_POINT ( 'NONE',  ( 26.08349330513380337, -4.000000000000000000, 4.898587196589415787E-16 ) ) ;
#19658=AXIS2_PLACEMENT_3D ( 'NONE', #5969, #22732, #13533 ) ;
#19679=CARTESIAN_POINT ( 'NONE',  ( 0.000000000000000000, 2.253471898105741801E-15, 6.500000000000000000 ) ) ;
#19699=EDGE_LOOP ( 'NONE', ( #8936, #54347, #12773, #34922, #35928 ) ) ;
#19718=ORIENTED_EDGE ( 'NONE', *, *, #21824, .T. ) ;
#19750=CARTESIAN_POINT ( 'NONE',  ( 32.61650669486618881, -3.851859888774471706E-31, 4.000000000000000888 ) ) ;
#19751=CARTESIAN_POINT ( 'NONE',  ( 6.162888688655346670, -3.752776749732575468, -6.499999999999999112 ) ) ;
#19801=CARTESIAN_POINT ( 'NONE',  ( 38.86650669486618881, 1.474610560812782335E-15, 0.000000000000000000 ) ) ;
#19816=ADVANCED_FACE ( 'NONE', ( #70932 ), #22763, .T. ) ;
#19840=AXIS2_PLACEMENT_3D ( 'NONE', #91747, #67475, #1095 ) ;
#19864=CARTESIAN_POINT ( 'NONE',  ( 0.000000000000000000, 4.898587196589412829E-16, -4.000000000000000000 ) ) ;
#19891=CIRCLE ( 'NONE', #30420, 4.000000000000000888 ) ;
#19913=AXIS2_PLACEMENT_3D ( 'NONE', #34235, #99448, #25623 ) ;
#19915=CONICAL_SURFACE ( 'NONE', #102477, 3.309500000000001663, 0.9599310885968770357 ) ;
#19922=VERTEX_POINT ( 'NONE', #82734 ) ;
#19937=DIRECTION ( 'NONE',  ( -1.000000000000000000, -1.224606353822377258E-16, -0.000000000000000000 ) ) ;
#19962=CARTESIAN_POINT ( 'NONE',  ( 14.83349330513380337, 1.593028355512270567E-15, 0.000000000000000000 ) ) ;
#20019=VERTEX_POINT ( 'NONE', #56723 ) ;
#20041=EDGE_LOOP ( 'NONE', ( #7519, #52811 ) ) ;
#20056=VECTOR ( 'NONE', #26348, 1000.000000000000000 ) ;
#20062=AXIS2_PLACEMENT_3D ( 'NONE', #98854, #74588, #664 ) ;
#20066=AXIS2_PLACEMENT_3D ( 'NONE', #38112, #70969, #93122 ) ;
#20068=CARTESIAN_POINT ( 'NONE',  ( 22.33349330513380337, 1.593028355512270567E-15, 0.000000000000000000 ) ) ;
#20091=CARTESIAN_POINT ( 'NONE',  ( 47.33349330513379982, 1.593028355512270567E-15, 0.000000000000000000 ) ) ;
#20096=DIRECTION ( 'NONE',  ( 0.000000000000000000, -1.000000000000000000, 0.000000000000000000 ) ) ;
#20108=DIRECTION ( 'NONE',  ( -1.000000000000000000, -0.000000000000000000, -0.000000000000000000 ) ) ;
#20109=ORIENTED_EDGE ( 'NONE', *, *, #91136, .T. ) ;
#20121=LINE ( 'NONE', #76704, #78424 ) ;
#20139=CONICAL_SURFACE ( 'NONE', #80361, 3.309500000000001663, 0.9599310885968770357 ) ;
#20149=ADVANCED_FACE ( 'NONE', ( #51826 ), #86438, .T. ) ;
#20174=CARTESIAN_POINT ( 'NONE',  ( 25.11650669486618881, -3.851859888774471706E-31, 4.000000000000000888 ) ) ;
#20197=FACE_OUTER_BOUND ( 'NONE', #77913, .T. ) ;
#20220=AXIS2_PLACEMENT_3D ( 'NONE', #22391, #65470, #55234 ) ;
#20233=DIRECTION ( 'NONE',  ( 0.000000000000000000, -1.000000000000000000, 0.000000000000000000 ) ) ;
#20239=CIRCLE ( 'NONE', #83917, 4.000000000000001776 ) ;
#20277=ORIENTED_EDGE ( 'NONE', *, *, #100533, .T. ) ;
#20289=AXIS2_PLACEMENT_3D ( 'NONE', #103028, #37258, #100484 ) ;
#20291=AXIS2_PLACEMENT_3D ( 'NONE', #47149, #89751, #15847 ) ;
#20299=ORIENTED_EDGE ( 'NONE', *, *, #45458, .T. ) ;
#20302=CIRCLE ( 'NONE', #35762, 6.500000000000000000 ) ;
#20307=CARTESIAN_POINT ( 'NONE',  ( 0.000000000000000000, 5.629165124598848102, 3.250000000000005329 ) ) ;
#20310=VERTEX_POINT ( 'NONE', #6316 ) ;
#20323=AXIS2_PLACEMENT_3D ( 'NONE', #77786, #4958, #95558 ) ;
#20329=CARTESIAN_POINT ( 'NONE',  ( 40.11650669486618881, 4.898587196589411843E-16, -4.000000000000000888 ) ) ;
#20332=ORIENTED_EDGE ( 'NONE', *, *, #44424, .F. ) ;
#20337=CARTESIAN_POINT ( 'NONE',  ( 5.975663821520835306, 7.000939006314205848, 0.8740179403730332641 ) ) ;
#20353=ORIENTED_EDGE ( 'NONE', *, *, #11957, .F. ) ;
#20363=ORIENTED_EDGE ( 'NONE', *, *, #101815, .T. ) ;
#20365=ORIENTED_EDGE ( 'NONE', *, *, #21824, .F. ) ;
#20373=VERTEX_POINT ( 'NONE', #33829 ) ;
#20382=AXIS2_PLACEMENT_3D ( 'NONE', #11735, #35538, #12277 ) ;
#20397=CIRCLE ( 'NONE', #34150, 4.000000000000000888 ) ;
#20455=CARTESIAN_POINT ( 'NONE',  ( 29.34999999999999787, 1.533819458162526451E-15, 0.000000000000000000 ) ) ;
#20460=DIRECTION ( 'NONE',  ( -0.5735764363510494901, -0.8191520442889894671, 0.000000000000000000 ) ) ;
#20472=DIRECTION ( 'NONE',  ( 0.000000000000000000, 0.000000000000000000, 1.000000000000000000 ) ) ;
#20487=CIRCLE ( 'NONE', #77242, 4.000000000000000888 ) ;
#20497=EDGE_LOOP ( 'NONE', ( #105389, #50923, #102566, #30499, #100608, #47452 ) ) ;
#20511=EDGE_CURVE ( 'NONE', #19922, #77684, #52628, .T. ) ;
#20515=EDGE_CURVE ( 'NONE', #35550, #14924, #72534, .T. ) ;
#20540=DIRECTION ( 'NONE',  ( -1.000000000000000000, -0.000000000000000000, -0.000000000000000000 ) ) ;
#20561=CARTESIAN_POINT ( 'NONE',  ( 13.09999999999999787, -3.309499999999999886, 4.475777889183790779E-16 ) ) ;
#20579=DIRECTION ( 'NONE',  ( 0.5735764363510462704, 0.8191520442889915765, 0.000000000000000000 ) ) ;
#20593=ORIENTED_EDGE ( 'NONE', *, *, #35206, .F. ) ;
#20628=ORIENTED_EDGE ( 'NONE', *, *, #98167, .F. ) ;
#20732=DIRECTION ( 'NONE',  ( -1.000000000000000000, -1.224606353822377258E-16, -0.000000000000000000 ) ) ;
#20744=AXIS2_PLACEMENT_3D ( 'NONE', #40655, #51252, #100878 ) ;
#20750=ADVANCED_FACE ( 'NONE', ( #77858 ), #95134, .T. ) ;
#20755=LINE ( 'NONE', #78394, #66092 ) ;
#20775=ORIENTED_EDGE ( 'NONE', *, *, #37179, .T. ) ;
#20793=CIRCLE ( 'NONE', #93109, 4.000000000000000888 ) ;
#20819=CARTESIAN_POINT ( 'NONE',  ( 46.36650669486618881, 1.474610560812782335E-15, 0.000000000000000000 ) ) ;
#20825=DIRECTION ( 'NONE',  ( 0.000000000000000000, -1.000000000000000000, 0.000000000000000000 ) ) ;
#20856=VECTOR ( 'NONE', #63939, 1000.000000000000000 ) ;
#20862=ADVANCED_FACE ( 'NONE', ( #22306 ), #55152, .T. ) ;
#20869=CARTESIAN_POINT ( 'NONE',  ( 6.289692432696983637, 6.589071317541204564, 2.245373559999253033 ) ) ;
#20874=AXIS2_PLACEMENT_3D ( 'NONE', #102271, #12719, #21915 ) ;
#20877=VECTOR ( 'NONE', #105972, 1000.000000000000000 ) ;
#20908=AXIS2_PLACEMENT_3D ( 'NONE', #85357, #50838, #74592 ) ;
#20914=CYLINDRICAL_SURFACE ( 'NONE', #82262, 4.000000000000000000 ) ;
#20920=EDGE_CURVE ( 'NONE', #99126, #75857, #22916, .T. ) ;
#20961=ORIENTED_EDGE ( 'NONE', *, *, #95242, .F. ) ;
#20981=ORIENTED_EDGE ( 'NONE', *, *, #16211, .T. ) ;
#20985=ORIENTED_EDGE ( 'NONE', *, *, #736, .T. ) ;
#20998=DIRECTION ( 'NONE',  ( 0.000000000000000000, -1.000000000000000000, 0.000000000000000000 ) ) ;
#21015=EDGE_CURVE ( 'NONE', #74342, #78081, #46976, .T. ) ;
#21037=EDGE_CURVE ( 'NONE', #74776, #76086, #91810, .T. ) ;
#21040=LINE ( 'NONE', #22071, #48968 ) ;
#21059=ADVANCED_FACE ( 'NONE', ( #73458 ), #21169, .T. ) ;
#21068=VERTEX_POINT ( 'NONE', #2224 ) ;
#21079=VERTEX_POINT ( 'NONE', #3311 ) ;
#21107=CARTESIAN_POINT ( 'NONE',  ( 11.84999999999999787, 1.533819458162526451E-15, 0.000000000000000000 ) ) ;
#21132=CARTESIAN_POINT ( 'NONE',  ( 0.05533025579362303714, -6.264553569211845918, 2.149474931388141830 ) ) ;
#21152=DIRECTION ( 'NONE',  ( -1.000000000000000000, -1.224606353822377258E-16, -0.000000000000000000 ) ) ;
#21169=CONICAL_SURFACE ( 'NONE', #40064, 6.500000000000000000, 1.047197551196600296 ) ;
#21190=DIRECTION ( 'NONE',  ( -1.000000000000000000, -0.000000000000000000, -0.000000000000000000 ) ) ;
#21243=EDGE_LOOP ( 'NONE', ( #99189, #38073, #10834, #26393, #60068, #22509 ) ) ;
#21264=DIRECTION ( 'NONE',  ( -1.000000000000000000, -1.224606353822377258E-16, -0.000000000000000000 ) ) ;
#21272=EDGE_CURVE ( 'NONE', #958, #106610, #56904, .T. ) ;
#21273=ORIENTED_EDGE ( 'NONE', *, *, #94857, .T. ) ;
#21291=CIRCLE ( 'NONE', #79838, 3.309500000000001663 ) ;
#21300=CARTESIAN_POINT ( 'NONE',  ( 26.36650669486618881, 4.000000000000003553, 4.898587196589414801E-16 ) ) ;
#21301=CONICAL_SURFACE ( 'NONE', #81512, 3.309500000000001663, 0.9599310885968770357 ) ;
#21332=ORIENTED_EDGE ( 'NONE', *, *, #62915, .F. ) ;
#21349=DIRECTION ( 'NONE',  ( 0.5735764363510462704, 0.8191520442889915765, 0.000000000000000000 ) ) ;
#21354=EDGE_CURVE ( 'NONE', #70423, #64859, #40206, .T. ) ;
#21359=ORIENTED_EDGE ( 'NONE', *, *, #67931, .T. ) ;
#21395=ORIENTED_EDGE ( 'NONE', *, *, #34710, .F. ) ;
#21400=ORIENTED_EDGE ( 'NONE', *, *, #97418, .T. ) ;
#21424=B_SPLINE_CURVE_WITH_KNOTS ( 'NONE', 3,
 ( #77613, #69526, #5320, #86785, #53855 ),
 .UNSPECIFIED., .F., .F.,
 ( 4, 1, 4 ),
 ( 0.000000000000000000, 0.003752776749732567464, 0.007505553499465134927 ),
 .UNSPECIFIED. ) ;
#21451=CARTESIAN_POINT ( 'NONE',  ( 43.58349330513380693, 4.898587196589405926E-16, -4.000000000000001776 ) ) ;
#21459=VERTEX_POINT ( 'NONE', #95917 ) ;
#21461=ORIENTED_EDGE ( 'NONE', *, *, #81615, .F. ) ;
#21466=EDGE_CURVE ( 'NONE', #23893, #9941, #79191, .T. ) ;
#21501=ORIENTED_EDGE ( 'NONE', *, *, #7536, .T. ) ;
#21502=AXIS2_PLACEMENT_3D ( 'NONE', #79705, #88348, #20998 ) ;
#21503=ORIENTED_EDGE ( 'NONE', *, *, #95578, .T. ) ;
#21522=CARTESIAN_POINT ( 'NONE',  ( 26.84999999999999787, 1.533819458162526451E-15, 0.000000000000000000 ) ) ;
#21525=VERTEX_POINT ( 'NONE', #41387 ) ;
#21560=DIRECTION ( 'NONE',  ( 0.000000000000000000, -1.000000000000000000, 0.000000000000000000 ) ) ;
#21586=CARTESIAN_POINT ( 'NONE',  ( 13.09999999999999787, 1.533819458162526451E-15, 0.000000000000000000 ) ) ;
#21587=VECTOR ( 'NONE', #64415, 1000.000000000000000 ) ;
#21594=VERTEX_POINT ( 'NONE', #24699 ) ;
#21610=EDGE_CURVE ( 'NONE', #64980, #74552, #68187, .T. ) ;
#21629=DIRECTION ( 'NONE',  ( -1.000000000000000000, -0.000000000000000000, -0.000000000000000000 ) ) ;
#21646=CARTESIAN_POINT ( 'NONE',  ( -2.478418403666082792E-15, -5.948846446048902337, 2.696295709017763276 ) ) ;
#21674=CONICAL_SURFACE ( 'NONE', #100851, 4.000000000000001776, 0.9599310885968808105 ) ;
#21687=CARTESIAN_POINT ( 'NONE',  ( 25.59999999999999787, 1.533819458162526451E-15, 0.000000000000000000 ) ) ;
#21709=CARTESIAN_POINT ( 'NONE',  ( 6.222583235320747974, 4.088462131826499757, -6.499999999999999112 ) ) ;
#21742=AXIS2_PLACEMENT_3D ( 'NONE', #29433, #47152, #96267 ) ;
#21766=CARTESIAN_POINT ( 'NONE',  ( 8.099999999999999645, 3.752776749732561257, -6.499999999999999112 ) ) ;
#21771=DIRECTION ( 'NONE',  ( -1.000000000000000000, -1.224606353822377258E-16, -0.000000000000000000 ) ) ;
#21781=CARTESIAN_POINT ( 'NONE',  ( 0.000000000000000000, 0.000000000000000000, 4.000000000000000000 ) ) ;
#21789=CARTESIAN_POINT ( 'NONE',  ( 28.58349330513380337, 4.000000000000003553, 0.000000000000000000 ) ) ;
#21824=EDGE_CURVE ( 'NONE', #19922, #16154, #43962, .T. ) ;
#21879=FACE_OUTER_BOUND ( 'NONE', #5691, .T. ) ;
#21882=ORIENTED_EDGE ( 'NONE', *, *, #35443, .T. ) ;
#21901=CIRCLE ( 'NONE', #64976, 4.000000000000000888 ) ;
#21902=CARTESIAN_POINT ( 'NONE',  ( 6.162888688655346670, -3.752776749732575468, -6.499999999999999112 ) ) ;
#21915=DIRECTION ( 'NONE',  ( 0.000000000000000000, -1.000000000000000000, 0.000000000000000000 ) ) ;
#21954=CONICAL_SURFACE ( 'NONE', #13282, 6.500000000000000000, 1.047197551196600296 ) ;
#21955=CARTESIAN_POINT ( 'NONE',  ( 26.84999999999999787, 1.533819458162526451E-15, 0.000000000000000000 ) ) ;
#21956=AXIS2_PLACEMENT_3D ( 'NONE', #35249, #50851, #84837 ) ;
#21968=EDGE_LOOP ( 'NONE', ( #10773, #36502, #81702, #30509, #18501 ) ) ;
#21987=DIRECTION ( 'NONE',  ( -1.000000000000000000, -1.224606353822377258E-16, -0.000000000000000000 ) ) ;
#22003=CARTESIAN_POINT ( 'NONE',  ( 9.833493305133801599, -4.000000000000000000, 4.898587196589415787E-16 ) ) ;
#22027=AXIS2_PLACEMENT_3D ( 'NONE', #91481, #85518, #44526 ) ;
#22057=DIRECTION ( 'NONE',  ( -1.000000000000000000, -1.224606353822377258E-16, -0.000000000000000000 ) ) ;
#22068=ORIENTED_EDGE ( 'NONE', *, *, #98458, .T. ) ;
#22071=CARTESIAN_POINT ( 'NONE',  ( 16.84999999999999787, 3.309500000000003439, 4.052968581778167743E-16 ) ) ;
#22075=AXIS2_PLACEMENT_3D ( 'NONE', #97660, #15162, #48047 ) ;
#22077=CARTESIAN_POINT ( 'NONE',  ( 24.34999999999999787, 1.533819458162526451E-15, 0.000000000000000000 ) ) ;
#22079=CIRCLE ( 'NONE', #13412, 4.000000000000000888 ) ;
#22115=ORIENTED_EDGE ( 'NONE', *, *, #37496, .F. ) ;
#22150=DIRECTION ( 'NONE',  ( -1.000000000000000000, -1.224606353822377258E-16, -0.000000000000000000 ) ) ;
#22215=AXIS2_PLACEMENT_3D ( 'NONE', #92841, #92301, #19004 ) ;
#22232=DIRECTION ( 'NONE',  ( -1.000000000000000000, -0.000000000000000000, -0.000000000000000000 ) ) ;
#22233=ORIENTED_EDGE ( 'NONE', *, *, #63437, .F. ) ;
#22236=FACE_OUTER_BOUND ( 'NONE', #68298, .T. ) ;
#22243=AXIS2_PLACEMENT_3D ( 'NONE', #53849, #29111, #72165 ) ;
#22247=ORIENTED_EDGE ( 'NONE', *, *, #43306, .T. ) ;
#22274=FACE_OUTER_BOUND ( 'NONE', #99264, .T. ) ;
#22288=CIRCLE ( 'NONE', #11927, 4.000000000000000888 ) ;
#22296=AXIS2_PLACEMENT_3D ( 'NONE', #104111, #29741, #103073 ) ;
#22302=CARTESIAN_POINT ( 'NONE',  ( 6.394337469123806628, -3.776351736504769629, -6.540833074877204112 ) ) ;
#22306=FACE_OUTER_BOUND ( 'NONE', #90894, .T. ) ;
#22327=VECTOR ( 'NONE', #32080, 1000.000000000000000 ) ;
#22355=FACE_OUTER_BOUND ( 'NONE', #33428, .T. ) ;
#22383=ORIENTED_EDGE ( 'NONE', *, *, #26199, .F. ) ;
#22391=CARTESIAN_POINT ( 'NONE',  ( 32.33349330513379982, 1.593028355512270567E-15, 0.000000000000000000 ) ) ;
#22410=CARTESIAN_POINT ( 'NONE',  ( 19.83349330513379982, -7.703719777548943412E-31, 4.000000000000001776 ) ) ;
#22445=ORIENTED_EDGE ( 'NONE', *, *, #77380, .F. ) ;
#22447=ORIENTED_EDGE ( 'NONE', *, *, #84517, .T. ) ;
#22455=CARTESIAN_POINT ( 'NONE',  ( 8.099999999999999645, -3.752776749732575468, -6.499999999999999112 ) ) ;
#22478=DIRECTION ( 'NONE',  ( 0.000000000000000000, 1.000000000000000000, 0.000000000000000000 ) ) ;
#22502=VECTOR ( 'NONE', #96965, 1000.000000000000000 ) ;
#22509=ORIENTED_EDGE ( 'NONE', *, *, #11178, .F. ) ;
#22533=EDGE_LOOP ( 'NONE', ( #84328, #81169, #21359, #64487, #57079 ) ) ;
#22540=DIRECTION ( 'NONE',  ( 1.000000000000000000, 1.224606353822377258E-16, 0.000000000000000000 ) ) ;
#22546=DIRECTION ( 'NONE',  ( 0.000000000000000000, -1.000000000000000000, 0.000000000000000000 ) ) ;
#22553=CIRCLE ( 'NONE', #15653, 4.000000000000000888 ) ;
#22555=ORIENTED_EDGE ( 'NONE', *, *, #40008, .F. ) ;
#22576=DIRECTION ( 'NONE',  ( 0.000000000000000000, -1.000000000000000000, 0.000000000000000000 ) ) ;
#22581=AXIS2_PLACEMENT_3D ( 'NONE', #97358, #97896, #56892 ) ;
#22614=VERTEX_POINT ( 'NONE', #9368 ) ;
#22642=ADVANCED_FACE ( 'NONE', ( #90850 ), #62988, .T. ) ;
#22650=DIRECTION ( 'NONE',  ( 0.000000000000000000, -3.466879843239602429E-16, -1.000000000000000000 ) ) ;
#22658=DIRECTION ( 'NONE',  ( 0.000000000000000000, 0.000000000000000000, 1.000000000000000000 ) ) ;
#22675=EDGE_CURVE ( 'NONE', #55265, #61594, #93938, .T. ) ;
#22680=DIRECTION ( 'NONE',  ( 0.000000000000000000, -1.000000000000000000, 0.000000000000000000 ) ) ;
#22693=ORIENTED_EDGE ( 'NONE', *, *, #65172, .T. ) ;
#22695=CARTESIAN_POINT ( 'NONE',  ( 43.10000000000000142, 3.309500000000003439, 4.052968581778167743E-16 ) ) ;
#22713=ORIENTED_EDGE ( 'NONE', *, *, #63982, .F. ) ;
#22728=CARTESIAN_POINT ( 'NONE',  ( 35.59999999999999432, 1.533819458162526451E-15, 0.000000000000000000 ) ) ;
#22732=DIRECTION ( 'NONE',  ( -1.000000000000000000, -1.224606353822377258E-16, -0.000000000000000000 ) ) ;
#22754=DIRECTION ( 'NONE',  ( -1.000000000000000000, -1.224606353822377258E-16, -0.000000000000000000 ) ) ;
#22759=CARTESIAN_POINT ( 'NONE',  ( 6.644028492724100232, 3.901260126080569712, 6.757180751913672623 ) ) ;
#22763=CONICAL_SURFACE ( 'NONE', #83024, 3.309500000000001663, 0.9599310885968770357 ) ;
#22802=ORIENTED_EDGE ( 'NONE', *, *, #91691, .F. ) ;
#22806=DIRECTION ( 'NONE',  ( 0.000000000000000000, -1.000000000000000000, 0.000000000000000000 ) ) ;
#22831=CARTESIAN_POINT ( 'NONE',  ( 40.59999999999999432, 1.533819458162526451E-15, 0.000000000000000000 ) ) ;
#22876=VERTEX_POINT ( 'NONE', #36899 ) ;
#22889=DIRECTION ( 'NONE',  ( -1.000000000000000000, -0.000000000000000000, -0.000000000000000000 ) ) ;
#22916=CIRCLE ( 'NONE', #64250, 4.000000000000001776 ) ;
#22934=DIRECTION ( 'NONE',  ( 0.000000000000000000, 1.000000000000000000, 0.000000000000000000 ) ) ;
#22939=CARTESIAN_POINT ( 'NONE',  ( 6.562874270078298267, -3.301808241302750080, -6.845811579416824166 ) ) ;
#22942=DIRECTION ( 'NONE',  ( 0.5735764363510462704, 0.8191520442889915765, 0.000000000000000000 ) ) ;
#22951=ADVANCED_FACE ( 'NONE', ( #27756 ), #40639, .T. ) ;
#22976=CARTESIAN_POINT ( 'NONE',  ( 6.289812543865804351, -5.581224740283312613, 3.991031161979334385 ) ) ;
#22982=DIRECTION ( 'NONE',  ( -1.000000000000000000, -0.000000000000000000, -0.000000000000000000 ) ) ;
#22987=ORIENTED_EDGE ( 'NONE', *, *, #47816, .F. ) ;
#22992=ADVANCED_FACE ( 'NONE', ( #87547 ), #16546, .T. ) ;
#23049=EDGE_LOOP ( 'NONE', ( #61482, #90044, #42812, #78514, #91405, #55694 ) ) ;
#23055=DIRECTION ( 'NONE',  ( -1.000000000000000000, -1.224606353822377258E-16, -0.000000000000000000 ) ) ;
#23056=ORIENTED_EDGE ( 'NONE', *, *, #97786, .T. ) ;
#23058=CARTESIAN_POINT ( 'NONE',  ( 31.08349330513380337, 1.593028355512270567E-15, 0.000000000000000000 ) ) ;
#23093=VECTOR ( 'NONE', #40073, 1000.000000000000000 ) ;
#23094=DIRECTION ( 'NONE',  ( -1.000000000000000000, -1.224606353822377258E-16, -0.000000000000000000 ) ) ;
#23110=ORIENTED_EDGE ( 'NONE', *, *, #58806, .T. ) ;
#23113=EDGE_CURVE ( 'NONE', #18278, #57508, #18264, .T. ) ;
#23124=EDGE_CURVE ( 'NONE', #87161, #50002, #97447, .T. ) ;
#23127=VECTOR ( 'NONE', #9183, 1000.000000000000000 ) ;
#23132=AXIS2_PLACEMENT_3D ( 'NONE', #79555, #31047, #79030 ) ;
#23145=CARTESIAN_POINT ( 'NONE',  ( 24.83349330513380337, 1.593028355512270567E-15, 0.000000000000000000 ) ) ;
#23152=ORIENTED_EDGE ( 'NONE', *, *, #3037, .T. ) ;
#23163=CARTESIAN_POINT ( 'NONE',  ( 23.58349330513380337, -4.000000000000000888, 4.898587196589416773E-16 ) ) ;
#23179=DIRECTION ( 'NONE',  ( -1.000000000000000000, -1.224606353822377258E-16, -0.000000000000000000 ) ) ;
#23195=AXIS2_PLACEMENT_3D ( 'NONE', #78356, #29326, #104221 ) ;
#23200=ORIENTED_EDGE ( 'NONE', *, *, #38606, .T. ) ;
#23249=ORIENTED_EDGE ( 'NONE', *, *, #16840, .F. ) ;
#23274=EDGE_CURVE ( 'NONE', #61302, #54801, #13060, .T. ) ;
#23307=DIRECTION ( 'NONE',  ( -0.5735764363510497121, 0.8191520442889892450, 1.003171929053521665E-16 ) ) ;
#23338=AXIS2_PLACEMENT_3D ( 'NONE', #64220, #86904, #103597 ) ;
#23343=AXIS2_PLACEMENT_3D ( 'NONE', #23352, #23895, #89129 ) ;
#23345=EDGE_CURVE ( 'NONE', #70963, #36026, #52723, .T. ) ;
#23350=EDGE_LOOP ( 'NONE', ( #39609, #22447, #81613, #32035, #17191, #55450 ) ) ;
#23352=CARTESIAN_POINT ( 'NONE',  ( 19.83349330513379982, 1.593028355512270567E-15, 0.000000000000000000 ) ) ;
#23358=DIRECTION ( 'NONE',  ( -1.000000000000000000, -1.224606353822377258E-16, -0.000000000000000000 ) ) ;
#23365=DIRECTION ( 'NONE',  ( -1.000000000000000000, -0.000000000000000000, -0.000000000000000000 ) ) ;
#23376=DIRECTION ( 'NONE',  ( -1.000000000000000000, -1.224606353822377258E-16, -0.000000000000000000 ) ) ;
#23446=DIRECTION ( 'NONE',  ( -1.000000000000000000, -0.000000000000000000, -0.000000000000000000 ) ) ;
#23460=CARTESIAN_POINT ( 'NONE',  ( 0.1061556211655340781, 6.421950209808278132, 1.876855952934451510 ) ) ;
#23474=DIRECTION ( 'NONE',  ( 1.000000000000000000, 1.224606353822377258E-16, 0.000000000000000000 ) ) ;
#23481=ORIENTED_EDGE ( 'NONE', *, *, #74203, .F. ) ;
#23494=FACE_BOUND ( 'NONE', #20041, .T. ) ;
#23510=ORIENTED_EDGE ( 'NONE', *, *, #105556, .F. ) ;
#23512=DIRECTION ( 'NONE',  ( 0.000000000000000000, -1.000000000000000000, 0.000000000000000000 ) ) ;
#23541=CARTESIAN_POINT ( 'NONE',  ( 23.58349330513380337, -4.000000000000000000, 4.898587196589415787E-16 ) ) ;
#23563=LINE ( 'NONE', #56407, #85901 ) ;
#23603=EDGE_CURVE ( 'NONE', #101293, #65538, #82044, .T. ) ;
#23630=CARTESIAN_POINT ( 'NONE',  ( 21.08349330513380337, -4.000000000000000000, 4.898587196589415787E-16 ) ) ;
#23632=CARTESIAN_POINT ( 'NONE',  ( 24.83349330513380337, -4.000000000000000888, 4.898587196589416773E-16 ) ) ;
#23642=DIRECTION ( 'NONE',  ( -1.000000000000000000, -1.224606353822377258E-16, -0.000000000000000000 ) ) ;
#23649=DIRECTION ( 'NONE',  ( 0.000000000000000000, 1.000000000000000000, 0.000000000000000000 ) ) ;
#23713=ORIENTED_EDGE ( 'NONE', *, *, #79485, .F. ) ;
#23714=EDGE_CURVE ( 'NONE', #39800, #52601, #104382, .T. ) ;
#23715=LINE ( 'NONE', #65744, #91004 ) ;
#23731=VECTOR ( 'NONE', #52988, 1000.000000000000000 ) ;
#23747=EDGE_CURVE ( 'NONE', #84498, #45468, #104459, .T. ) ;
#23796=CARTESIAN_POINT ( 'NONE',  ( 33.58349330513379982, 1.593028355512270567E-15, 0.000000000000000000 ) ) ;
#23798=DIRECTION ( 'NONE',  ( 0.000000000000000000, -1.000000000000000000, 0.000000000000000000 ) ) ;
#23802=ORIENTED_EDGE ( 'NONE', *, *, #68925, .T. ) ;
#23816=AXIS2_PLACEMENT_3D ( 'NONE', #1822, #34780, #74651 ) ;
#23823=ADVANCED_FACE ( 'NONE', ( #50383 ), #76968, .F. ) ;
#23828=ORIENTED_EDGE ( 'NONE', *, *, #105675, .T. ) ;
#23831=ORIENTED_EDGE ( 'NONE', *, *, #33199, .T. ) ;
#23844=ORIENTED_EDGE ( 'NONE', *, *, #285, .T. ) ;
#23845=ORIENTED_EDGE ( 'NONE', *, *, #45041, .F. ) ;
#23849=DIRECTION ( 'NONE',  ( 0.000000000000000000, -1.000000000000000000, 0.000000000000000000 ) ) ;
#23862=ORIENTED_EDGE ( 'NONE', *, *, #69934, .F. ) ;
#23888=AXIS2_PLACEMENT_3D ( 'NONE', #67349, #66809, #58172 ) ;
#23893=VERTEX_POINT ( 'NONE', #37447 ) ;
#23895=DIRECTION ( 'NONE',  ( -1.000000000000000000, -1.224606353822377258E-16, -0.000000000000000000 ) ) ;
#23940=AXIS2_PLACEMENT_3D ( 'NONE', #26238, #50975, #18665 ) ;
#23992=CIRCLE ( 'NONE', #73834, 4.000000000000000888 ) ;
#24002=LINE ( 'NONE', #25599, #25304 ) ;
#24018=CLOSED_SHELL ( 'NONE', ( #41149, #64573, #97270, #16200, #2919, #57972, #24304, #59707, #68940, #76418, #79773, #103755, #86541, #39908, #60051, #92380, #87714, #36965, #9586, #14955, #22642, #68465, #86204, #2971, #47511, #45712, #18252, #20149, #24034, #73207, #14770, #76490, #35537, #25578, #51885, #43736, #33355, #76476, #93140, #51895, #62935, #62982, #41558, #9136, #46188, #63849, #81123, #63284, #28500, #89919, #69275, #59896, #45285, #25155, #25219, #13384, #68295, #48558, #67813, #8887, #19058, #47227, #68828, #15548, #37108, #59228, #38023, #78178, #39613, #65570, #101900, #41412, #38892, #20862, #59544, #386, #82278, #89670, #106729, #61677, #4886, #77597, #75843, #89298, #81624, #61788, #32540, #62111, #59794, #25796, #27101, #10285, #29024, #82066, #86410, #87435, #74866, #38301, #78261, #42150, #75368, #42221, #3282, #20750, #26127, #21059, #46583, #35027, #30239, #30137, #24604, #3996, #83586, #13159, #3316, #23823, #48595, #59164, #49013, #86756, #79998, #19816, #84951, #65819, #40831, #9435, #86820, #93060, #19569, #104472, #15873, #88908, #86708, #6455, #65080, #100131, #26376, #16684, #74127, #54601, #35191, #73124, #72392, #99609, #7031, #67009, #66078, #77104, #52905, #33947, #43581, #69753, #8725, #77976, #105228, #63504, #60577, #67972, #73814, #42497, #6610, #36298, #100508, #74752, #54298, #82123, #53303, #14499, #16908, #56439, #70098, #102597, #49408, #73860, #92622, #57552, #4009, #39556, #51186, #12578, #83073, #59793, #11231, #53631, #12553, #7492, #70895, #62649, #6908, #30855, #24941, #13713, #66732, #6806, #13722, #67172, #22992, #100710, #32443, #22951, #55954, #100000, #63225, #96098, #33488, #98475, #84293, #41865, #76025, #67471, #67527, #90921, #13436, #19203, #96337 ) ) ;
#24034=ADVANCED_FACE ( 'NONE', ( #616 ), #82645, .T. ) ;
#24059=CARTESIAN_POINT ( 'NONE',  ( 0.4037800551813793826, -7.199367570657615900, -0.5303295852573158831 ) ) ;
#24067=CARTESIAN_POINT ( 'NONE',  ( 6.936184427528457874, 0.000000000000000000, 0.000000000000000000 ) ) ;
#24100=DIRECTION ( 'NONE',  ( -1.000000000000000000, -1.224606353822377258E-16, -0.000000000000000000 ) ) ;
#24123=ORIENTED_EDGE ( 'NONE', *, *, #95248, .F. ) ;
#24161=EDGE_CURVE ( 'NONE', #76835, #70900, #9747, .T. ) ;
#24164=VECTOR ( 'NONE', #68083, 1000.000000000000000 ) ;
#24171=ORIENTED_EDGE ( 'NONE', *, *, #79828, .F. ) ;
#24225=CONICAL_SURFACE ( 'NONE', #17287, 3.309500000000001663, 0.9599310885968770357 ) ;
#24228=ORIENTED_EDGE ( 'NONE', *, *, #66298, .T. ) ;
#24229=VECTOR ( 'NONE', #51886, 1000.000000000000000 ) ;
#24281=EDGE_CURVE ( 'NONE', #80206, #82046, #32272, .T. ) ;
#24286=DIRECTION ( 'NONE',  ( 0.000000000000000000, -1.000000000000000000, 0.000000000000000000 ) ) ;
#24292=CARTESIAN_POINT ( 'NONE',  ( 45.11650669486618881, 1.474610560812782335E-15, 0.000000000000000000 ) ) ;
#24302=VECTOR ( 'NONE', #21190, 1000.000000000000000 ) ;
#24304=ADVANCED_FACE ( 'NONE', ( #61044 ), #61534, .T. ) ;
#24315=DIRECTION ( 'NONE',  ( -1.000000000000000000, -1.224606353822377258E-16, -0.000000000000000000 ) ) ;
#24321=CIRCLE ( 'NONE', #56987, 4.000000000000001776 ) ;
#24322=DIRECTION ( 'NONE',  ( -1.000000000000000000, -1.224606353822377258E-16, -0.000000000000000000 ) ) ;
#24333=FACE_OUTER_BOUND ( 'NONE', #41251, .T. ) ;
#24357=CARTESIAN_POINT ( 'NONE',  ( 29.83349330513380337, -7.703719777548943412E-31, 4.000000000000001776 ) ) ;
#24358=ORIENTED_EDGE ( 'NONE', *, *, #38802, .F. ) ;
#24425=EDGE_CURVE ( 'NONE', #54801, #47728, #7024, .T. ) ;
#24444=EDGE_CURVE ( 'NONE', #38628, #78066, #99444, .T. ) ;
#24447=EDGE_LOOP ( 'NONE', ( #77033, #98571, #35812, #87188, #103127, #46671 ) ) ;
#24467=DIRECTION ( 'NONE',  ( -1.000000000000000000, -1.224606353822377258E-16, -0.000000000000000000 ) ) ;
#24472=VERTEX_POINT ( 'NONE', #71233 ) ;
#24505=EDGE_CURVE ( 'NONE', #10553, #46481, #20302, .T. ) ;
#24574=ORIENTED_EDGE ( 'NONE', *, *, #65521, .F. ) ;
#24597=VECTOR ( 'NONE', #52155, 1000.000000000000114 ) ;
#24604=ADVANCED_FACE ( 'NONE', ( #100688 ), #51609, .F. ) ;
#24610=B_SPLINE_CURVE_WITH_KNOTS ( 'NONE', 3,
 ( #65674, #98558, #24708, #57556, #90482, #16589 ),
 .UNSPECIFIED., .F., .F.,
 ( 4, 2, 4 ),
 ( 0.000000000000000000, 0.0003491763592121705667, 0.0006983527184243411333 ),
 .UNSPECIFIED. ) ;
#24636=FACE_OUTER_BOUND ( 'NONE', #75925, .T. ) ;
#24687=CARTESIAN_POINT ( 'NONE',  ( 11.36650669486618881, 4.898587196589411843E-16, -4.000000000000000888 ) ) ;
#24697=CARTESIAN_POINT ( 'NONE',  ( 6.333820801331365047, 6.982605850972475103, -0.9057718968918052616 ) ) ;
#24699=CARTESIAN_POINT ( 'NONE',  ( 6.162888688655344005, -3.752776749732561257, 6.500000000000000000 ) ) ;
#24700=FACE_OUTER_BOUND ( 'NONE', #47785, .T. ) ;
#24706=CARTESIAN_POINT ( 'NONE',  ( 41.08349330513380693, 1.593028355512270567E-15, 0.000000000000000000 ) ) ;
#24708=CARTESIAN_POINT ( 'NONE',  ( 6.394343112843833055, 7.552705921139274636, -6.068871123799707842E-16 ) ) ;
#24735=DIRECTION ( 'NONE',  ( 0.000000000000000000, 0.000000000000000000, 1.000000000000000000 ) ) ;
#24739=CARTESIAN_POINT ( 'NONE',  ( 45.59999999999999432, 1.533819458162526451E-15, 0.000000000000000000 ) ) ;
#24748=FACE_OUTER_BOUND ( 'NONE', #105080, .T. ) ;
#24761=CARTESIAN_POINT ( 'NONE',  ( 0.2578475836320698322, -4.367703157927325108, 5.434916218090832807 ) ) ;
#24797=UNCERTAINTY_MEASURE_WITH_UNIT (LENGTH_MEASURE( 1.000000000000000082E-05 ), #40714, 'distance_accuracy_value', 'NONE');
#24846=CIRCLE ( 'NONE', #85107, 4.000000000000000888 ) ;
#24879=CIRCLE ( 'NONE', #74816, 4.000000000000001776 ) ;
#24895=CARTESIAN_POINT ( 'NONE',  ( 28.86650669486618881, 4.898587196589411843E-16, -4.000000000000000888 ) ) ;
#24932=EDGE_CURVE ( 'NONE', #52531, #45510, #97506, .T. ) ;
#24935=VECTOR ( 'NONE', #2649, 1000.000000000000000 ) ;
#24941=ADVANCED_FACE ( 'NONE', ( #10224 ), #63131, .T. ) ;
#24971=CIRCLE ( 'NONE', #49019, 4.000000000000001776 ) ;
#24978=ORIENTED_EDGE ( 'NONE', *, *, #104303, .T. ) ;
#24986=VERTEX_POINT ( 'NONE', #50157 ) ;
#24988=DIRECTION ( 'NONE',  ( -0.5735764363510494901, -0.8191520442889894671, 0.000000000000000000 ) ) ;
#25048=CARTESIAN_POINT ( 'NONE',  ( 0.2578475836320709980, 6.890627091270373761, 1.065083781909174077 ) ) ;
#25084=VERTEX_POINT ( 'NONE', #42224 ) ;
#25090=CARTESIAN_POINT ( 'NONE',  ( 0.4037800551813707228, 4.058962678540093627, -5.969670414742686226 ) ) ;
#25132=CARTESIAN_POINT ( 'NONE',  ( 45.59999999999999432, 1.533819458162526451E-15, 0.000000000000000000 ) ) ;
#25155=ADVANCED_FACE ( 'NONE', ( #59496 ), #102940, .T. ) ;
#25208=AXIS2_PLACEMENT_3D ( 'NONE', #40264, #21987, #64037 ) ;
#25219=ADVANCED_FACE ( 'NONE', ( #65974 ), #6211, .T. ) ;
#25223=VERTEX_POINT ( 'NONE', #3375 ) ;
#25232=ORIENTED_EDGE ( 'NONE', *, *, #48689, .F. ) ;
#25235=CARTESIAN_POINT ( 'NONE',  ( 6.692588830498428898, 7.935834885954428763, 0.04058884017440098774 ) ) ;
#25237=EDGE_CURVE ( 'NONE', #65882, #86927, #19069, .T. ) ;
#25242=DIRECTION ( 'NONE',  ( -1.000000000000000000, -1.224606353822377258E-16, -0.000000000000000000 ) ) ;
#25278=VECTOR ( 'NONE', #65921, 1000.000000000000000 ) ;
#25289=EDGE_CURVE ( 'NONE', #100726, #86709, #29284, .T. ) ;
#25304=VECTOR ( 'NONE', #56845, 1000.000000000000000 ) ;
#25329=VERTEX_POINT ( 'NONE', #19605 ) ;
#25427=VECTOR ( 'NONE', #79852, 1000.000000000000000 ) ;
#25440=CARTESIAN_POINT ( 'NONE',  ( 23.58349330513380337, 4.000000000000002665, 0.000000000000000000 ) ) ;
#25511=CIRCLE ( 'NONE', #15142, 4.000000000000000888 ) ;
#25520=CIRCLE ( 'NONE', #97841, 4.000000000000000888 ) ;
#25574=ORIENTED_EDGE ( 'NONE', *, *, #60303, .T. ) ;
#25578=ADVANCED_FACE ( 'NONE', ( #101929 ), #95932, .T. ) ;
#25599=CARTESIAN_POINT ( 'NONE',  ( 32.33349330513379982, -4.000000000000000000, 4.898587196589415787E-16 ) ) ;
#25623=DIRECTION ( 'NONE',  ( 0.000000000000000000, -1.000000000000000000, 0.000000000000000000 ) ) ;
#25647=CONICAL_SURFACE ( 'NONE', #10044, 3.309500000000001663, 0.9599310885968770357 ) ;
#25658=AXIS2_PLACEMENT_3D ( 'NONE', #88659, #14220, #62803 ) ;
#25659=VERTEX_POINT ( 'NONE', #10777 ) ;
#25665=EDGE_CURVE ( 'NONE', #11792, #82981, #86315, .T. ) ;
#25666=VERTEX_POINT ( 'NONE', #59907 ) ;
#25667=CARTESIAN_POINT ( 'NONE',  ( 6.575918192882429736, -7.701766175471821185, 1.336937141848248750E-15 ) ) ;
#25668=CONICAL_SURFACE ( 'NONE', #54858, 3.309500000000001663, 0.9599310885968770357 ) ;
#25673=DIRECTION ( 'NONE',  ( 0.000000000000000000, -1.000000000000000000, 0.000000000000000000 ) ) ;
#25676=DIRECTION ( 'NONE',  ( 0.000000000000000000, -1.000000000000000000, 0.000000000000000000 ) ) ;
#25695=EDGE_CURVE ( 'NONE', #36026, #44445, #43174, .T. ) ;
#25706=ORIENTED_EDGE ( 'NONE', *, *, #27043, .F. ) ;
#25720=CARTESIAN_POINT ( 'NONE',  ( 27.33349330513380337, 1.593028355512270567E-15, 0.000000000000000000 ) ) ;
#25739=CARTESIAN_POINT ( 'NONE',  ( 37.33349330513379982, 1.593028355512270567E-15, 0.000000000000000000 ) ) ;
#25772=ORIENTED_EDGE ( 'NONE', *, *, #94239, .F. ) ;
#25776=EDGE_LOOP ( 'NONE', ( #58240, #7146, #104042, #98660, #86592 ) ) ;
#25796=ADVANCED_FACE ( 'NONE', ( #103529 ), #8056, .T. ) ;
#25806=CARTESIAN_POINT ( 'NONE',  ( 28.58349330513380337, 1.593028355512270567E-15, 0.000000000000000000 ) ) ;
#25828=EDGE_CURVE ( 'NONE', #66609, #92310, #54540, .T. ) ;
#25838=DIRECTION ( 'NONE',  ( -1.000000000000000000, -1.224606353822377258E-16, -0.000000000000000000 ) ) ;
#25848=CARTESIAN_POINT ( 'NONE',  ( 13.58349330513380160, 1.593028355512270567E-15, 0.000000000000000000 ) ) ;
#25868=VERTEX_POINT ( 'NONE', #23163 ) ;
#25881=CARTESIAN_POINT ( 'NONE',  ( 21.84999999999999787, 3.309500000000003439, 0.000000000000000000 ) ) ;
#25898=DIRECTION ( 'NONE',  ( -1.000000000000000000, -0.000000000000000000, -0.000000000000000000 ) ) ;
#25906=ORIENTED_EDGE ( 'NONE', *, *, #3473, .F. ) ;
#25924=LINE ( 'NONE', #74930, #39582 ) ;
#25925=CIRCLE ( 'NONE', #86182, 4.000000000000000888 ) ;
#25950=LINE ( 'NONE', #84137, #104746 ) ;
#25998=CARTESIAN_POINT ( 'NONE',  ( 0.000000000000000000, 0.000000000000000000, 0.000000000000000000 ) ) ;
#26006=ORIENTED_EDGE ( 'NONE', *, *, #81851, .F. ) ;
#26011=FACE_OUTER_BOUND ( 'NONE', #41969, .T. ) ;
#26051=ORIENTED_EDGE ( 'NONE', *, *, #48889, .F. ) ;
#26066=ORIENTED_EDGE ( 'NONE', *, *, #67922, .T. ) ;
#26095=EDGE_CURVE ( 'NONE', #54801, #61302, #52875, .T. ) ;
#26127=ADVANCED_FACE ( 'NONE', ( #11183 ), #21954, .T. ) ;
#26156=ORIENTED_EDGE ( 'NONE', *, *, #50265, .T. ) ;
#26168=CONICAL_SURFACE ( 'NONE', #84636, 4.000000000000001776, 0.9599310885968808105 ) ;
#26178=CARTESIAN_POINT ( 'NONE',  ( 6.692588830498431562, -7.935834885954435869, 0.04058884017440032160 ) ) ;
#26186=VERTEX_POINT ( 'NONE', #93193 ) ;
#26195=EDGE_LOOP ( 'NONE', ( #50583, #102655, #53196, #51507, #88858 ) ) ;
#26199=EDGE_CURVE ( 'NONE', #70423, #63451, #1498, .T. ) ;
#26210=DIRECTION ( 'NONE',  ( 0.000000000000000000, -1.000000000000000000, 0.000000000000000000 ) ) ;
#26216=VERTEX_POINT ( 'NONE', #21451 ) ;
#26221=EDGE_CURVE ( 'NONE', #56846, #51415, #38177, .T. ) ;
#26229=DIRECTION ( 'NONE',  ( 0.000000000000000000, -1.000000000000000000, 0.000000000000000000 ) ) ;
#26238=CARTESIAN_POINT ( 'NONE',  ( 0.000000000000000000, 0.000000000000000000, 0.000000000000000000 ) ) ;
#26290=LINE ( 'NONE', #89910, #34476 ) ;
#26297=DIRECTION ( 'NONE',  ( -1.000000000000000000, -1.224606353822377258E-16, -0.000000000000000000 ) ) ;
#26314=ORIENTED_EDGE ( 'NONE', *, *, #2319, .F. ) ;
#26319=CARTESIAN_POINT ( 'NONE',  ( 6.162888688655344005, -3.752776749732561257, 6.500000000000000000 ) ) ;
#26348=DIRECTION ( 'NONE',  ( -1.000000000000000000, -0.000000000000000000, -0.000000000000000000 ) ) ;
#26360=CARTESIAN_POINT ( 'NONE',  ( 43.10000000000000142, -3.309499999999999886, 4.475777889183790779E-16 ) ) ;
#26374=ORIENTED_EDGE ( 'NONE', *, *, #99001, .F. ) ;
#26376=ADVANCED_FACE ( 'NONE', ( #67208 ), #56387, .T. ) ;
#26393=ORIENTED_EDGE ( 'NONE', *, *, #94216, .F. ) ;
#26394=CARTESIAN_POINT ( 'NONE',  ( 0.05613245601076726626, 1.278525034532176141, -6.499999999999999112 ) ) ;
#26395=CARTESIAN_POINT ( 'NONE',  ( 6.562934840145639548, 4.277581483015136854, 6.282640795011892543 ) ) ;
#26406=ORIENTED_EDGE ( 'NONE', *, *, #104489, .T. ) ;
#26407=CYLINDRICAL_SURFACE ( 'NONE', #18505, 4.000000000000000000 ) ;
#26438=DIRECTION ( 'NONE',  ( -1.000000000000000000, -1.224606353822377258E-16, -0.000000000000000000 ) ) ;
#26440=CYLINDRICAL_SURFACE ( 'NONE', #66423, 4.000000000000000000 ) ;
#26457=EDGE_CURVE ( 'NONE', #25084, #105946, #13361, .T. ) ;
#26462=DIRECTION ( 'NONE',  ( -1.000000000000000000, -1.224606353822377258E-16, -0.000000000000000000 ) ) ;
#26489=VECTOR ( 'NONE', #15412, 1000.000000000000000 ) ;
#26507=ORIENTED_EDGE ( 'NONE', *, *, #58122, .F. ) ;
#26521=DIRECTION ( 'NONE',  ( -1.000000000000000000, -1.224606353822377258E-16, -0.000000000000000000 ) ) ;
#26545=DIRECTION ( 'NONE',  ( 0.000000000000000000, 1.000000000000000000, 0.000000000000000000 ) ) ;
#26554=ORIENTED_EDGE ( 'NONE', *, *, #18071, .T. ) ;
#26559=CARTESIAN_POINT ( 'NONE',  ( 0.000000000000000000, 4.898587196589412829E-16, -4.000000000000000000 ) ) ;
#26561=DIRECTION ( 'NONE',  ( -1.000000000000000000, -1.224606353822377258E-16, -0.000000000000000000 ) ) ;
#26586=DIRECTION ( 'NONE',  ( -1.000000000000000000, -1.224606353822377258E-16, -0.000000000000000000 ) ) ;
#26589=ORIENTED_EDGE ( 'NONE', *, *, #103541, .F. ) ;
#26631=EDGE_CURVE ( 'NONE', #77823, #39684, #39187, .T. ) ;
#26667=ORIENTED_EDGE ( 'NONE', *, *, #71874, .F. ) ;
#26696=VERTEX_POINT ( 'NONE', #99954 ) ;
#26697=EDGE_CURVE ( 'NONE', #40330, #66259, #28909, .T. ) ;
#26750=DIRECTION ( 'NONE',  ( 0.000000000000000000, -1.000000000000000000, 0.000000000000000000 ) ) ;
#26759=CIRCLE ( 'NONE', #40494, 4.000000000000000888 ) ;
#26778=CARTESIAN_POINT ( 'NONE',  ( 31.08349330513380337, 4.898587196589405926E-16, -4.000000000000001776 ) ) ;
#26812=CARTESIAN_POINT ( 'NONE',  ( 5.819846122303830249, 6.321060697774965931, 2.051601713726983078 ) ) ;
#26843=CARTESIAN_POINT ( 'NONE',  ( 5.975663821522140928, 7.000939006314000679, -0.8740179403733884245 ) ) ;
#26847=AXIS2_PLACEMENT_3D ( 'NONE', #36075, #99151, #2052 ) ;
#26849=CIRCLE ( 'NONE', #45595, 3.309500000000001663 ) ;
#26859=DIRECTION ( 'NONE',  ( 0.000000000000000000, 0.5000000000000018874, 0.8660254037844374864 ) ) ;
#26870=EDGE_CURVE ( 'NONE', #21594, #76213, #23715, .T. ) ;
#26876=CARTESIAN_POINT ( 'NONE',  ( 10.11650669486618881, 4.898587196589411843E-16, -4.000000000000000888 ) ) ;
#26898=VERTEX_POINT ( 'NONE', #8020 ) ;
#26899=EDGE_CURVE ( 'NONE', #93985, #596, #34131, .T. ) ;
#26903=AXIS2_PLACEMENT_3D ( 'NONE', #69766, #61697, #80484 ) ;
#26909=CARTESIAN_POINT ( 'NONE',  ( 11.36650669486618881, -3.851859888774471706E-31, 4.000000000000000888 ) ) ;
#26911=ORIENTED_EDGE ( 'NONE', *, *, #35079, .F. ) ;
#26946=DIRECTION ( 'NONE',  ( -1.000000000000000000, -0.000000000000000000, -0.000000000000000000 ) ) ;
#26948=ORIENTED_EDGE ( 'NONE', *, *, #14262, .T. ) ;
#26963=DIRECTION ( 'NONE',  ( -1.000000000000000000, -0.000000000000000000, -0.000000000000000000 ) ) ;
#26966=DIRECTION ( 'NONE',  ( 0.5735764363510466035, -0.8191520442889914655, 1.003171929053524500E-16 ) ) ;
#26984=CIRCLE ( 'NONE', #82049, 3.309500000000001663 ) ;
#27017=EDGE_CURVE ( 'NONE', #44463, #86259, #65206, .T. ) ;
#27024=EDGE_CURVE ( 'NONE', #61594, #55094, #56479, .T. ) ;
#27026=DIRECTION ( 'NONE',  ( -1.000000000000000000, -0.000000000000000000, -0.000000000000000000 ) ) ;
#27029=CARTESIAN_POINT ( 'NONE',  ( 6.562874270078295602, 3.301808241302743863, 6.845811579416823278 ) ) ;
#27043=EDGE_CURVE ( 'NONE', #77685, #60237, #25511, .T. ) ;
#27051=VECTOR ( 'NONE', #84971, 1000.000000000000000 ) ;
#27074=CARTESIAN_POINT ( 'NONE',  ( 8.099999999999999645, 4.898587196589412829E-16, -4.000000000000000000 ) ) ;
#27098=CARTESIAN_POINT ( 'NONE',  ( 18.86650669486618881, 1.474610560812782335E-15, 0.000000000000000000 ) ) ;
#27099=EDGE_LOOP ( 'NONE', ( #91132, #39116, #19288, #10208, #85389 ) ) ;
#27101=ADVANCED_FACE ( 'NONE', ( #92670 ), #101311, .T. ) ;
#27122=EDGE_CURVE ( 'NONE', #49696, #70900, #34501, .T. ) ;
#27140=DIRECTION ( 'NONE',  ( 0.000000000000000000, -1.000000000000000000, 0.000000000000000000 ) ) ;
#27196=LINE ( 'NONE', #19112, #80774 ) ;
#27202=VERTEX_POINT ( 'NONE', #59795 ) ;
#27213=CARTESIAN_POINT ( 'NONE',  ( 26.84999999999999787, 1.533819458162526451E-15, 0.000000000000000000 ) ) ;
#27219=CIRCLE ( 'NONE', #30674, 4.000000000000000888 ) ;
#27234=ORIENTED_EDGE ( 'NONE', *, *, #66520, .T. ) ;
#27252=ORIENTED_EDGE ( 'NONE', *, *, #68744, .F. ) ;
#27262=ORIENTED_EDGE ( 'NONE', *, *, #20920, .T. ) ;
#27271=DIRECTION ( 'NONE',  ( 0.5735764363510462704, 0.8191520442889915765, 0.000000000000000000 ) ) ;
#27290=DIRECTION ( 'NONE',  ( -1.000000000000000000, -1.224606353822377258E-16, -0.000000000000000000 ) ) ;
#27295=VECTOR ( 'NONE', #13665, 1000.000000000000000 ) ;
#27304=DIRECTION ( 'NONE',  ( 0.000000000000000000, -1.000000000000000000, 0.000000000000000000 ) ) ;
#27307=EDGE_CURVE ( 'NONE', #85998, #42587, #86730, .T. ) ;
#27309=CARTESIAN_POINT ( 'NONE',  ( 43.86650669486618881, -3.851859888774471706E-31, 4.000000000000000888 ) ) ;
#27322=CARTESIAN_POINT ( 'NONE',  ( 0.000000000000000000, 0.000000000000000000, 0.000000000000000000 ) ) ;
#27351=ORIENTED_EDGE ( 'NONE', *, *, #57675, .F. ) ;
#27385=AXIS2_PLACEMENT_3D ( 'NONE', #23145, #32297, #16618 ) ;
#27412=DIRECTION ( 'NONE',  ( -1.000000000000000000, -1.224606353822377258E-16, -0.000000000000000000 ) ) ;
#27423=DIRECTION ( 'NONE',  ( -1.000000000000000000, -1.224606353822377258E-16, -0.000000000000000000 ) ) ;
#27474=CARTESIAN_POINT ( 'NONE',  ( 13.86650669486618881, 1.474610560812782335E-15, 0.000000000000000000 ) ) ;
#27477=B_SPLINE_CURVE_WITH_KNOTS ( 'NONE', 3,
 ( #64936, #39619, #15317, #49264, #106439, #15849 ),
 .UNSPECIFIED., .F., .F.,
 ( 4, 2, 4 ),
 ( 0.003990927807053584568, 0.005983070073873398773, 0.007975212340693213844 ),
 .UNSPECIFIED. ) ;
#27517=CARTESIAN_POINT ( 'NONE',  ( 17.33349330513380337, 4.898587196589405926E-16, -4.000000000000001776 ) ) ;
#27527=VERTEX_POINT ( 'NONE', #66552 ) ;
#27558=EDGE_CURVE ( 'NONE', #81048, #75857, #82736, .T. ) ;
#27582=ORIENTED_EDGE ( 'NONE', *, *, #84280, .T. ) ;
#27588=DIRECTION ( 'NONE',  ( 0.000000000000000000, -1.000000000000000000, 0.000000000000000000 ) ) ;
#27608=CARTESIAN_POINT ( 'NONE',  ( 30.11650669486618881, 4.000000000000003553, 4.898587196589414801E-16 ) ) ;
#27614=CONICAL_SURFACE ( 'NONE', #101641, 3.309500000000001663, 0.9599310885968770357 ) ;
#27654=ORIENTED_EDGE ( 'NONE', *, *, #13559, .F. ) ;
#27682=CARTESIAN_POINT ( 'NONE',  ( 23.86650669486618881, 1.474610560812782335E-15, 0.000000000000000000 ) ) ;
#27702=VECTOR ( 'NONE', #18190, 1000.000000000000000 ) ;
#27756=FACE_OUTER_BOUND ( 'NONE', #83645, .T. ) ;
#27763=DIRECTION ( 'NONE',  ( -0.5735764363510497121, 0.8191520442889892450, 1.003171929053521665E-16 ) ) ;
#27791=ORIENTED_EDGE ( 'NONE', *, *, #83537, .T. ) ;
#27798=AXIS2_PLACEMENT_3D ( 'NONE', #98716, #90648, #16754 ) ;
#27820=CARTESIAN_POINT ( 'NONE',  ( 7.500000000000001776, 0.000000000000000000, 0.000000000000000000 ) ) ;
#27825=AXIS2_PLACEMENT_3D ( 'NONE', #19301, #5703, #63966 ) ;
#27828=PRODUCT_DEFINITION_SHAPE ( 'NONE', 'NONE',  #52852 ) ;
#27840=AXIS2_PLACEMENT_3D ( 'NONE', #86643, #14294, #12711 ) ;
#27845=DIRECTION ( 'NONE',  ( 0.000000000000000000, 0.000000000000000000, -1.000000000000000000 ) ) ;
#27865=AXIS2_PLACEMENT_3D ( 'NONE', #25806, #40864, #100165 ) ;
#27868=EDGE_CURVE ( 'NONE', #64268, #33845, #35296, .T. ) ;
#27869=VERTEX_POINT ( 'NONE', #37950 ) ;
#27888=CARTESIAN_POINT ( 'NONE',  ( 43.58349330513380693, -7.703719777548943412E-31, 4.000000000000001776 ) ) ;
#27906=CARTESIAN_POINT ( 'NONE',  ( 37.61650669486618881, -3.851859888774471706E-31, 4.000000000000000888 ) ) ;
#27919=DIRECTION ( 'NONE',  ( -1.000000000000000000, -1.224606353822377258E-16, -0.000000000000000000 ) ) ;
#27938=EDGE_CURVE ( 'NONE', #31781, #35660, #2532, .T. ) ;
#27942=CIRCLE ( 'NONE', #7235, 3.309500000000001663 ) ;
#27943=FACE_OUTER_BOUND ( 'NONE', #78286, .T. ) ;
#27944=DIRECTION ( 'NONE',  ( 0.5735764363510462704, 0.8191520442889915765, 0.000000000000000000 ) ) ;
#27946=VECTOR ( 'NONE', #65807, 1000.000000000000000 ) ;
#27950=DIRECTION ( 'NONE',  ( 0.000000000000000000, 0.000000000000000000, 1.000000000000000000 ) ) ;
#27961=ORIENTED_EDGE ( 'NONE', *, *, #35328, .F. ) ;
#27967=ORIENTED_EDGE ( 'NONE', *, *, #94916, .T. ) ;
#27968=CARTESIAN_POINT ( 'NONE',  ( 6.585530689845731089, -4.023059358968668953, -6.499999999999999112 ) ) ;
#27974=ORIENTED_EDGE ( 'NONE', *, *, #60385, .F. ) ;
#27975=CYLINDRICAL_SURFACE ( 'NONE', #78151, 4.000000000000000000 ) ;
#28003=DIRECTION ( 'NONE',  ( -1.000000000000000000, -1.224606353822377258E-16, -0.000000000000000000 ) ) ;
#28032=CARTESIAN_POINT ( 'NONE',  ( 5.821933341150374197, -1.421180797416045749, 6.500000000000000000 ) ) ;
#28049=ORIENTED_EDGE ( 'NONE', *, *, #16114, .T. ) ;
#28051=FACE_OUTER_BOUND ( 'NONE', #27099, .T. ) ;
#28072=CIRCLE ( 'NONE', #40115, 3.309500000000001663 ) ;
#28110=CARTESIAN_POINT ( 'NONE',  ( 17.33349330513380337, 1.593028355512270567E-15, 0.000000000000000000 ) ) ;
#28209=DIRECTION ( 'NONE',  ( 0.000000000000000000, -1.000000000000000000, 0.000000000000000000 ) ) ;
#28290=EDGE_LOOP ( 'NONE', ( #91961, #102693, #58325, #102240, #30202 ) ) ;
#28293=DIRECTION ( 'NONE',  ( -0.7071067811865530128, 0.000000000000000000, 0.7071067811865421326 ) ) ;
#28322=DIRECTION ( 'NONE',  ( -1.000000000000000000, -1.224606353822377258E-16, -0.000000000000000000 ) ) ;
#28326=ORIENTED_EDGE ( 'NONE', *, *, #32198, .F. ) ;
#28359=FACE_OUTER_BOUND ( 'NONE', #51537, .T. ) ;
#28370=ORIENTED_EDGE ( 'NONE', *, *, #49995, .F. ) ;
#28374=AXIS2_PLACEMENT_3D ( 'NONE', #88585, #98778, #16822 ) ;
#28385=EDGE_CURVE ( 'NONE', #85998, #82432, #45922, .T. ) ;
#28392=ORIENTED_EDGE ( 'NONE', *, *, #77768, .F. ) ;
#28412=AXIS2_PLACEMENT_3D ( 'NONE', #59068, #19183, #26210 ) ;
#28419=CARTESIAN_POINT ( 'NONE',  ( 23.58349330513380337, 4.000000000000003553, 0.000000000000000000 ) ) ;
#28451=DIRECTION ( 'NONE',  ( 0.000000000000000000, 1.000000000000000000, 0.000000000000000000 ) ) ;
#28471=CARTESIAN_POINT ( 'NONE',  ( 41.85000000000000142, -3.309499999999999886, 0.000000000000000000 ) ) ;
#28484=ORIENTED_EDGE ( 'NONE', *, *, #33260, .F. ) ;
#28486=VERTEX_POINT ( 'NONE', #100091 ) ;
#28490=CARTESIAN_POINT ( 'NONE',  ( 29.34999999999999787, 3.309500000000003439, 0.000000000000000000 ) ) ;
#28496=AXIS2_PLACEMENT_3D ( 'NONE', #39711, #14875, #97383 ) ;
#28500=ADVANCED_FACE ( 'NONE', ( #37537 ), #57905, .T. ) ;
#28517=ORIENTED_EDGE ( 'NONE', *, *, #69339, .T. ) ;
#28527=ORIENTED_EDGE ( 'NONE', *, *, #48323, .F. ) ;
#28529=AXIS2_PLACEMENT_3D ( 'NONE', #91549, #9532, #32791 ) ;
#28538=DIRECTION ( 'NONE',  ( 0.000000000000000000, -1.000000000000000000, 0.000000000000000000 ) ) ;
#28576=ORIENTED_EDGE ( 'NONE', *, *, #84920, .T. ) ;
#28581=EDGE_CURVE ( 'NONE', #84797, #93508, #68244, .T. ) ;
#28595=ORIENTED_EDGE ( 'NONE', *, *, #50411, .T. ) ;
#28737=CARTESIAN_POINT ( 'NONE',  ( 27.61650669486618881, 1.474610560812782335E-15, 0.000000000000000000 ) ) ;
#28750=EDGE_CURVE ( 'NONE', #70900, #74905, #58715, .T. ) ;
#28756=AXIS2_PLACEMENT_3D ( 'NONE', #9270, #43253, #83172 ) ;
#28758=DIRECTION ( 'NONE',  ( -1.000000000000000000, -1.224606353822377258E-16, -0.000000000000000000 ) ) ;
#28766=AXIS2_PLACEMENT_3D ( 'NONE', #16518, #58031, #8423 ) ;
#28773=CARTESIAN_POINT ( 'NONE',  ( 30.59999999999999787, 1.533819458162526451E-15, 0.000000000000000000 ) ) ;
#28804=EDGE_CURVE ( 'NONE', #80206, #64859, #7232, .T. ) ;
#28807=ORIENTED_EDGE ( 'NONE', *, *, #41815, .T. ) ;
#28814=EDGE_CURVE ( 'NONE', #104331, #16154, #40141, .T. ) ;
#28825=ORIENTED_EDGE ( 'NONE', *, *, #81751, .F. ) ;
#28828=CONICAL_SURFACE ( 'NONE', #8115, 4.000000000000001776, 0.9599310885968808105 ) ;
#28839=FACE_OUTER_BOUND ( 'NONE', #25776, .T. ) ;
#28850=VECTOR ( 'NONE', #60301, 1000.000000000000000 ) ;
#28853=CARTESIAN_POINT ( 'NONE',  ( 8.866506694866188809, 1.474610560812782335E-15, 0.000000000000000000 ) ) ;
#28881=AXIS2_PLACEMENT_3D ( 'NONE', #33853, #49461, #89931 ) ;
#28887=ORIENTED_EDGE ( 'NONE', *, *, #92131, .F. ) ;
#28909=CIRCLE ( 'NONE', #89149, 3.309500000000001663 ) ;
#28911=AXIS2_PLACEMENT_3D ( 'NONE', #41059, #49673, #66391 ) ;
#28924=AXIS2_PLACEMENT_3D ( 'NONE', #86491, #30366, #55646 ) ;
#28928=ORIENTED_EDGE ( 'NONE', *, *, #100102, .T. ) ;
#28929=DIRECTION ( 'NONE',  ( 0.5735764363510466035, -0.8191520442889914655, 1.003171929053524500E-16 ) ) ;
#28932=ORIENTED_EDGE ( 'NONE', *, *, #53491, .T. ) ;
#28946=EDGE_CURVE ( 'NONE', #9279, #81048, #90731, .T. ) ;
#28956=ORIENTED_EDGE ( 'NONE', *, *, #2626, .T. ) ;
#28962=EDGE_CURVE ( 'NONE', #58076, #92260, #1148, .T. ) ;
#28965=LINE ( 'NONE', #5688, #46731 ) ;
#28974=CARTESIAN_POINT ( 'NONE',  ( 17.33349330513380337, 1.593028355512270567E-15, 0.000000000000000000 ) ) ;
#28984=CARTESIAN_POINT ( 'NONE',  ( 46.36650669486618881, 1.474610560812782335E-15, 0.000000000000000000 ) ) ;
#28987=CARTESIAN_POINT ( 'NONE',  ( 6.562974947121715807, -7.579827465851462165, -0.5629870116737624164 ) ) ;
#29001=CIRCLE ( 'NONE', #87706, 4.000000000000001776 ) ;
#29024=ADVANCED_FACE ( 'NONE', ( #32615 ), #52836, .T. ) ;
#29041=EDGE_LOOP ( 'NONE', ( #56918, #37421, #95664, #10376, #3795, #69425 ) ) ;
#29050=AXIS2_PLACEMENT_3D ( 'NONE', #52874, #36210, #93346 ) ;
#29060=EDGE_CURVE ( 'NONE', #99083, #13309, #24002, .T. ) ;
#29096=CARTESIAN_POINT ( 'NONE',  ( 42.33349330513380693, 1.593028355512270567E-15, 0.000000000000000000 ) ) ;
#29097=DIRECTION ( 'NONE',  ( 0.000000000000000000, -1.000000000000000000, 0.000000000000000000 ) ) ;
#29099=VERTEX_POINT ( 'NONE', #82183 ) ;
#29102=VERTEX_POINT ( 'NONE', #16944 ) ;
#29111=DIRECTION ( 'NONE',  ( -1.000000000000000000, -1.224606353822377258E-16, -0.000000000000000000 ) ) ;
#29118=ORIENTED_EDGE ( 'NONE', *, *, #38306, .T. ) ;
#29126=DIRECTION ( 'NONE',  ( -1.000000000000000000, -1.224606353822377258E-16, -0.000000000000000000 ) ) ;
#29134=DIRECTION ( 'NONE',  ( 0.000000000000000000, -1.000000000000000000, 0.000000000000000000 ) ) ;
#29136=DIRECTION ( 'NONE',  ( 0.000000000000000000, -1.000000000000000000, 0.000000000000000000 ) ) ;
#29197=EDGE_LOOP ( 'NONE', ( #32567, #92417, #37723 ) ) ;
#29226=DIRECTION ( 'NONE',  ( 0.000000000000000000, 1.000000000000000000, 0.000000000000000000 ) ) ;
#29230=CARTESIAN_POINT ( 'NONE',  ( 0.2573354458087866448, -6.889406814520517841, 1.067197363239228203 ) ) ;
#29245=DIRECTION ( 'NONE',  ( 0.000000000000000000, 1.000000000000000000, 0.000000000000000000 ) ) ;
#29283=LINE ( 'NONE', #62165, #24302 ) ;
#29284=LINE ( 'NONE', #92365, #23731 ) ;
#29297=DIRECTION ( 'NONE',  ( -1.000000000000000000, -1.224606353822377258E-16, -0.000000000000000000 ) ) ;
#29323=AXIS2_PLACEMENT_3D ( 'NONE', #42417, #65101, #97998 ) ;
#29326=DIRECTION ( 'NONE',  ( -1.000000000000000000, -1.224606353822377258E-16, -0.000000000000000000 ) ) ;
#29335=VERTEX_POINT ( 'NONE', #569 ) ;
#29349=CARTESIAN_POINT ( 'NONE',  ( 38.09999999999999432, 1.533819458162526451E-15, 0.000000000000000000 ) ) ;
#29351=CARTESIAN_POINT ( 'NONE',  ( 21.84999999999999787, 3.309500000000003439, 4.052968581778167743E-16 ) ) ;
#29352=ORIENTED_EDGE ( 'NONE', *, *, #60099, .T. ) ;
#29412=DIRECTION ( 'NONE',  ( -0.5735764363510497121, 0.8191520442889892450, 1.003171929053521665E-16 ) ) ;
#29430=CARTESIAN_POINT ( 'NONE',  ( 18.86650669486618881, 1.474610560812782335E-15, 0.000000000000000000 ) ) ;
#29433=CARTESIAN_POINT ( 'NONE',  ( 17.61650669486618881, 1.474610560812782335E-15, 0.000000000000000000 ) ) ;
#29512=VERTEX_POINT ( 'NONE', #94431 ) ;
#29513=CIRCLE ( 'NONE', #20908, 4.000000000000000888 ) ;
#29529=EDGE_CURVE ( 'NONE', #95250, #55889, #77705, .T. ) ;
#29540=FACE_OUTER_BOUND ( 'NONE', #35512, .T. ) ;
#29543=AXIS2_PLACEMENT_3D ( 'NONE', #93146, #12743, #36546 ) ;
#29552=AXIS2_PLACEMENT_3D ( 'NONE', #30177, #30726, #46349 ) ;
#29556=CIRCLE ( 'NONE', #79399, 4.000000000000001776 ) ;
#29559=ORIENTED_EDGE ( 'NONE', *, *, #54518, .T. ) ;
#29561=DIRECTION ( 'NONE',  ( -1.000000000000000000, -0.000000000000000000, -0.000000000000000000 ) ) ;
#29569=DIRECTION ( 'NONE',  ( 0.000000000000000000, -1.000000000000000000, 0.000000000000000000 ) ) ;
#29578=CARTESIAN_POINT ( 'NONE',  ( 6.575918192882431512, 3.850883087735901711, -6.669925161966311578 ) ) ;
#29580=CIRCLE ( 'NONE', #58810, 4.000000000000000888 ) ;
#29602=EDGE_CURVE ( 'NONE', #1636, #82896, #71840, .T. ) ;
#29603=ORIENTED_EDGE ( 'NONE', *, *, #62421, .F. ) ;
#29636=VECTOR ( 'NONE', #11551, 1000.000000000000000 ) ;
#29645=CARTESIAN_POINT ( 'NONE',  ( 16.36650669486618881, 1.474610560812782335E-15, 0.000000000000000000 ) ) ;
#29648=DIRECTION ( 'NONE',  ( -1.000000000000000000, -1.224606353822377258E-16, -0.000000000000000000 ) ) ;
#29658=EDGE_CURVE ( 'NONE', #55349, #100024, #64698, .T. ) ;
#29698=DIRECTION ( 'NONE',  ( 0.000000000000000000, -1.000000000000000000, 0.000000000000000000 ) ) ;
#29713=DIRECTION ( 'NONE',  ( 0.000000000000000000, -1.000000000000000000, 0.000000000000000000 ) ) ;
#29715=VERTEX_POINT ( 'NONE', #52219 ) ;
#29741=DIRECTION ( 'NONE',  ( -1.000000000000000000, -1.224606353822377258E-16, -0.000000000000000000 ) ) ;
#29750=ORIENTED_EDGE ( 'NONE', *, *, #2319, .T. ) ;
#29761=DIRECTION ( 'NONE',  ( 0.000000000000000000, -1.000000000000000000, 0.000000000000000000 ) ) ;
#29774=AXIS2_PLACEMENT_3D ( 'NONE', #41431, #91594, #50048 ) ;
#29778=EDGE_CURVE ( 'NONE', #48427, #76319, #89104, .T. ) ;
#29792=DIRECTION ( 'NONE',  ( -1.000000000000000000, -1.224606353822377258E-16, -0.000000000000000000 ) ) ;
#29796=CARTESIAN_POINT ( 'NONE',  ( 6.281178480976146616, 3.752776749732564809, 6.499999999999995559 ) ) ;
#29798=DIRECTION ( 'NONE',  ( 0.000000000000000000, -1.000000000000000000, 0.000000000000000000 ) ) ;
#29799=DIRECTION ( 'NONE',  ( 0.000000000000000000, 0.000000000000000000, 1.000000000000000000 ) ) ;
#29852=ORIENTED_EDGE ( 'NONE', *, *, #2980, .T. ) ;
#29943=CARTESIAN_POINT ( 'NONE',  ( 20.59999999999999787, 1.533819458162526451E-15, 0.000000000000000000 ) ) ;
#30016=CARTESIAN_POINT ( 'NONE',  ( 6.562934840145641324, -4.277581483015143959, -6.282640795011894319 ) ) ;
#30055=CARTESIAN_POINT ( 'NONE',  ( 13.58349330513380160, 1.593028355512270567E-15, 0.000000000000000000 ) ) ;
#30057=VECTOR ( 'NONE', #7881, 1000.000000000000000 ) ;
#30059=ORIENTED_EDGE ( 'NONE', *, *, #11543, .T. ) ;
#30076=CARTESIAN_POINT ( 'NONE',  ( 22.33349330513380337, 1.593028355512270567E-15, 0.000000000000000000 ) ) ;
#30090=VECTOR ( 'NONE', #103484, 1000.000000000000000 ) ;
#30101=ORIENTED_EDGE ( 'NONE', *, *, #82391, .T. ) ;
#30104=VERTEX_POINT ( 'NONE', #60100 ) ;
#30134=AXIS2_PLACEMENT_3D ( 'NONE', #86619, #4615, #12682 ) ;
#30137=ADVANCED_FACE ( 'NONE', ( #56186 ), #39525, .F. ) ;
#30163=DIRECTION ( 'NONE',  ( -1.000000000000000000, -1.224606353822377258E-16, -0.000000000000000000 ) ) ;
#30177=CARTESIAN_POINT ( 'NONE',  ( 32.61650669486618881, 1.474610560812782335E-15, 0.000000000000000000 ) ) ;
#30200=CIRCLE ( 'NONE', #88704, 4.000000000000001776 ) ;
#30202=ORIENTED_EDGE ( 'NONE', *, *, #56646, .F. ) ;
#30239=ADVANCED_FACE ( 'NONE', ( #97723 ), #14150, .F. ) ;
#30276=AXIS2_PLACEMENT_3D ( 'NONE', #12567, #54605, #61695 ) ;
#30292=CARTESIAN_POINT ( 'NONE',  ( 33.58349330513379982, 1.593028355512270567E-15, 0.000000000000000000 ) ) ;
#30300=CARTESIAN_POINT ( 'NONE',  ( 8.866506694866188809, 4.000000000000003553, 4.898587196589414801E-16 ) ) ;
#30343=VECTOR ( 'NONE', #44043, 1000.000000000000000 ) ;
#30347=AXIS2_PLACEMENT_3D ( 'NONE', #103070, #84757, #101473 ) ;
#30351=CIRCLE ( 'NONE', #83745, 4.000000000000001776 ) ;
#30354=ORIENTED_EDGE ( 'NONE', *, *, #27043, .T. ) ;
#30365=DIRECTION ( 'NONE',  ( 0.000000000000000000, -1.000000000000000000, 0.000000000000000000 ) ) ;
#30366=DIRECTION ( 'NONE',  ( 1.000000000000000000, 1.224606353822377258E-16, 0.000000000000000000 ) ) ;
#30372=ORIENTED_EDGE ( 'NONE', *, *, #12233, .F. ) ;
#30393=CARTESIAN_POINT ( 'NONE',  ( 0.000000000000000000, 0.000000000000000000, 0.000000000000000000 ) ) ;
#30420=AXIS2_PLACEMENT_3D ( 'NONE', #100050, #49361, #252 ) ;
#30443=VECTOR ( 'NONE', #36296, 1000.000000000000000 ) ;
#30445=CARTESIAN_POINT ( 'NONE',  ( 36.84999999999999432, 3.309500000000003439, 4.052968581778167743E-16 ) ) ;
#30499=ORIENTED_EDGE ( 'NONE', *, *, #86784, .T. ) ;
#30508=EDGE_CURVE ( 'NONE', #82981, #6993, #15175, .T. ) ;
#30509=ORIENTED_EDGE ( 'NONE', *, *, #63976, .T. ) ;
#30520=ORIENTED_EDGE ( 'NONE', *, *, #105357, .T. ) ;
#30537=DIRECTION ( 'NONE',  ( -1.000000000000000000, -1.224606353822377258E-16, -0.000000000000000000 ) ) ;
#30551=CARTESIAN_POINT ( 'NONE',  ( 0.000000000000000000, 4.898587196589412829E-16, -4.000000000000000000 ) ) ;
#30568=ORIENTED_EDGE ( 'NONE', *, *, #88829, .F. ) ;
#30587=LINE ( 'NONE', #13295, #10600 ) ;
#30590=ORIENTED_EDGE ( 'NONE', *, *, #50404, .F. ) ;
#30593=AXIS2_PLACEMENT_3D ( 'NONE', #99336, #48138, #65402 ) ;
#30628=DIRECTION ( 'NONE',  ( 1.000000000000000000, 1.224606353822377258E-16, 0.000000000000000000 ) ) ;
#30642=VERTEX_POINT ( 'NONE', #19408 ) ;
#30656=ORIENTED_EDGE ( 'NONE', *, *, #95335, .T. ) ;
#30662=DIRECTION ( 'NONE',  ( 1.000000000000000000, 1.224606353822377258E-16, 0.000000000000000000 ) ) ;
#30672=AXIS2_PLACEMENT_3D ( 'NONE', #54421, #4847, #70109 ) ;
#30674=AXIS2_PLACEMENT_3D ( 'NONE', #55823, #6230, #47222 ) ;
#30689=CARTESIAN_POINT ( 'NONE',  ( 29.83349330513380337, 1.593028355512270567E-15, 0.000000000000000000 ) ) ;
#30699=EDGE_LOOP ( 'NONE', ( #29559, #49204, #89510, #105783, #2607 ) ) ;
#30725=EDGE_CURVE ( 'NONE', #78066, #99126, #82397, .T. ) ;
#30726=DIRECTION ( 'NONE',  ( -1.000000000000000000, -1.224606353822377258E-16, -0.000000000000000000 ) ) ;
#30739=DIRECTION ( 'NONE',  ( 0.000000000000000000, -1.000000000000000000, 0.000000000000000000 ) ) ;
#30750=FACE_OUTER_BOUND ( 'NONE', #100018, .T. ) ;
#30773=DIRECTION ( 'NONE',  ( -1.000000000000000000, -1.224606353822377258E-16, -0.000000000000000000 ) ) ;
#30784=CONICAL_SURFACE ( 'NONE', #42756, 3.309500000000001663, 0.9599310885968770357 ) ;
#30785=ORIENTED_EDGE ( 'NONE', *, *, #81041, .F. ) ;
#30786=ORIENTED_EDGE ( 'NONE', *, *, #44327, .F. ) ;
#30804=VECTOR ( 'NONE', #92625, 1000.000000000000000 ) ;
#30806=EDGE_LOOP ( 'NONE', ( #41793, #65332, #98543, #20365, #14038 ) ) ;
#30834=CYLINDRICAL_SURFACE ( 'NONE', #33677, 4.000000000000000000 ) ;
#30855=ADVANCED_FACE ( 'NONE', ( #71607 ), #96109, .T. ) ;
#30871=AXIS2_PLACEMENT_3D ( 'NONE', #21522, #4248, #45767 ) ;
#30873=ORIENTED_EDGE ( 'NONE', *, *, #19474, .T. ) ;
#30880=DIRECTION ( 'NONE',  ( 0.000000000000000000, -1.000000000000000000, 0.000000000000000000 ) ) ;
#30913=AXIS2_PLACEMENT_3D ( 'NONE', #88419, #12383, #30739 ) ;
#30920=EDGE_CURVE ( 'NONE', #75440, #35999, #3102, .T. ) ;
#30931=DIRECTION ( 'NONE',  ( 0.000000000000000000, -1.000000000000000000, 0.000000000000000000 ) ) ;
#30954=AXIS2_PLACEMENT_3D ( 'NONE', #60085, #10946, #92408 ) ;
#30955=FACE_OUTER_BOUND ( 'NONE', #50324, .T. ) ;
#30981=VERTEX_POINT ( 'NONE', #65658 ) ;
#30989=AXIS2_PLACEMENT_3D ( 'NONE', #27322, #99007, #66128 ) ;
#30996=DIRECTION ( 'NONE',  ( 0.000000000000000000, -1.224646799147353700E-16, 1.000000000000000000 ) ) ;
#31025=EDGE_LOOP ( 'NONE', ( #8467, #16136, #89407, #20985, #66465 ) ) ;
#31043=DIRECTION ( 'NONE',  ( 0.000000000000000000, 1.000000000000000000, 0.000000000000000000 ) ) ;
#31047=DIRECTION ( 'NONE',  ( -1.000000000000000000, -1.224606353822377258E-16, -0.000000000000000000 ) ) ;
#31062=CARTESIAN_POINT ( 'NONE',  ( 40.59999999999999432, -3.309499999999999886, 0.000000000000000000 ) ) ;
#31073=VECTOR ( 'NONE', #99707, 1000.000000000000114 ) ;
#31074=VERTEX_POINT ( 'NONE', #45122 ) ;
#31083=CIRCLE ( 'NONE', #67237, 4.000000000000000888 ) ;
#31090=EDGE_CURVE ( 'NONE', #79890, #16749, #82473, .T. ) ;
#31122=EDGE_CURVE ( 'NONE', #99083, #73940, #63432, .T. ) ;
#31140=CARTESIAN_POINT ( 'NONE',  ( 21.84999999999999787, 1.533819458162526451E-15, 0.000000000000000000 ) ) ;
#31156=CIRCLE ( 'NONE', #93183, 4.000000000000000888 ) ;
#31157=DIRECTION ( 'NONE',  ( 0.000000000000000000, 0.000000000000000000, 1.000000000000000000 ) ) ;
#31183=ORIENTED_EDGE ( 'NONE', *, *, #18444, .T. ) ;
#31200=VERTEX_POINT ( 'NONE', #102272 ) ;
#31246=AXIS2_PLACEMENT_3D ( 'NONE', #58114, #34944, #101251 ) ;
#31265=AXIS2_PLACEMENT_3D ( 'NONE', #62021, #62534, #21560 ) ;
#31273=DIRECTION ( 'NONE',  ( 0.000000000000000000, -1.000000000000000000, 0.000000000000000000 ) ) ;
#31296=VERTEX_POINT ( 'NONE', #67477 ) ;
#31323=CONICAL_SURFACE ( 'NONE', #74312, 4.000000000000001776, 0.9599310885968808105 ) ;
#31336=EDGE_CURVE ( 'NONE', #63670, #105753, #54900, .T. ) ;
#31367=CARTESIAN_POINT ( 'NONE',  ( 27.33349330513380337, -7.703719777548943412E-31, 4.000000000000001776 ) ) ;
#31389=CARTESIAN_POINT ( 'NONE',  ( 47.40949999999999420, 0.000000000000000000, 4.000000000000000000 ) ) ;
#31390=CARTESIAN_POINT ( 'NONE',  ( 0.000000000000000000, 0.000000000000000000, 0.000000000000000000 ) ) ;
#31414=CARTESIAN_POINT ( 'NONE',  ( 40.59999999999999432, 1.533819458162526451E-15, 0.000000000000000000 ) ) ;
#31418=CONICAL_SURFACE ( 'NONE', #50313, 3.309500000000001663, 0.9599310885968770357 ) ;
#31431=ORIENTED_EDGE ( 'NONE', *, *, #16782, .T. ) ;
#31456=DIRECTION ( 'NONE',  ( 0.000000000000000000, 0.000000000000000000, 1.000000000000000000 ) ) ;
#31475=VECTOR ( 'NONE', #44569, 1000.000000000000000 ) ;
#31530=EDGE_LOOP ( 'NONE', ( #106093, #83569, #69342, #61532, #16264, #82023 ) ) ;
#31534=CARTESIAN_POINT ( 'NONE',  ( 16.84999999999999787, -3.309499999999999886, 0.000000000000000000 ) ) ;
#31553=DIRECTION ( 'NONE',  ( -0.5735764363510494901, -0.8191520442889894671, 0.000000000000000000 ) ) ;
#31567=ORIENTED_EDGE ( 'NONE', *, *, #48889, .T. ) ;
#31587=EDGE_LOOP ( 'NONE', ( #46479, #33168, #49986, #35985, #38093 ) ) ;
#31598=SURFACE_SIDE_STYLE ('',( #97352 ) ) ;
#31599=LINE ( 'NONE', #46691, #20877 ) ;
#31600=EDGE_LOOP ( 'NONE', ( #65355, #76169, #87779, #38502, #4935, #43953 ) ) ;
#31603=EDGE_LOOP ( 'NONE', ( #46807, #93864, #52139, #77457, #85576, #63803 ) ) ;
#31604=DIRECTION ( 'NONE',  ( 0.000000000000000000, -1.000000000000000000, 0.000000000000000000 ) ) ;
#31617=VECTOR ( 'NONE', #79719, 1000.000000000000000 ) ;
#31620=CARTESIAN_POINT ( 'NONE',  ( 19.34999999999999787, -3.309499999999999886, 0.000000000000000000 ) ) ;
#31625=ORIENTED_EDGE ( 'NONE', *, *, #28962, .F. ) ;
#31692=VERTEX_POINT ( 'NONE', #75828 ) ;
#31701=DIRECTION ( 'NONE',  ( 0.000000000000000000, -1.000000000000000000, 0.000000000000000000 ) ) ;
#31715=EDGE_CURVE ( 'NONE', #33833, #103460, #106643, .T. ) ;
#31750=CIRCLE ( 'NONE', #38610, 4.000000000000000000 ) ;
#31769=ORIENTED_EDGE ( 'NONE', *, *, #63025, .F. ) ;
#31781=VERTEX_POINT ( 'NONE', #86615 ) ;
#31814=EDGE_LOOP ( 'NONE', ( #82807, #3464 ) ) ;
#31836=ORIENTED_EDGE ( 'NONE', *, *, #18437, .T. ) ;
#31851=VECTOR ( 'NONE', #82260, 1000.000000000000000 ) ;
#31880=ORIENTED_EDGE ( 'NONE', *, *, #105270, .F. ) ;
#31903=CARTESIAN_POINT ( 'NONE',  ( 19.34999999999999787, -3.309499999999999886, 4.475777889183790779E-16 ) ) ;
#31920=ORIENTED_EDGE ( 'NONE', *, *, #79256, .T. ) ;
#31945=VECTOR ( 'NONE', #68090, 1000.000000000000000 ) ;
#31946=EDGE_CURVE ( 'NONE', #3450, #73270, #100698, .T. ) ;
#31974=DIRECTION ( 'NONE',  ( -1.000000000000000000, -0.000000000000000000, -0.000000000000000000 ) ) ;
#32011=EDGE_CURVE ( 'NONE', #39800, #61594, #27196, .T. ) ;
#32012=VERTEX_POINT ( 'NONE', #91889 ) ;
#32023=FACE_OUTER_BOUND ( 'NONE', #31603, .T. ) ;
#32027=ORIENTED_EDGE ( 'NONE', *, *, #34908, .F. ) ;
#32029=CARTESIAN_POINT ( 'NONE',  ( 0.000000000000000000, 4.898587196589412829E-16, -4.000000000000000000 ) ) ;
#32035=ORIENTED_EDGE ( 'NONE', *, *, #31715, .F. ) ;
#32059=CARTESIAN_POINT ( 'NONE',  ( 0.000000000000000000, 0.000000000000000000, 0.000000000000000000 ) ) ;
#32075=CARTESIAN_POINT ( 'NONE',  ( 0.2565376335220204695, -2.516992571281984947, -6.499999999999999112 ) ) ;
#32077=CARTESIAN_POINT ( 'NONE',  ( 43.58349330513380693, 1.593028355512270567E-15, 0.000000000000000000 ) ) ;
#32078=DIRECTION ( 'NONE',  ( -0.5735764363510494901, -0.8191520442889894671, 0.000000000000000000 ) ) ;
#32080=DIRECTION ( 'NONE',  ( -0.5735764363510494901, -0.8191520442889894671, 0.000000000000000000 ) ) ;
#32086=ORIENTED_EDGE ( 'NONE', *, *, #93126, .F. ) ;
#32164=VECTOR ( 'NONE', #53080, 1000.000000000000000 ) ;
#32189=VECTOR ( 'NONE', #48126, 1000.000000000000000 ) ;
#32198=EDGE_CURVE ( 'NONE', #52930, #27869, #68878, .T. ) ;
#32216=ORIENTED_EDGE ( 'NONE', *, *, #73533, .T. ) ;
#32253=CARTESIAN_POINT ( 'NONE',  ( 11.36650669486618881, 1.474610560812782335E-15, 0.000000000000000000 ) ) ;
#32257=EDGE_CURVE ( 'NONE', #105650, #94111, #51598, .T. ) ;
#32272=CIRCLE ( 'NONE', #73574, 3.309500000000001663 ) ;
#32273=CIRCLE ( 'NONE', #63301, 4.000000000000001776 ) ;
#32297=DIRECTION ( 'NONE',  ( -1.000000000000000000, -1.224606353822377258E-16, -0.000000000000000000 ) ) ;
#32300=LINE ( 'NONE', #65171, #95855 ) ;
#32308=CYLINDRICAL_SURFACE ( 'NONE', #70866, 4.000000000000000000 ) ;
#32332=VERTEX_POINT ( 'NONE', #27074 ) ;
#32352=AXIS2_PLACEMENT_3D ( 'NONE', #47932, #22650, #64157 ) ;
#32355=CARTESIAN_POINT ( 'NONE',  ( 0.000000000000000000, 0.000000000000000000, 4.000000000000000000 ) ) ;
#32360=DIRECTION ( 'NONE',  ( -1.000000000000000000, -0.000000000000000000, -0.000000000000000000 ) ) ;
#32386=CARTESIAN_POINT ( 'NONE',  ( 6.463481858019715531, 7.246446802359423067, -1.128819432756289487 ) ) ;
#32410=AXIS2_PLACEMENT_3D ( 'NONE', #36817, #45417, #86419 ) ;
#32421=CIRCLE ( 'NONE', #87538, 3.309500000000001663 ) ;
#32431=AXIS2_PLACEMENT_3D ( 'NONE', #64495, #72045, #97366 ) ;
#32443=ADVANCED_FACE ( 'NONE', ( #62083 ), #87797, .T. ) ;
#32452=DIRECTION ( 'NONE',  ( 0.000000000000000000, -1.000000000000000000, 0.000000000000000000 ) ) ;
#32466=CARTESIAN_POINT ( 'NONE',  ( 41.36650669486618881, -3.851859888774471706E-31, 4.000000000000000888 ) ) ;
#32469=DIRECTION ( 'NONE',  ( -1.000000000000000000, -1.224606353822377258E-16, -0.000000000000000000 ) ) ;
#32483=EDGE_LOOP ( 'NONE', ( #69792, #82200, #67061, #28326, #26911 ) ) ;
#32484=CIRCLE ( 'NONE', #63444, 3.309500000000001663 ) ;
#32507=EDGE_CURVE ( 'NONE', #31074, #45473, #104964, .T. ) ;
#32522=EDGE_CURVE ( 'NONE', #68449, #59572, #94667, .T. ) ;
#32527=VERTEX_POINT ( 'NONE', #64707 ) ;
#32534=FACE_OUTER_BOUND ( 'NONE', #24447, .T. ) ;
#32540=ADVANCED_FACE ( 'NONE', ( #97061 ), #70620, .T. ) ;
#32550=EDGE_CURVE ( 'NONE', #26186, #93546, #105682, .T. ) ;
#32565=EDGE_CURVE ( 'NONE', #49522, #99943, #99634, .T. ) ;
#32567=ORIENTED_EDGE ( 'NONE', *, *, #65521, .T. ) ;
#32570=CARTESIAN_POINT ( 'NONE',  ( 27.33349330513380337, 4.898587196589405926E-16, -4.000000000000001776 ) ) ;
#32572=CYLINDRICAL_SURFACE ( 'NONE', #11382, 4.000000000000000000 ) ;
#32593=DIRECTION ( 'NONE',  ( -1.000000000000000000, -1.224606353822377258E-16, -0.000000000000000000 ) ) ;
#32595=DIRECTION ( 'NONE',  ( 0.000000000000000000, 0.000000000000000000, 1.000000000000000000 ) ) ;
#32615=FACE_OUTER_BOUND ( 'NONE', #41761, .T. ) ;
#32649=DIRECTION ( 'NONE',  ( -1.000000000000000000, -1.224606353822377258E-16, -0.000000000000000000 ) ) ;
#32655=ORIENTED_EDGE ( 'NONE', *, *, #26221, .T. ) ;
#32740=EDGE_LOOP ( 'NONE', ( #36755, #89387, #85169, #98596, #11772, #22987 ) ) ;
#32780=ORIENTED_EDGE ( 'NONE', *, *, #60152, .T. ) ;
#32791=DIRECTION ( 'NONE',  ( 0.000000000000000000, 1.000000000000000000, 0.000000000000000000 ) ) ;
#32821=AXIS2_PLACEMENT_3D ( 'NONE', #14015, #21629, #72267 ) ;
#32827=CARTESIAN_POINT ( 'NONE',  ( 15.59999999999999787, 1.533819458162526451E-15, 0.000000000000000000 ) ) ;
#32841=CARTESIAN_POINT ( 'NONE',  ( 28.09999999999999787, 3.309500000000003439, 4.052968581778167743E-16 ) ) ;
#32872=CARTESIAN_POINT ( 'NONE',  ( 12.33349330513380337, 1.593028355512270567E-15, 0.000000000000000000 ) ) ;
#32889=DIRECTION ( 'NONE',  ( -1.000000000000000000, -1.224606353822377258E-16, -0.000000000000000000 ) ) ;
#32892=DIRECTION ( 'NONE',  ( 0.5735764363510466035, -0.8191520442889914655, 1.003171929053524500E-16 ) ) ;
#32916=CIRCLE ( 'NONE', #93178, 4.000000000000000888 ) ;
#32918=AXIS2_PLACEMENT_3D ( 'NONE', #97353, #30537, #13249 ) ;
#32943=CARTESIAN_POINT ( 'NONE',  ( 6.326622418652845248, -1.327077765692999733, 6.831545684615177194 ) ) ;
#32945=DIRECTION ( 'NONE',  ( 0.000000000000000000, -1.000000000000000000, 0.000000000000000000 ) ) ;
#32972=VERTEX_POINT ( 'NONE', #10061 ) ;
#32985=ORIENTED_EDGE ( 'NONE', *, *, #55159, .F. ) ;
#33074=ORIENTED_EDGE ( 'NONE', *, *, #86794, .F. ) ;
#33082=CARTESIAN_POINT ( 'NONE',  ( 48.10000000000000142, 0.000000000000000000, 0.000000000000000000 ) ) ;
#33104=VERTEX_POINT ( 'NONE', #57805 ) ;
#33107=AXIS2_PLACEMENT_3D ( 'NONE', #9912, #50894, #83277 ) ;
#33121=CARTESIAN_POINT ( 'NONE',  ( 21.36650669486618881, 1.474610560812782335E-15, 0.000000000000000000 ) ) ;
#33168=ORIENTED_EDGE ( 'NONE', *, *, #33450, .T. ) ;
#33181=CARTESIAN_POINT ( 'NONE',  ( 38.58349330513380693, 1.593028355512270567E-15, 0.000000000000000000 ) ) ;
#33195=ORIENTED_EDGE ( 'NONE', *, *, #50250, .F. ) ;
#33197=ORIENTED_EDGE ( 'NONE', *, *, #19382, .F. ) ;
#33199=EDGE_CURVE ( 'NONE', #49522, #63698, #55666, .T. ) ;
#33204=ORIENTED_EDGE ( 'NONE', *, *, #63437, .T. ) ;
#33218=DIRECTION ( 'NONE',  ( 0.000000000000000000, -1.000000000000000000, 0.000000000000000000 ) ) ;
#33229=CARTESIAN_POINT ( 'NONE',  ( 0.000000000000000000, 0.000000000000000000, 0.000000000000000000 ) ) ;
#33232=DIRECTION ( 'NONE',  ( 0.5735764363510466035, -0.8191520442889914655, 1.003171929053524500E-16 ) ) ;
#33260=EDGE_CURVE ( 'NONE', #92310, #83331, #92858, .T. ) ;
#33313=ORIENTED_EDGE ( 'NONE', *, *, #106495, .F. ) ;
#33325=AXIS2_PLACEMENT_3D ( 'NONE', #44991, #70317, #54623 ) ;
#33331=DIRECTION ( 'NONE',  ( -1.000000000000000000, -0.000000000000000000, -0.000000000000000000 ) ) ;
#33355=ADVANCED_FACE ( 'NONE', ( #100934 ), #11849, .T. ) ;
#33389=CIRCLE ( 'NONE', #33325, 3.309500000000001663 ) ;
#33394=( GEOMETRIC_REPRESENTATION_CONTEXT ( 3 ) GLOBAL_UNCERTAINTY_ASSIGNED_CONTEXT ( ( #314 ) ) GLOBAL_UNIT_ASSIGNED_CONTEXT ( ( #86417, #52410, #93958 ) ) REPRESENTATION_CONTEXT ( 'NONE', 'WORKASPACE' ) );
#33425=CARTESIAN_POINT ( 'NONE',  ( 0.000000000000000000, 4.898587196589412829E-16, -4.000000000000000000 ) ) ;
#33427=ORIENTED_EDGE ( 'NONE', *, *, #73053, .T. ) ;
#33428=EDGE_LOOP ( 'NONE', ( #5668, #39709, #2326, #91248, #10996 ) ) ;
#33432=ORIENTED_EDGE ( 'NONE', *, *, #101380, .T. ) ;
#33450=EDGE_CURVE ( 'NONE', #78409, #87161, #23992, .T. ) ;
#33461=ORIENTED_EDGE ( 'NONE', *, *, #97343, .T. ) ;
#33465=ORIENTED_EDGE ( 'NONE', *, *, #96715, .F. ) ;
#33488=ADVANCED_FACE ( 'NONE', ( #34120 ), #68715, .T. ) ;
#33491=DIRECTION ( 'NONE',  ( -1.000000000000000000, -1.224606353822377258E-16, -0.000000000000000000 ) ) ;
#33511=EDGE_LOOP ( 'NONE', ( #28527, #36703, #106737, #5915, #16569 ) ) ;
#33542=EDGE_CURVE ( 'NONE', #74736, #6290, #82541, .T. ) ;
#33545=AXIS2_PLACEMENT_3D ( 'NONE', #14588, #89566, #56100 ) ;
#33612=CARTESIAN_POINT ( 'NONE',  ( 16.08349330513380337, 4.000000000000003553, 0.000000000000000000 ) ) ;
#33618=ORIENTED_EDGE ( 'NONE', *, *, #72780, .F. ) ;
#33624=DIRECTION ( 'NONE',  ( -1.000000000000000000, -1.224606353822377258E-16, -0.000000000000000000 ) ) ;
#33636=AXIS2_PLACEMENT_3D ( 'NONE', #25132, #101119, #59616 ) ;
#33637=ORIENTED_EDGE ( 'NONE', *, *, #64129, .T. ) ;
#33642=AXIS2_PLACEMENT_3D ( 'NONE', #1702, #66997, #34658 ) ;
#33647=CIRCLE ( 'NONE', #2595, 4.000000000000001776 ) ;
#33677=AXIS2_PLACEMENT_3D ( 'NONE', #6504, #65287, #39442 ) ;
#33678=CARTESIAN_POINT ( 'NONE',  ( 6.683837171061805194, -3.955946848495972556, -6.851900933636989599 ) ) ;
#33687=ORIENTED_EDGE ( 'NONE', *, *, #91651, .F. ) ;
#33704=ORIENTED_EDGE ( 'NONE', *, *, #27024, .T. ) ;
#33714=FACE_OUTER_BOUND ( 'NONE', #81541, .T. ) ;
#33794=DIRECTION ( 'NONE',  ( 0.000000000000000000, -1.000000000000000000, 0.000000000000000000 ) ) ;
#33826=AXIS2_PLACEMENT_3D ( 'NONE', #17860, #44254, #2169 ) ;
#33829=CARTESIAN_POINT ( 'NONE',  ( 21.36650669486618881, 4.000000000000003553, 4.898587196589414801E-16 ) ) ;
#33833=VERTEX_POINT ( 'NONE', #60586 ) ;
#33843=EDGE_LOOP ( 'NONE', ( #40785, #19533 ) ) ;
#33845=VERTEX_POINT ( 'NONE', #16929 ) ;
#33853=CARTESIAN_POINT ( 'NONE',  ( 23.58349330513380337, 1.593028355512270567E-15, 0.000000000000000000 ) ) ;
#33858=CARTESIAN_POINT ( 'NONE',  ( 6.445370176742044599, 4.584736124524362744, -5.738941594274773905 ) ) ;
#33947=ADVANCED_FACE ( 'NONE', ( #61611 ), #85888, .T. ) ;
#34003=DIRECTION ( 'NONE',  ( -1.000000000000000000, -1.224606353822377258E-16, -0.000000000000000000 ) ) ;
#34032=ORIENTED_EDGE ( 'NONE', *, *, #63982, .T. ) ;
#34051=DIRECTION ( 'NONE',  ( -1.000000000000000000, -0.000000000000000000, -0.000000000000000000 ) ) ;
#34067=AXIS2_PLACEMENT_3D ( 'NONE', #99919, #50822, #19054 ) ;
#34091=CYLINDRICAL_SURFACE ( 'NONE', #4503, 4.000000000000000000 ) ;
#34111=AXIS2_PLACEMENT_3D ( 'NONE', #58070, #26297, #66710 ) ;
#34120=FACE_OUTER_BOUND ( 'NONE', #49580, .T. ) ;
#34125=VERTEX_POINT ( 'NONE', #89976 ) ;
#34131=CIRCLE ( 'NONE', #59996, 4.000000000000001776 ) ;
#34136=AXIS2_PLACEMENT_3D ( 'NONE', #101803, #43047, #83489 ) ;
#34150=AXIS2_PLACEMENT_3D ( 'NONE', #59763, #50047, #9052 ) ;
#34152=FACE_OUTER_BOUND ( 'NONE', #58501, .T. ) ;
#34171=VERTEX_POINT ( 'NONE', #66768 ) ;
#34172=CIRCLE ( 'NONE', #99574, 4.000000000000000888 ) ;
#34205=ORIENTED_EDGE ( 'NONE', *, *, #105765, .F. ) ;
#34216=LINE ( 'NONE', #58997, #65657 ) ;
#34223=ORIENTED_EDGE ( 'NONE', *, *, #86522, .T. ) ;
#34235=CARTESIAN_POINT ( 'NONE',  ( 22.61650669486618526, 1.474610560812782335E-15, 0.000000000000000000 ) ) ;
#34248=ORIENTED_EDGE ( 'NONE', *, *, #18437, .F. ) ;
#34249=CARTESIAN_POINT ( 'NONE',  ( 17.61650669486618881, 1.474610560812782335E-15, 0.000000000000000000 ) ) ;
#34255=DIRECTION ( 'NONE',  ( 0.000000000000000000, -1.000000000000000000, 0.000000000000000000 ) ) ;
#34297=VECTOR ( 'NONE', #103407, 1000.000000000000000 ) ;
#34339=CARTESIAN_POINT ( 'NONE',  ( 0.000000000000000000, 4.898587196589412829E-16, -4.000000000000000000 ) ) ;
#34355=ORIENTED_EDGE ( 'NONE', *, *, #47887, .T. ) ;
#34396=CARTESIAN_POINT ( 'NONE',  ( 16.08349330513380337, -4.000000000000000888, 4.898587196589416773E-16 ) ) ;
#34398=CARTESIAN_POINT ( 'NONE',  ( 6.222742520105473574, 7.673830019007162662, 0.2914634815676387380 ) ) ;
#34400=AXIS2_PLACEMENT_3D ( 'NONE', #44827, #77713, #102519 ) ;
#34403=ORIENTED_EDGE ( 'NONE', *, *, #9345, .T. ) ;
#34418=EDGE_CURVE ( 'NONE', #70900, #74232, #36244, .T. ) ;
#34419=EDGE_CURVE ( 'NONE', #6164, #64268, #38153, .T. ) ;
#34429=CARTESIAN_POINT ( 'NONE',  ( 14.83349330513380337, 4.000000000000002665, 0.000000000000000000 ) ) ;
#34455=EDGE_LOOP ( 'NONE', ( #16255, #5930, #51502, #20277, #38819 ) ) ;
#34476=VECTOR ( 'NONE', #324, 1000.000000000000000 ) ;
#34497=CIRCLE ( 'NONE', #8574, 4.000000000000001776 ) ;
#34501=B_SPLINE_CURVE_WITH_KNOTS ( 'NONE', 3,
 ( #68951, #85663, #44673, #26394, #59258, #43591 ),
 .UNSPECIFIED., .F., .F.,
 ( 4, 2, 4 ),
 ( 0.01913986446825127405, 0.02104055318008571374, 0.02294124189192014995 ),
 .UNSPECIFIED. ) ;
#34518=VERTEX_POINT ( 'NONE', #1340 ) ;
#34553=CARTESIAN_POINT ( 'NONE',  ( 38.58349330513380693, 4.000000000000003553, 0.000000000000000000 ) ) ;
#34588=FACE_OUTER_BOUND ( 'NONE', #95659, .T. ) ;
#34599=EDGE_CURVE ( 'NONE', #82896, #26696, #31083, .T. ) ;
#34602=AXIS2_PLACEMENT_3D ( 'NONE', #101187, #8969, #75841 ) ;
#34603=CARTESIAN_POINT ( 'NONE',  ( 0.000000000000000000, 0.000000000000000000, 0.000000000000000000 ) ) ;
#34613=ORIENTED_EDGE ( 'NONE', *, *, #16880, .T. ) ;
#34658=DIRECTION ( 'NONE',  ( 0.000000000000000000, -1.000000000000000000, 0.000000000000000000 ) ) ;
#34673=ORIENTED_EDGE ( 'NONE', *, *, #59744, .T. ) ;
#34710=EDGE_CURVE ( 'NONE', #103853, #28486, #17272, .T. ) ;
#34724=EDGE_CURVE ( 'NONE', #65781, #10582, #43128, .T. ) ;
#34739=ORIENTED_EDGE ( 'NONE', *, *, #97312, .F. ) ;
#34746=EDGE_CURVE ( 'NONE', #105753, #64733, #49966, .T. ) ;
#34750=CARTESIAN_POINT ( 'NONE',  ( 16.84999999999999787, 3.309500000000003439, 0.000000000000000000 ) ) ;
#34780=DIRECTION ( 'NONE',  ( -1.000000000000000000, -1.224606353822377258E-16, -0.000000000000000000 ) ) ;
#34789=CARTESIAN_POINT ( 'NONE',  ( 6.585468679846623985, -3.617797563910821079, -6.733790807807556789 ) ) ;
#34796=EDGE_LOOP ( 'NONE', ( #74656, #28956, #83212, #12391, #79280, #70454 ) ) ;
#34820=CARTESIAN_POINT ( 'NONE',  ( 12.33349330513380337, 1.593028355512270567E-15, 0.000000000000000000 ) ) ;
#34823=LINE ( 'NONE', #75770, #18146 ) ;
#34829=EDGE_LOOP ( 'NONE', ( #15867, #11466, #23831, #42213, #41877 ) ) ;
#34831=CARTESIAN_POINT ( 'NONE',  ( 48.10000000000000142, 0.000000000000000000, 0.000000000000000000 ) ) ;
#34850=VECTOR ( 'NONE', #20108, 1000.000000000000000 ) ;
#34900=CARTESIAN_POINT ( 'NONE',  ( 6.333820801330125150, 4.275724398227219503, 5.594228103108966010 ) ) ;
#34908=EDGE_CURVE ( 'NONE', #21459, #444, #67325, .T. ) ;
#34912=ORIENTED_EDGE ( 'NONE', *, *, #9827, .F. ) ;
#34922=ORIENTED_EDGE ( 'NONE', *, *, #104303, .F. ) ;
#34925=DIRECTION ( 'NONE',  ( -1.000000000000000000, -0.000000000000000000, -0.000000000000000000 ) ) ;
#34938=DIRECTION ( 'NONE',  ( 0.000000000000000000, -1.000000000000000000, 0.000000000000000000 ) ) ;
#34944=DIRECTION ( 'NONE',  ( -1.000000000000000000, -0.000000000000000000, -0.000000000000000000 ) ) ;
#34951=DIRECTION ( 'NONE',  ( 0.000000000000000000, -1.000000000000000000, 0.000000000000000000 ) ) ;
#34974=CARTESIAN_POINT ( 'NONE',  ( 26.08349330513380337, 4.898587196589405926E-16, -4.000000000000001776 ) ) ;
#34984=CARTESIAN_POINT ( 'NONE',  ( 0.5805565836007605673, 3.752776749732565253, 6.499999999999997335 ) ) ;
#34996=EDGE_LOOP ( 'NONE', ( #4956, #37827, #82297, #42372, #46924 ) ) ;
#35003=CARTESIAN_POINT ( 'NONE',  ( 6.289572920342626716, 5.584521518880458224, 3.985288806461539046 ) ) ;
#35008=DIRECTION ( 'NONE',  ( 0.000000000000000000, -1.000000000000000000, 0.000000000000000000 ) ) ;
#35027=ADVANCED_FACE ( 'NONE', ( #86707 ), #105925, .T. ) ;
#35034=ORIENTED_EDGE ( 'NONE', *, *, #1876, .T. ) ;
#35037=CIRCLE ( 'NONE', #9180, 3.309500000000001663 ) ;
#35056=VERTEX_POINT ( 'NONE', #64538 ) ;
#35059=DIRECTION ( 'NONE',  ( 0.000000000000000000, 1.000000000000000000, 0.000000000000000000 ) ) ;
#35063=EDGE_CURVE ( 'NONE', #34125, #97567, #100770, .T. ) ;
#35078=AXIS2_PLACEMENT_3D ( 'NONE', #94690, #12141, #52597 ) ;
#35079=EDGE_CURVE ( 'NONE', #74552, #52930, #50791, .T. ) ;
#35090=ORIENTED_EDGE ( 'NONE', *, *, #43431, .T. ) ;
#35121=ORIENTED_EDGE ( 'NONE', *, *, #13823, .F. ) ;
#35127=CARTESIAN_POINT ( 'NONE',  ( 38.58349330513380693, -4.000000000000000888, 4.898587196589416773E-16 ) ) ;
#35140=CARTESIAN_POINT ( 'NONE',  ( 6.162888688655344005, 3.752776749732561257, -6.499999999999999112 ) ) ;
#35164=ORIENTED_EDGE ( 'NONE', *, *, #57378, .F. ) ;
#35191=ADVANCED_FACE ( 'NONE', ( #52583 ), #86050, .T. ) ;
#35206=EDGE_CURVE ( 'NONE', #45468, #25329, #57716, .T. ) ;
#35212=DIRECTION ( 'NONE',  ( 0.000000000000000000, 0.000000000000000000, 1.000000000000000000 ) ) ;
#35222=EDGE_LOOP ( 'NONE', ( #13448, #20353, #52187, #92184 ) ) ;
#35227=DIRECTION ( 'NONE',  ( -1.000000000000000000, -0.000000000000000000, -0.000000000000000000 ) ) ;
#35228=EDGE_LOOP ( 'NONE', ( #47918, #9339, #46907, #33432, #8856 ) ) ;
#35249=CARTESIAN_POINT ( 'NONE',  ( 34.35000000000000142, 1.533819458162526451E-15, 0.000000000000000000 ) ) ;
#35270=CARTESIAN_POINT ( 'NONE',  ( 29.34999999999999787, 3.309500000000003439, 4.052968581778167743E-16 ) ) ;
#35296=CIRCLE ( 'NONE', #23195, 4.000000000000001776 ) ;
#35301=DIRECTION ( 'NONE',  ( 1.000000000000000000, 0.000000000000000000, 0.000000000000000000 ) ) ;
#35308=AXIS2_PLACEMENT_3D ( 'NONE', #100014, #60652, #50918 ) ;
#35310=ORIENTED_EDGE ( 'NONE', *, *, #23124, .T. ) ;
#35317=CARTESIAN_POINT ( 'NONE',  ( 5.975663821522259944, -4.257391242883624471, -5.625982059626766230 ) ) ;
#35328=EDGE_CURVE ( 'NONE', #54801, #13998, #71962, .T. ) ;
#35351=LINE ( 'NONE', #18084, #55891 ) ;
#35354=DIRECTION ( 'NONE',  ( 0.000000000000000000, -1.000000000000000000, 0.000000000000000000 ) ) ;
#35374=AXIS2_PLACEMENT_3D ( 'NONE', #33121, #42234, #97819 ) ;
#35375=DIRECTION ( 'NONE',  ( 0.5735764363510466035, -0.8191520442889914655, 1.003171929053524500E-16 ) ) ;
#35387=VERTEX_POINT ( 'NONE', #90269 ) ;
#35402=CARTESIAN_POINT ( 'NONE',  ( 14.34999999999999787, 1.533819458162526451E-15, 0.000000000000000000 ) ) ;
#35424=FACE_OUTER_BOUND ( 'NONE', #4877, .T. ) ;
#35426=VERTEX_POINT ( 'NONE', #9324 ) ;
#35431=CARTESIAN_POINT ( 'NONE',  ( 48.10000000000000142, 0.000000000000000000, 0.000000000000000000 ) ) ;
#35443=EDGE_CURVE ( 'NONE', #65538, #20373, #81822, .T. ) ;
#35466=AXIS2_PLACEMENT_3D ( 'NONE', #60019, #67561, #10360 ) ;
#35475=CARTESIAN_POINT ( 'NONE',  ( 40.11650669486618881, 1.474610560812782335E-15, 0.000000000000000000 ) ) ;
#35485=DIRECTION ( 'NONE',  ( -1.000000000000000000, -1.224606353822377258E-16, -0.000000000000000000 ) ) ;
#35490=EDGE_CURVE ( 'NONE', #59773, #103513, #43964, .T. ) ;
#35499=CARTESIAN_POINT ( 'NONE',  ( 0.000000000000000000, 4.898587196589412829E-16, -4.000000000000000000 ) ) ;
#35512=EDGE_LOOP ( 'NONE', ( #32985, #84659, #77674, #23200, #104230 ) ) ;
#35519=CARTESIAN_POINT ( 'NONE',  ( 0.2595206531158509300, 2.531175536751804511, 6.499999999999996447 ) ) ;
#35526=CIRCLE ( 'NONE', #25208, 4.000000000000000888 ) ;
#35537=ADVANCED_FACE ( 'NONE', ( #89747 ), #54323, .T. ) ;
#35538=DIRECTION ( 'NONE',  ( 1.000000000000000000, 1.224606353822377258E-16, 0.000000000000000000 ) ) ;
#35550=VERTEX_POINT ( 'NONE', #76194 ) ;
#35560=DIRECTION ( 'NONE',  ( -1.000000000000000000, -1.224606353822377258E-16, -0.000000000000000000 ) ) ;
#35583=CARTESIAN_POINT ( 'NONE',  ( 6.222582369487714260, -4.088457415080680057, 6.500000000000000888 ) ) ;
#35602=DIRECTION ( 'NONE',  ( 0.000000000000000000, -1.000000000000000000, 0.000000000000000000 ) ) ;
#35660=VERTEX_POINT ( 'NONE', #63224 ) ;
#35686=VECTOR ( 'NONE', #54856, 1000.000000000000000 ) ;
#35709=DIRECTION ( 'NONE',  ( 0.000000000000000000, -1.000000000000000000, 0.000000000000000000 ) ) ;
#35710=CARTESIAN_POINT ( 'NONE',  ( 31.08349330513380337, 4.000000000000002665, 0.000000000000000000 ) ) ;
#35720=CIRCLE ( 'NONE', #28881, 4.000000000000001776 ) ;
#35746=DIRECTION ( 'NONE',  ( -0.5735764363510494901, -0.8191520442889894671, 0.000000000000000000 ) ) ;
#35752=FILL_AREA_STYLE_COLOUR ( '', #91894 ) ;
#35755=CONICAL_SURFACE ( 'NONE', #92519, 4.000000000000001776, 0.9599310885968808105 ) ;
#35762=AXIS2_PLACEMENT_3D ( 'NONE', #51065, #43002, #892 ) ;
#35768=FACE_OUTER_BOUND ( 'NONE', #14427, .T. ) ;
#35778=ORIENTED_EDGE ( 'NONE', *, *, #61347, .T. ) ;
#35795=CARTESIAN_POINT ( 'NONE',  ( 12.33349330513380337, 4.000000000000002665, 0.000000000000000000 ) ) ;
#35808=ORIENTED_EDGE ( 'NONE', *, *, #64692, .T. ) ;
#35812=ORIENTED_EDGE ( 'NONE', *, *, #55486, .T. ) ;
#35849=CARTESIAN_POINT ( 'NONE',  ( 48.10000000000000142, 4.052968581778165278E-16, -3.309499999999999886 ) ) ;
#35875=ORIENTED_EDGE ( 'NONE', *, *, #62328, .T. ) ;
#35892=CIRCLE ( 'NONE', #39327, 4.000000000000001776 ) ;
#35901=EDGE_CURVE ( 'NONE', #39684, #106458, #66388, .T. ) ;
#35909=CONICAL_SURFACE ( 'NONE', #8284, 3.309500000000001663, 0.9599310885968770357 ) ;
#35912=CARTESIAN_POINT ( 'NONE',  ( 30.11650669486618881, 1.474610560812782335E-15, 0.000000000000000000 ) ) ;
#35928=ORIENTED_EDGE ( 'NONE', *, *, #98743, .F. ) ;
#35969=VERTEX_POINT ( 'NONE', #9200 ) ;
#35985=ORIENTED_EDGE ( 'NONE', *, *, #69952, .F. ) ;
#35997=LINE ( 'NONE', #3046, #30343 ) ;
#35999=VERTEX_POINT ( 'NONE', #549 ) ;
#36017=CYLINDRICAL_SURFACE ( 'NONE', #88711, 4.000000000000000000 ) ;
#36018=AXIS2_PLACEMENT_3D ( 'NONE', #47900, #80806, #39318 ) ;
#36021=CIRCLE ( 'NONE', #8391, 4.000000000000001776 ) ;
#36026=VERTEX_POINT ( 'NONE', #24895 ) ;
#36030=DIRECTION ( 'NONE',  ( -1.000000000000000000, -1.224606353822377258E-16, -0.000000000000000000 ) ) ;
#36053=DIRECTION ( 'NONE',  ( 0.000000000000000000, 1.000000000000000000, 0.000000000000000000 ) ) ;
#36054=DIRECTION ( 'NONE',  ( 1.000000000000000000, 0.000000000000000000, 0.000000000000000000 ) ) ;
#36060=DIRECTION ( 'NONE',  ( -1.000000000000000000, -0.000000000000000000, -0.000000000000000000 ) ) ;
#36075=CARTESIAN_POINT ( 'NONE',  ( 22.61650669486618526, 1.474610560812782335E-15, 0.000000000000000000 ) ) ;
#36129=CARTESIAN_POINT ( 'NONE',  ( 5.980097492742836529, -2.767486787161697492, 6.500000000000000000 ) ) ;
#36152=CARTESIAN_POINT ( 'NONE',  ( 34.83349330513379982, 1.593028355512270567E-15, 0.000000000000000000 ) ) ;
#36182=AXIS2_PLACEMENT_3D ( 'NONE', #52545, #61193, #54123 ) ;
#36186=CARTESIAN_POINT ( 'NONE',  ( 14.83349330513380337, 1.593028355512270567E-15, 0.000000000000000000 ) ) ;
#36210=DIRECTION ( 'NONE',  ( -1.000000000000000000, -1.224606353822377258E-16, -0.000000000000000000 ) ) ;
#36218=ORIENTED_EDGE ( 'NONE', *, *, #76436, .T. ) ;
#36226=DIRECTION ( 'NONE',  ( 0.5735764363510466035, -0.8191520442889914655, 1.003171929053524500E-16 ) ) ;
#36244=CIRCLE ( 'NONE', #56888, 6.500000000000000888 ) ;
#36264=ORIENTED_EDGE ( 'NONE', *, *, #84338, .F. ) ;
#36292=SURFACE_STYLE_FILL_AREA ( #61064 ) ;
#36294=AXIS2_PLACEMENT_3D ( 'NONE', #2810, #102040, #10889 ) ;
#36296=DIRECTION ( 'NONE',  ( -0.5735764363510494901, -0.8191520442889894671, 0.000000000000000000 ) ) ;
#36298=ADVANCED_FACE ( 'NONE', ( #92790 ), #100347, .T. ) ;
#36308=CARTESIAN_POINT ( 'NONE',  ( 0.000000000000000000, 0.000000000000000000, 0.000000000000000000 ) ) ;
#36340=AXIS2_PLACEMENT_3D ( 'NONE', #100816, #17274, #35602 ) ;
#36366=FACE_OUTER_BOUND ( 'NONE', #99883, .T. ) ;
#36395=AXIS2_PLACEMENT_3D ( 'NONE', #60363, #93237, #28538 ) ;
#36418=AXIS2_PLACEMENT_3D ( 'NONE', #74848, #64653, #90520 ) ;
#36422=EDGE_CURVE ( 'NONE', #31296, #13541, #35526, .T. ) ;
#36475=CARTESIAN_POINT ( 'NONE',  ( 20.11650669486618881, 4.898587196589411843E-16, -4.000000000000000888 ) ) ;
#36502=ORIENTED_EDGE ( 'NONE', *, *, #28385, .F. ) ;
#36528=ORIENTED_EDGE ( 'NONE', *, *, #88915, .T. ) ;
#36536=CARTESIAN_POINT ( 'NONE',  ( 19.83349330513379982, 4.000000000000003553, 0.000000000000000000 ) ) ;
#36546=DIRECTION ( 'NONE',  ( 0.000000000000000000, 0.000000000000000000, 1.000000000000000000 ) ) ;
#36559=DIRECTION ( 'NONE',  ( -1.000000000000000000, -1.224606353822377258E-16, -0.000000000000000000 ) ) ;
#36564=EDGE_CURVE ( 'NONE', #31296, #56662, #80045, .T. ) ;
#36565=CARTESIAN_POINT ( 'NONE',  ( 44.35000000000000142, -3.309499999999999886, 4.475777889183790779E-16 ) ) ;
#36578=EDGE_CURVE ( 'NONE', #77668, #25666, #94087, .T. ) ;
#36586=CIRCLE ( 'NONE', #101981, 4.000000000000000888 ) ;
#36613=CARTESIAN_POINT ( 'NONE',  ( 6.643884894376894223, 3.901062859471879030, -6.756839076125894294 ) ) ;
#36642=VECTOR ( 'NONE', #47191, 1000.000000000000000 ) ;
#36643=EDGE_CURVE ( 'NONE', #55983, #51415, #30351, .T. ) ;
#36648=ORIENTED_EDGE ( 'NONE', *, *, #36578, .T. ) ;
#36656=CARTESIAN_POINT ( 'NONE',  ( 6.168902648239040332, 0.6556005035805820835, 6.499999999999999112 ) ) ;
#36668=CARTESIAN_POINT ( 'NONE',  ( 23.58349330513380337, 1.593028355512270567E-15, 0.000000000000000000 ) ) ;
#36684=CARTESIAN_POINT ( 'NONE',  ( 28.09999999999999787, 1.533819458162526451E-15, 0.000000000000000000 ) ) ;
#36685=CARTESIAN_POINT ( 'NONE',  ( 5.947762761376478302, -2.501851166488387790, -6.500000000000002665 ) ) ;
#36703=ORIENTED_EDGE ( 'NONE', *, *, #99870, .T. ) ;
#36730=EDGE_CURVE ( 'NONE', #76929, #81954, #42782, .T. ) ;
#36734=AXIS2_PLACEMENT_3D ( 'NONE', #9930, #41240, #1285 ) ;
#36742=CIRCLE ( 'NONE', #5738, 4.000000000000001776 ) ;
#36754=DIRECTION ( 'NONE',  ( -0.5735764363510497121, 0.8191520442889892450, 1.003171929053521665E-16 ) ) ;
#36755=ORIENTED_EDGE ( 'NONE', *, *, #48689, .T. ) ;
#36770=EDGE_CURVE ( 'NONE', #63953, #99126, #18533, .T. ) ;
#36787=DIRECTION ( 'NONE',  ( 0.000000000000000000, -1.000000000000000000, 0.000000000000000000 ) ) ;
#36791=DIRECTION ( 'NONE',  ( -1.000000000000000000, -1.224606353822377258E-16, -0.000000000000000000 ) ) ;
#36797=DIRECTION ( 'NONE',  ( -1.000000000000000000, -1.224606353822377258E-16, -0.000000000000000000 ) ) ;
#36806=LINE ( 'NONE', #3343, #71395 ) ;
#36817=CARTESIAN_POINT ( 'NONE',  ( 24.34999999999999787, 1.533819458162526451E-15, 0.000000000000000000 ) ) ;
#36826=ORIENTED_EDGE ( 'NONE', *, *, #79828, .T. ) ;
#36853=DIRECTION ( 'NONE',  ( 0.000000000000000000, 0.000000000000000000, -1.000000000000000000 ) ) ;
#36877=CARTESIAN_POINT ( 'NONE',  ( 19.83349330513379982, 1.593028355512270567E-15, 0.000000000000000000 ) ) ;
#36883=CARTESIAN_POINT ( 'NONE',  ( 42.33349330513380693, 1.593028355512270567E-15, 0.000000000000000000 ) ) ;
#36899=CARTESIAN_POINT ( 'NONE',  ( 38.58349330513380693, -7.703719777548943412E-31, 4.000000000000001776 ) ) ;
#36901=CARTESIAN_POINT ( 'NONE',  ( 35.59999999999999432, 1.533819458162526451E-15, 0.000000000000000000 ) ) ;
#36905=DIRECTION ( 'NONE',  ( 0.000000000000000000, 1.000000000000000000, 0.000000000000000000 ) ) ;
#36910=ORIENTED_EDGE ( 'NONE', *, *, #88722, .F. ) ;
#36943=CARTESIAN_POINT ( 'NONE',  ( 9.833493305133801599, -7.703719777548943412E-31, 4.000000000000001776 ) ) ;
#36965=ADVANCED_FACE ( 'NONE', ( #46501 ), #20139, .T. ) ;
#37001=DIRECTION ( 'NONE',  ( 0.000000000000000000, 1.000000000000000000, 0.000000000000000000 ) ) ;
#37048=DIRECTION ( 'NONE',  ( 0.000000000000000000, -1.000000000000000000, 0.000000000000000000 ) ) ;
#37065=CIRCLE ( 'NONE', #54163, 4.000000000000001776 ) ;
#37071=CARTESIAN_POINT ( 'NONE',  ( 0.000000000000000000, 0.000000000000000000, 4.000000000000000000 ) ) ;
#37108=ADVANCED_FACE ( 'NONE', ( #85249 ), #43720, .T. ) ;
#37112=EDGE_CURVE ( 'NONE', #6290, #74736, #26984, .T. ) ;
#37163=EDGE_LOOP ( 'NONE', ( #82704, #22247, #43620, #12382, #28370 ) ) ;
#37179=EDGE_CURVE ( 'NONE', #55349, #74552, #68302, .T. ) ;
#37258=DIRECTION ( 'NONE',  ( -1.000000000000000000, -1.224606353822377258E-16, -0.000000000000000000 ) ) ;
#37278=VECTOR ( 'NONE', #44598, 1000.000000000000114 ) ;
#37302=FACE_OUTER_BOUND ( 'NONE', #35228, .T. ) ;
#37354=AXIS2_PLACEMENT_3D ( 'NONE', #70979, #70460, #61854 ) ;
#37376=AXIS2_PLACEMENT_3D ( 'NONE', #66651, #18121, #27304 ) ;
#37383=ORIENTED_EDGE ( 'NONE', *, *, #46202, .T. ) ;
#37420=FACE_OUTER_BOUND ( 'NONE', #86244, .T. ) ;
#37421=ORIENTED_EDGE ( 'NONE', *, *, #76903, .T. ) ;
#37430=LINE ( 'NONE', #54081, #44040 ) ;
#37432=DIRECTION ( 'NONE',  ( 0.000000000000000000, -1.000000000000000000, 0.000000000000000000 ) ) ;
#37443=EDGE_CURVE ( 'NONE', #99943, #48231, #105144, .T. ) ;
#37445=ORIENTED_EDGE ( 'NONE', *, *, #65246, .T. ) ;
#37447=CARTESIAN_POINT ( 'NONE',  ( 21.84999999999999787, -3.309499999999999886, 4.475777889183790779E-16 ) ) ;
#37448=CARTESIAN_POINT ( 'NONE',  ( 48.10000000000000142, 0.000000000000000000, 3.309499999999999886 ) ) ;
#37458=ORIENTED_EDGE ( 'NONE', *, *, #61657, .T. ) ;
#37470=CIRCLE ( 'NONE', #4708, 3.309500000000001663 ) ;
#37496=EDGE_CURVE ( 'NONE', #87130, #73965, #2593, .T. ) ;
#37505=CARTESIAN_POINT ( 'NONE',  ( 6.936184427528457874, 1.053834543709838281E-15, 8.605212085995399107 ) ) ;
#37517=EDGE_CURVE ( 'NONE', #958, #5935, #55835, .T. ) ;
#37522=AXIS2_PLACEMENT_3D ( 'NONE', #34603, #84182, #17333 ) ;
#37537=FACE_OUTER_BOUND ( 'NONE', #731, .T. ) ;
#37538=ORIENTED_EDGE ( 'NONE', *, *, #96907, .F. ) ;
#37547=DIRECTION ( 'NONE',  ( 0.5735764363510466035, -0.8191520442889914655, 1.003171929053524500E-16 ) ) ;
#37550=ORIENTED_EDGE ( 'NONE', *, *, #67786, .T. ) ;
#37562=DIRECTION ( 'NONE',  ( 0.000000000000000000, -1.000000000000000000, 0.000000000000000000 ) ) ;
#37601=CARTESIAN_POINT ( 'NONE',  ( 17.61650669486618881, 1.474610560812782335E-15, 0.000000000000000000 ) ) ;
#37614=VECTOR ( 'NONE', #52511, 999.9999999999998863 ) ;
#37624=EDGE_CURVE ( 'NONE', #7789, #11792, #21901, .T. ) ;
#37646=DIRECTION ( 'NONE',  ( 0.000000000000000000, 0.000000000000000000, -1.000000000000000000 ) ) ;
#37648=EDGE_CURVE ( 'NONE', #9279, #78066, #5272, .T. ) ;
#37649=AXIS2_PLACEMENT_3D ( 'NONE', #60439, #93315, #19471 ) ;
#37667=CARTESIAN_POINT ( 'NONE',  ( 44.83349330513380693, 1.593028355512270567E-15, 0.000000000000000000 ) ) ;
#37711=EDGE_CURVE ( 'NONE', #85984, #75882, #1250, .T. ) ;
#37717=DIRECTION ( 'NONE',  ( 0.000000000000000000, 0.000000000000000000, -1.000000000000000000 ) ) ;
#37723=ORIENTED_EDGE ( 'NONE', *, *, #24505, .F. ) ;
#37741=ORIENTED_EDGE ( 'NONE', *, *, #27122, .F. ) ;
#37775=EDGE_LOOP ( 'NONE', ( #65968, #1441, #104640, #96992, #51574, #14613 ) ) ;
#37789=DIRECTION ( 'NONE',  ( -1.000000000000000000, -1.224606353822377258E-16, -0.000000000000000000 ) ) ;
#37796=CONICAL_SURFACE ( 'NONE', #15416, 4.000000000000001776, 0.9599310885968808105 ) ;
#37806=ORIENTED_EDGE ( 'NONE', *, *, #35063, .T. ) ;
#37824=CARTESIAN_POINT ( 'NONE',  ( 43.10000000000000142, 1.533819458162526451E-15, 0.000000000000000000 ) ) ;
#37827=ORIENTED_EDGE ( 'NONE', *, *, #89470, .T. ) ;
#37894=ORIENTED_EDGE ( 'NONE', *, *, #73094, .F. ) ;
#37917=AXIS2_PLACEMENT_3D ( 'NONE', #69300, #28322, #35354 ) ;
#37926=ORIENTED_EDGE ( 'NONE', *, *, #105675, .F. ) ;
#37930=ORIENTED_EDGE ( 'NONE', *, *, #40352, .T. ) ;
#37950=CARTESIAN_POINT ( 'NONE',  ( 20.11650669486618881, -3.999999999999998224, 0.000000000000000000 ) ) ;
#37969=AXIS2_PLACEMENT_3D ( 'NONE', #29943, #63894, #20825 ) ;
#37973=LINE ( 'NONE', #13104, #6556 ) ;
#37982=LINE ( 'NONE', #54102, #47067 ) ;
#38020=DIRECTION ( 'NONE',  ( 0.000000000000000000, -1.000000000000000000, 0.000000000000000000 ) ) ;
#38023=ADVANCED_FACE ( 'NONE', ( #54590 ), #54637, .T. ) ;
#38066=CARTESIAN_POINT ( 'NONE',  ( -5.641239428713638286E-16, -0.6346842323199932689, -6.500000000000000000 ) ) ;
#38073=ORIENTED_EDGE ( 'NONE', *, *, #23747, .T. ) ;
#38076=DIRECTION ( 'NONE',  ( -1.000000000000000000, -1.224606353822377258E-16, -0.000000000000000000 ) ) ;
#38091=CARTESIAN_POINT ( 'NONE',  ( 5.947762761376481855, -6.880090707843056208, -1.083333333333333259 ) ) ;
#38093=ORIENTED_EDGE ( 'NONE', *, *, #53491, .F. ) ;
#38112=CARTESIAN_POINT ( 'NONE',  ( 48.10000000000000142, 0.000000000000000000, 0.000000000000000000 ) ) ;
#38117=AXIS2_PLACEMENT_3D ( 'NONE', #87974, #63167, #45917 ) ;
#38153=LINE ( 'NONE', #14348, #55107 ) ;
#38177=LINE ( 'NONE', #39217, #90765 ) ;
#38222=DIRECTION ( 'NONE',  ( -1.000000000000000000, -1.224606353822377258E-16, -0.000000000000000000 ) ) ;
#38233=CARTESIAN_POINT ( 'NONE',  ( 5.975663821522314123, -7.000939006314191637, 0.8740179403730684582 ) ) ;
#38235=CARTESIAN_POINT ( 'NONE',  ( 22.33349330513380337, -4.000000000000000000, 4.898587196589415787E-16 ) ) ;
#38236=FACE_OUTER_BOUND ( 'NONE', #64990, .T. ) ;
#38293=DIRECTION ( 'NONE',  ( -1.000000000000000000, -1.224606353822377258E-16, -0.000000000000000000 ) ) ;
#38300=DIRECTION ( 'NONE',  ( -1.000000000000000000, -1.224606353822377258E-16, -0.000000000000000000 ) ) ;
#38301=ADVANCED_FACE ( 'NONE', ( #23494, #39666 ), #88736, .T. ) ;
#38305=VECTOR ( 'NONE', #87458, 1000.000000000000114 ) ;
#38306=EDGE_CURVE ( 'NONE', #103934, #74067, #58115, .T. ) ;
#38358=CARTESIAN_POINT ( 'NONE',  ( 0.5805565836007701153, -7.505553499465148271, -1.383738442504732931E-16 ) ) ;
#38389=ORIENTED_EDGE ( 'NONE', *, *, #103598, .F. ) ;
#38407=DIRECTION ( 'NONE',  ( 0.000000000000000000, -1.000000000000000000, 0.000000000000000000 ) ) ;
#38409=CARTESIAN_POINT ( 'NONE',  ( 10.59999999999999609, 3.309500000000003439, 4.052968581778167743E-16 ) ) ;
#38502=ORIENTED_EDGE ( 'NONE', *, *, #104431, .T. ) ;
#38510=EDGE_CURVE ( 'NONE', #44939, #87130, #78906, .T. ) ;
#38537=CARTESIAN_POINT ( 'NONE',  ( 33.58349330513379982, 4.000000000000002665, 0.000000000000000000 ) ) ;
#38560=FACE_OUTER_BOUND ( 'NONE', #20497, .T. ) ;
#38562=ORIENTED_EDGE ( 'NONE', *, *, #24932, .T. ) ;
#38600=DIRECTION ( 'NONE',  ( -1.000000000000000000, -1.224606353822377258E-16, -0.000000000000000000 ) ) ;
#38606=EDGE_CURVE ( 'NONE', #73965, #77684, #99525, .T. ) ;
#38610=AXIS2_PLACEMENT_3D ( 'NONE', #14277, #96813, #47176 ) ;
#38615=EDGE_CURVE ( 'NONE', #56862, #12958, #71737, .T. ) ;
#38618=ORIENTED_EDGE ( 'NONE', *, *, #81851, .T. ) ;
#38621=DIRECTION ( 'NONE',  ( -1.000000000000000000, -0.000000000000000000, -0.000000000000000000 ) ) ;
#38628=VERTEX_POINT ( 'NONE', #11510 ) ;
#38632=CARTESIAN_POINT ( 'NONE',  ( 6.463344223170843783, -7.245769408789104027, -1.129975644293424786 ) ) ;
#38635=ORIENTED_EDGE ( 'NONE', *, *, #36578, .F. ) ;
#38644=DIRECTION ( 'NONE',  ( -0.000000000000000000, 0.000000000000000000, 1.000000000000000000 ) ) ;
#38646=DIRECTION ( 'NONE',  ( 0.000000000000000000, -1.000000000000000000, 0.000000000000000000 ) ) ;
#38669=AXIS2_PLACEMENT_3D ( 'NONE', #15438, #48328, #47272 ) ;
#38696=ORIENTED_EDGE ( 'NONE', *, *, #2460, .T. ) ;
#38750=CIRCLE ( 'NONE', #30134, 3.309500000000001663 ) ;
#38802=EDGE_CURVE ( 'NONE', #25666, #35056, #25520, .T. ) ;
#38819=ORIENTED_EDGE ( 'NONE', *, *, #87105, .T. ) ;
#38823=CARTESIAN_POINT ( 'NONE',  ( 0.000000000000000000, 0.000000000000000000, 4.000000000000000000 ) ) ;
#38834=EDGE_CURVE ( 'NONE', #55889, #62536, #27219, .T. ) ;
#38856=ORIENTED_EDGE ( 'NONE', *, *, #70473, .F. ) ;
#38892=ADVANCED_FACE ( 'NONE', ( #39163 ), #54713, .T. ) ;
#38901=ORIENTED_EDGE ( 'NONE', *, *, #93806, .F. ) ;
#38918=EDGE_LOOP ( 'NONE', ( #62297, #4396, #51162, #71362, #62054 ) ) ;
#38924=CARTESIAN_POINT ( 'NONE',  ( 6.394343112843832166, 3.776352960569632877, 6.540835195019754522 ) ) ;
#38945=AXIS2_PLACEMENT_3D ( 'NONE', #12352, #29648, #12879 ) ;
#38969=ORIENTED_EDGE ( 'NONE', *, *, #64517, .F. ) ;
#39005=LINE ( 'NONE', #66861, #68477 ) ;
#39034=CIRCLE ( 'NONE', #28496, 6.500000000000000888 ) ;
#39040=EDGE_LOOP ( 'NONE', ( #20775, #102531, #6091, #89768, #37894, #42030 ) ) ;
#39102=EDGE_CURVE ( 'NONE', #104331, #91175, #70860, .T. ) ;
#39105=FACE_OUTER_BOUND ( 'NONE', #34829, .T. ) ;
#39116=ORIENTED_EDGE ( 'NONE', *, *, #19424, .F. ) ;
#39152=DIRECTION ( 'NONE',  ( 0.000000000000000000, -1.000000000000000000, 0.000000000000000000 ) ) ;
#39153=ORIENTED_EDGE ( 'NONE', *, *, #25289, .T. ) ;
#39156=FACE_OUTER_BOUND ( 'NONE', #17478, .T. ) ;
#39160=CARTESIAN_POINT ( 'NONE',  ( 6.326592304916282217, -6.579439845142166732, -2.267162479624768689 ) ) ;
#39163=FACE_OUTER_BOUND ( 'NONE', #44578, .T. ) ;
#39167=EDGE_CURVE ( 'NONE', #23893, #53830, #80662, .T. ) ;
#39187=CIRCLE ( 'NONE', #20289, 3.309500000000001663 ) ;
#39199=CIRCLE ( 'NONE', #97756, 3.309500000000001663 ) ;
#39217=CARTESIAN_POINT ( 'NONE',  ( 0.000000000000000000, 4.898587196589412829E-16, -4.000000000000000000 ) ) ;
#39229=ORIENTED_EDGE ( 'NONE', *, *, #96902, .T. ) ;
#39259=VECTOR ( 'NONE', #48160, 1000.000000000000114 ) ;
#39288=ORIENTED_EDGE ( 'NONE', *, *, #92468, .T. ) ;
#39298=DIRECTION ( 'NONE',  ( -1.000000000000000000, -0.000000000000000000, -0.000000000000000000 ) ) ;
#39318=DIRECTION ( 'NONE',  ( 0.000000000000000000, -1.000000000000000000, 0.000000000000000000 ) ) ;
#39326=DIRECTION ( 'NONE',  ( -0.5735764363510497121, 0.8191520442889892450, 1.003171929053521665E-16 ) ) ;
#39327=AXIS2_PLACEMENT_3D ( 'NONE', #58305, #41593, #92798 ) ;
#39340=ORIENTED_EDGE ( 'NONE', *, *, #31946, .F. ) ;
#39347=DIRECTION ( 'NONE',  ( 0.000000000000000000, -1.000000000000000000, 0.000000000000000000 ) ) ;
#39367=CARTESIAN_POINT ( 'NONE',  ( 14.34999999999999787, 1.533819458162526451E-15, 0.000000000000000000 ) ) ;
#39372=ORIENTED_EDGE ( 'NONE', *, *, #92013, .F. ) ;
#39385=DIRECTION ( 'NONE',  ( 0.000000000000000000, -1.000000000000000000, 0.000000000000000000 ) ) ;
#39390=DIRECTION ( 'NONE',  ( -1.000000000000000000, -1.224606353822377258E-16, -0.000000000000000000 ) ) ;
#39391=DIRECTION ( 'NONE',  ( 0.000000000000000000, -1.000000000000000000, 0.000000000000000000 ) ) ;
#39398=ORIENTED_EDGE ( 'NONE', *, *, #77719, .T. ) ;
#39431=ORIENTED_EDGE ( 'NONE', *, *, #66582, .F. ) ;
#39439=FACE_OUTER_BOUND ( 'NONE', #69152, .T. ) ;
#39442=DIRECTION ( 'NONE',  ( 0.000000000000000000, 0.000000000000000000, 1.000000000000000000 ) ) ;
#39462=AXIS2_PLACEMENT_3D ( 'NONE', #42368, #59100, #83888 ) ;
#39475=CONICAL_SURFACE ( 'NONE', #46396, 3.309500000000001663, 0.9599310885968770357 ) ;
#39477=ORIENTED_EDGE ( 'NONE', *, *, #59656, .F. ) ;
#39485=FACE_OUTER_BOUND ( 'NONE', #48377, .T. ) ;
#39497=CIRCLE ( 'NONE', #92905, 4.000000000000001776 ) ;
#39504=ORIENTED_EDGE ( 'NONE', *, *, #98458, .F. ) ;
#39516=FACE_OUTER_BOUND ( 'NONE', #13232, .T. ) ;
#39525=PLANE ( 'NONE',  #106402 ) ;
#39539=DIRECTION ( 'NONE',  ( -1.000000000000000000, -1.224606353822377258E-16, -0.000000000000000000 ) ) ;
#39543=EDGE_CURVE ( 'NONE', #17581, #84503, #87765, .T. ) ;
#39556=ADVANCED_FACE ( 'NONE', ( #41533 ), #92759, .T. ) ;
#39582=VECTOR ( 'NONE', #26966, 1000.000000000000000 ) ;
#39592=LINE ( 'NONE', #30445, #89328 ) ;
#39594=FACE_OUTER_BOUND ( 'NONE', #34796, .T. ) ;
#39609=ORIENTED_EDGE ( 'NONE', *, *, #17136, .T. ) ;
#39613=ADVANCED_FACE ( 'NONE', ( #16732 ), #51488, .T. ) ;
#39619=CARTESIAN_POINT ( 'NONE',  ( 6.289692432696780244, 0.6618655008720331079, -6.828989928337167115 ) ) ;
#39625=CARTESIAN_POINT ( 'NONE',  ( 0.000000000000000000, 0.000000000000000000, 0.000000000000000000 ) ) ;
#39666=FACE_OUTER_BOUND ( 'NONE', #33843, .T. ) ;
#39684=VERTEX_POINT ( 'NONE', #83575 ) ;
#39693=CARTESIAN_POINT ( 'NONE',  ( 0.000000000000000000, -5.629165124598848990, -3.250000000000003553 ) ) ;
#39700=CONICAL_SURFACE ( 'NONE', #99956, 3.309500000000001663, 0.9599310885968770357 ) ;
#39709=ORIENTED_EDGE ( 'NONE', *, *, #17076, .T. ) ;
#39711=CARTESIAN_POINT ( 'NONE',  ( 0.000000000000000000, 0.000000000000000000, 0.000000000000000000 ) ) ;
#39732=DIRECTION ( 'NONE',  ( 0.000000000000000000, -1.000000000000000000, 0.000000000000000000 ) ) ;
#39753=ORIENTED_EDGE ( 'NONE', *, *, #50265, .F. ) ;
#39759=FACE_OUTER_BOUND ( 'NONE', #67572, .T. ) ;
#39765=AXIS2_PLACEMENT_3D ( 'NONE', #79365, #80413, #38407 ) ;
#39787=EDGE_LOOP ( 'NONE', ( #54785, #92263, #28825, #50830, #6156 ) ) ;
#39800=VERTEX_POINT ( 'NONE', #67940 ) ;
#39803=ORIENTED_EDGE ( 'NONE', *, *, #65566, .T. ) ;
#39815=EDGE_CURVE ( 'NONE', #101661, #9600, #3764, .T. ) ;
#39818=ORIENTED_EDGE ( 'NONE', *, *, #97287, .T. ) ;
#39821=DIRECTION ( 'NONE',  ( 0.000000000000000000, 1.000000000000000000, 0.000000000000000000 ) ) ;
#39838=CIRCLE ( 'NONE', #82858, 4.000000000000001776 ) ;
#39855=ORIENTED_EDGE ( 'NONE', *, *, #37648, .F. ) ;
#39887=EDGE_CURVE ( 'NONE', #73382, #86709, #54868, .T. ) ;
#39897=B_SPLINE_CURVE_WITH_KNOTS ( 'NONE', 3,
 ( #17159, #908, #50548, #83463, #9563, #42470 ),
 .UNSPECIFIED., .F., .F.,
 ( 4, 2, 4 ),
 ( 2.380733003137416059E-07, 0.001898835937927372897, 0.003797433802554431997 ),
 .UNSPECIFIED. ) ;
#39908=ADVANCED_FACE ( 'NONE', ( #90508 ), #49511, .T. ) ;
#39914=AXIS2_PLACEMENT_3D ( 'NONE', #51289, #102521, #26545 ) ;
#39917=ORIENTED_EDGE ( 'NONE', *, *, #98874, .F. ) ;
#39930=FACE_OUTER_BOUND ( 'NONE', #97237, .T. ) ;
#39941=CARTESIAN_POINT ( 'NONE',  ( 17.33349330513380337, -4.000000000000000000, 4.898587196589415787E-16 ) ) ;
#39945=AXIS2_PLACEMENT_3D ( 'NONE', #56044, #80871, #66290 ) ;
#39971=ORIENTED_EDGE ( 'NONE', *, *, #97831, .F. ) ;
#39973=CARTESIAN_POINT ( 'NONE',  ( 0.000000000000000000, 0.000000000000000000, 4.000000000000000000 ) ) ;
#39997=ORIENTED_EDGE ( 'NONE', *, *, #93001, .F. ) ;
#40002=AXIS2_PLACEMENT_3D ( 'NONE', #106057, #47823, #22546 ) ;
#40008=EDGE_CURVE ( 'NONE', #18717, #44354, #85082, .T. ) ;
#40064=AXIS2_PLACEMENT_3D ( 'NONE', #19543, #61032, #43242 ) ;
#40073=DIRECTION ( 'NONE',  ( -1.000000000000000000, -0.000000000000000000, -0.000000000000000000 ) ) ;
#40078=CARTESIAN_POINT ( 'NONE',  ( 25.59999999999999787, -3.309499999999999886, 4.475777889183790779E-16 ) ) ;
#40081=DIRECTION ( 'NONE',  ( -1.000000000000000000, -1.224606353822377258E-16, -0.000000000000000000 ) ) ;
#40095=VECTOR ( 'NONE', #65399, 1000.000000000000000 ) ;
#40115=AXIS2_PLACEMENT_3D ( 'NONE', #82469, #106187, #65222 ) ;
#40128=CARTESIAN_POINT ( 'NONE',  ( 47.33349330513379982, 1.593028355512270567E-15, 0.000000000000000000 ) ) ;
#40140=CARTESIAN_POINT ( 'NONE',  ( 0.4037800551813744976, 7.199367570657607018, 0.5303295852573157720 ) ) ;
#40141=LINE ( 'NONE', #13199, #9789 ) ;
#40149=CARTESIAN_POINT ( 'NONE',  ( 6.289692432696784685, -1.240516797660047330E-13, -6.828989928337167115 ) ) ;
#40206=CIRCLE ( 'NONE', #52211, 4.000000000000000888 ) ;
#40247=CIRCLE ( 'NONE', #17863, 4.000000000000001776 ) ;
#40253=DIRECTION ( 'NONE',  ( 0.000000000000000000, -1.000000000000000000, 0.000000000000000000 ) ) ;
#40264=CARTESIAN_POINT ( 'NONE',  ( 35.11650669486618170, 1.474610560812782335E-15, 0.000000000000000000 ) ) ;
#40292=CARTESIAN_POINT ( 'NONE',  ( 6.575925811255157072, -3.850887307289496686, 6.669932470447527351 ) ) ;
#40315=VERTEX_POINT ( 'NONE', #31389 ) ;
#40330=VERTEX_POINT ( 'NONE', #31903 ) ;
#40332=CARTESIAN_POINT ( 'NONE',  ( 0.000000000000000000, 0.000000000000000000, 4.000000000000000000 ) ) ;
#40334=DIRECTION ( 'NONE',  ( 1.000000000000000000, 1.224606353822377258E-16, 0.000000000000000000 ) ) ;
#40335=EDGE_CURVE ( 'NONE', #26696, #61668, #44661, .T. ) ;
#40341=VECTOR ( 'NONE', #34925, 1000.000000000000000 ) ;
#40349=CARTESIAN_POINT ( 'NONE',  ( 36.84999999999999432, 1.533819458162526451E-15, 0.000000000000000000 ) ) ;
#40352=EDGE_CURVE ( 'NONE', #77823, #51686, #78835, .T. ) ;
#40370=FACE_OUTER_BOUND ( 'NONE', #10459, .T. ) ;
#40379=DIRECTION ( 'NONE',  ( 0.000000000000000000, -1.000000000000000000, 0.000000000000000000 ) ) ;
#40381=ORIENTED_EDGE ( 'NONE', *, *, #65093, .F. ) ;
#40403=CARTESIAN_POINT ( 'NONE',  ( 43.58349330513380693, -4.000000000000000000, 4.898587196589415787E-16 ) ) ;
#40413=AXIS2_PLACEMENT_3D ( 'NONE', #90428, #17614, #50477 ) ;
#40473=CARTESIAN_POINT ( 'NONE',  ( 44.35000000000000142, 1.533819458162526451E-15, 0.000000000000000000 ) ) ;
#40478=EDGE_CURVE ( 'NONE', #26898, #9600, #39497, .T. ) ;
#40481=CIRCLE ( 'NONE', #87016, 4.000000000000001776 ) ;
#40494=AXIS2_PLACEMENT_3D ( 'NONE', #9104, #98645, #2073 ) ;
#40523=DIRECTION ( 'NONE',  ( 0.5735764363510466035, -0.8191520442889914655, 1.003171929053524500E-16 ) ) ;
#40534=ORIENTED_EDGE ( 'NONE', *, *, #16740, .F. ) ;
#40580=AXIS2_PLACEMENT_3D ( 'NONE', #87805, #13884, #31701 ) ;
#40594=ORIENTED_EDGE ( 'NONE', *, *, #41815, .F. ) ;
#40605=DIRECTION ( 'NONE',  ( -0.5735764363510494901, -0.8191520442889894671, 0.000000000000000000 ) ) ;
#40608=EDGE_CURVE ( 'NONE', #48231, #72001, #29001, .T. ) ;
#40613=CARTESIAN_POINT ( 'NONE',  ( 34.83349330513379982, 4.000000000000003553, 0.000000000000000000 ) ) ;
#40614=ORIENTED_EDGE ( 'NONE', *, *, #50323, .T. ) ;
#40627=CARTESIAN_POINT ( 'NONE',  ( 0.000000000000000000, 4.898587196589412829E-16, -4.000000000000000000 ) ) ;
#40635=DIRECTION ( 'NONE',  ( 0.000000000000000000, -1.000000000000000000, 0.000000000000000000 ) ) ;
#40639=CONICAL_SURFACE ( 'NONE', #26903, 3.309500000000001663, 0.9599310885968770357 ) ;
#40646=ORIENTED_EDGE ( 'NONE', *, *, #20515, .T. ) ;
#40652=CARTESIAN_POINT ( 'NONE',  ( 31.36650669486618881, 4.000000000000003553, 4.898587196589414801E-16 ) ) ;
#40655=CARTESIAN_POINT ( 'NONE',  ( 27.33349330513380337, 1.593028355512270567E-15, 0.000000000000000000 ) ) ;
#40714=( LENGTH_UNIT ( ) NAMED_UNIT ( * ) SI_UNIT ( .MILLI., .METRE. ) );
#40721=AXIS2_PLACEMENT_3D ( 'NONE', #44588, #60776, #52651 ) ;
#40780=CARTESIAN_POINT ( 'NONE',  ( 42.33349330513380693, -7.703719777548943412E-31, 4.000000000000001776 ) ) ;
#40782=DIRECTION ( 'NONE',  ( 0.000000000000000000, -1.000000000000000000, 0.000000000000000000 ) ) ;
#40785=ORIENTED_EDGE ( 'NONE', *, *, #46780, .F. ) ;
#40799=CARTESIAN_POINT ( 'NONE',  ( 34.35000000000000142, 1.533819458162526451E-15, 0.000000000000000000 ) ) ;
#40825=ORIENTED_EDGE ( 'NONE', *, *, #38510, .F. ) ;
#40831=ADVANCED_FACE ( 'NONE', ( #24636 ), #35909, .T. ) ;
#40864=DIRECTION ( 'NONE',  ( 1.000000000000000000, 1.224606353822377258E-16, 0.000000000000000000 ) ) ;
#40867=AXIS2_PLACEMENT_3D ( 'NONE', #48462, #7462, #40379 ) ;
#40876=VERTEX_POINT ( 'NONE', #26778 ) ;
#40924=ORIENTED_EDGE ( 'NONE', *, *, #58122, .T. ) ;
#40930=DIRECTION ( 'NONE',  ( 0.5735764363510462704, 0.8191520442889915765, 0.000000000000000000 ) ) ;
#40944=CARTESIAN_POINT ( 'NONE',  ( 36.08349330513379982, 1.593028355512270567E-15, 0.000000000000000000 ) ) ;
#40974=AXIS2_PLACEMENT_3D ( 'NONE', #104760, #88062, #72391 ) ;
#41009=DIRECTION ( 'NONE',  ( 0.000000000000000000, -1.000000000000000000, 0.000000000000000000 ) ) ;
#41048=CARTESIAN_POINT ( 'NONE',  ( 39.83349330513380693, 1.593028355512270567E-15, 0.000000000000000000 ) ) ;
#41059=CARTESIAN_POINT ( 'NONE',  ( 33.86650669486618881, 1.474610560812782335E-15, 0.000000000000000000 ) ) ;
#41062=CARTESIAN_POINT ( 'NONE',  ( 47.33349330513379982, 4.000000000000003553, 0.000000000000000000 ) ) ;
#41096=B_SPLINE_CURVE_WITH_KNOTS ( 'NONE', 3,
 ( #26319, #75336, #92059, #58092, #48922 ),
 .UNSPECIFIED., .F., .F.,
 ( 4, 1, 4 ),
 ( 0.000000000000000000, 0.003752776749732563560, 0.007505553499465127121 ),
 .UNSPECIFIED. ) ;
#41136=AXIS2_PLACEMENT_3D ( 'NONE', #28974, #13246, #55297 ) ;
#41138=EDGE_LOOP ( 'NONE', ( #86473, #88122, #94185, #14861, #14318 ) ) ;
#41149=ADVANCED_FACE ( 'NONE', ( #96789 ), #71425, .T. ) ;
#41168=CARTESIAN_POINT ( 'NONE',  ( 0.000000000000000000, 0.000000000000000000, 0.000000000000000000 ) ) ;
#41185=ORIENTED_EDGE ( 'NONE', *, *, #48459, .F. ) ;
#41187=EDGE_LOOP ( 'NONE', ( #23862, #61589, #105988, #86536, #106087 ) ) ;
#41192=ORIENTED_EDGE ( 'NONE', *, *, #60152, .F. ) ;
#41220=ORIENTED_EDGE ( 'NONE', *, *, #16211, .F. ) ;
#41223=EDGE_LOOP ( 'NONE', ( #16651, #43379, #28928 ) ) ;
#41226=DIRECTION ( 'NONE',  ( -1.000000000000000000, -1.224606353822377258E-16, -0.000000000000000000 ) ) ;
#41240=DIRECTION ( 'NONE',  ( -1.000000000000000000, -1.224606353822377258E-16, -0.000000000000000000 ) ) ;
#41245=DIRECTION ( 'NONE',  ( 0.000000000000000000, -1.000000000000000000, 0.000000000000000000 ) ) ;
#41251=EDGE_LOOP ( 'NONE', ( #47683, #49856, #30101, #93779, #67797, #54717 ) ) ;
#41275=DIRECTION ( 'NONE',  ( 0.000000000000000000, 0.000000000000000000, 1.000000000000000000 ) ) ;
#41278=CARTESIAN_POINT ( 'NONE',  ( 14.34999999999999787, 1.533819458162526451E-15, 0.000000000000000000 ) ) ;
#41280=ORIENTED_EDGE ( 'NONE', *, *, #106484, .T. ) ;
#41284=AXIS2_PLACEMENT_3D ( 'NONE', #27474, #28003, #77579 ) ;
#41293=AXIS2_PLACEMENT_3D ( 'NONE', #63938, #38600, #37562 ) ;
#41359=ORIENTED_EDGE ( 'NONE', *, *, #7536, .F. ) ;
#41382=ORIENTED_EDGE ( 'NONE', *, *, #86266, .F. ) ;
#41387=CARTESIAN_POINT ( 'NONE',  ( 38.09999999999999432, -3.309499999999999886, 4.475777889183790779E-16 ) ) ;
#41393=DIRECTION ( 'NONE',  ( 0.000000000000000000, -1.000000000000000000, 0.000000000000000000 ) ) ;
#41403=DIRECTION ( 'NONE',  ( -1.000000000000000000, -0.000000000000000000, -0.000000000000000000 ) ) ;
#41412=ADVANCED_FACE ( 'NONE', ( #64169 ), #25668, .T. ) ;
#41431=CARTESIAN_POINT ( 'NONE',  ( 0.000000000000000000, 0.000000000000000000, 0.000000000000000000 ) ) ;
#41437=ORIENTED_EDGE ( 'NONE', *, *, #3115, .T. ) ;
#41439=CARTESIAN_POINT ( 'NONE',  ( 36.08349330513379982, 4.898587196589405926E-16, -4.000000000000001776 ) ) ;
#41451=ORIENTED_EDGE ( 'NONE', *, *, #97181, .F. ) ;
#41468=EDGE_CURVE ( 'NONE', #106610, #80639, #90026, .T. ) ;
#41491=ORIENTED_EDGE ( 'NONE', *, *, #93302, .T. ) ;
#41492=ORIENTED_EDGE ( 'NONE', *, *, #36770, .F. ) ;
#41533=FACE_OUTER_BOUND ( 'NONE', #75716, .T. ) ;
#41539=EDGE_CURVE ( 'NONE', #44354, #75817, #56544, .T. ) ;
#41543=AXIS2_PLACEMENT_3D ( 'NONE', #96547, #94436, #22680 ) ;
#41558=ADVANCED_FACE ( 'NONE', ( #79673 ), #795, .T. ) ;
#41575=DIRECTION ( 'NONE',  ( 0.000000000000000000, -1.000000000000000000, 0.000000000000000000 ) ) ;
#41584=ORIENTED_EDGE ( 'NONE', *, *, #66113, .T. ) ;
#41592=FACE_OUTER_BOUND ( 'NONE', #81239, .T. ) ;
#41593=DIRECTION ( 'NONE',  ( -1.000000000000000000, -1.224606353822377258E-16, -0.000000000000000000 ) ) ;
#41594=CARTESIAN_POINT ( 'NONE',  ( 46.08349330513379982, 1.593028355512270567E-15, 0.000000000000000000 ) ) ;
#41597=AXIS2_PLACEMENT_3D ( 'NONE', #11197, #61386, #101304 ) ;
#41675=EDGE_CURVE ( 'NONE', #76319, #11128, #64529, .T. ) ;
#41761=EDGE_LOOP ( 'NONE', ( #81363, #87672, #39431, #83914, #62911 ) ) ;
#41793=ORIENTED_EDGE ( 'NONE', *, *, #101815, .F. ) ;
#41811=DIRECTION ( 'NONE',  ( -1.000000000000000000, -1.224606353822377258E-16, -0.000000000000000000 ) ) ;
#41815=EDGE_CURVE ( 'NONE', #66259, #40330, #38750, .T. ) ;
#41816=ORIENTED_EDGE ( 'NONE', *, *, #14219, .T. ) ;
#41821=EDGE_CURVE ( 'NONE', #103934, #31692, #70935, .T. ) ;
#41841=CARTESIAN_POINT ( 'NONE',  ( 33.09999999999999432, -3.309499999999999886, 0.000000000000000000 ) ) ;
#41865=ADVANCED_FACE ( 'NONE', ( #72518 ), #54183, .T. ) ;
#41877=ORIENTED_EDGE ( 'NONE', *, *, #7059, .T. ) ;
#41882=CARTESIAN_POINT ( 'NONE',  ( 27.61650669486618881, -3.851859888774471706E-31, 4.000000000000000888 ) ) ;
#41892=DIRECTION ( 'NONE',  ( 0.000000000000000000, -1.000000000000000000, 0.000000000000000000 ) ) ;
#41899=ORIENTED_EDGE ( 'NONE', *, *, #45110, .F. ) ;
#41913=FACE_OUTER_BOUND ( 'NONE', #85127, .T. ) ;
#41917=CIRCLE ( 'NONE', #59183, 4.000000000000000888 ) ;
#41919=CARTESIAN_POINT ( 'NONE',  ( 46.84999999999999432, -3.309499999999999886, 4.475777889183790779E-16 ) ) ;
#41936=CARTESIAN_POINT ( 'NONE',  ( 0.000000000000000000, 0.000000000000000000, 0.000000000000000000 ) ) ;
#41953=CARTESIAN_POINT ( 'NONE',  ( 22.33349330513380337, 1.593028355512270567E-15, 0.000000000000000000 ) ) ;
#41969=EDGE_LOOP ( 'NONE', ( #45348, #5376, #11254, #9640, #52775 ) ) ;
#41988=ORIENTED_EDGE ( 'NONE', *, *, #64692, .F. ) ;
#42011=DIRECTION ( 'NONE',  ( 0.000000000000000000, -1.000000000000000000, 0.000000000000000000 ) ) ;
#42021=VECTOR ( 'NONE', #89108, 1000.000000000000000 ) ;
#42030=ORIENTED_EDGE ( 'NONE', *, *, #29658, .F. ) ;
#42047=CARTESIAN_POINT ( 'NONE',  ( 12.33349330513380337, 1.593028355512270567E-15, 0.000000000000000000 ) ) ;
#42060=DIRECTION ( 'NONE',  ( 0.000000000000000000, -1.000000000000000000, 0.000000000000000000 ) ) ;
#42140=CIRCLE ( 'NONE', #102440, 4.000000000000000888 ) ;
#42150=ADVANCED_FACE ( 'NONE', ( #36366 ), #58213, .T. ) ;
#42163=CARTESIAN_POINT ( 'NONE',  ( 8.866506694866188809, 1.474610560812782335E-15, 0.000000000000000000 ) ) ;
#42166=DIRECTION ( 'NONE',  ( 0.000000000000000000, 1.000000000000000000, 0.000000000000000000 ) ) ;
#42197=DIRECTION ( 'NONE',  ( -0.5735764363510497121, 0.8191520442889892450, 1.003171929053521665E-16 ) ) ;
#42213=ORIENTED_EDGE ( 'NONE', *, *, #16066, .T. ) ;
#42221=ADVANCED_FACE ( 'NONE', ( #39516 ), #46529, .F. ) ;
#42224=CARTESIAN_POINT ( 'NONE',  ( 38.86650669486618881, -3.851859888774471706E-31, 4.000000000000000888 ) ) ;
#42234=DIRECTION ( 'NONE',  ( -1.000000000000000000, -1.224606353822377258E-16, -0.000000000000000000 ) ) ;
#42264=CIRCLE ( 'NONE', #59469, 4.000000000000001776 ) ;
#42310=ORIENTED_EDGE ( 'NONE', *, *, #65307, .F. ) ;
#42326=CARTESIAN_POINT ( 'NONE',  ( 0.000000000000000000, 0.000000000000000000, 4.000000000000000000 ) ) ;
#42336=AXIS2_PLACEMENT_3D ( 'NONE', #55379, #47291, #31157 ) ;
#42344=ORIENTED_EDGE ( 'NONE', *, *, #3236, .F. ) ;
#42368=CARTESIAN_POINT ( 'NONE',  ( 0.000000000000000000, 0.000000000000000000, 0.000000000000000000 ) ) ;
#42372=ORIENTED_EDGE ( 'NONE', *, *, #15723, .T. ) ;
#42417=CARTESIAN_POINT ( 'NONE',  ( 35.11650669486618170, 1.474610560812782335E-15, 0.000000000000000000 ) ) ;
#42440=ORIENTED_EDGE ( 'NONE', *, *, #89056, .F. ) ;
#42443=CARTESIAN_POINT ( 'NONE',  ( 11.08349330513380160, 4.898587196589405926E-16, -4.000000000000001776 ) ) ;
#42470=CARTESIAN_POINT ( 'NONE',  ( 0.000000000000000000, 5.629165124598848102, 3.250000000000005329 ) ) ;
#42491=VERTEX_POINT ( 'NONE', #85827 ) ;
#42497=ADVANCED_FACE ( 'NONE', ( #92280 ), #73762, .T. ) ;
#42500=ORIENTED_EDGE ( 'NONE', *, *, #70472, .F. ) ;
#42506=EDGE_LOOP ( 'NONE', ( #31836, #20981, #96275, #101572, #91171 ) ) ;
#42516=ORIENTED_EDGE ( 'NONE', *, *, #13823, .T. ) ;
#42520=ORIENTED_EDGE ( 'NONE', *, *, #64129, .F. ) ;
#42533=CARTESIAN_POINT ( 'NONE',  ( 15.11650669486618881, -3.851859888774471706E-31, 4.000000000000000888 ) ) ;
#42553=EDGE_CURVE ( 'NONE', #87110, #55862, #20487, .T. ) ;
#42587=VERTEX_POINT ( 'NONE', #79294 ) ;
#42609=CARTESIAN_POINT ( 'NONE',  ( 31.08349330513380337, 4.000000000000003553, 0.000000000000000000 ) ) ;
#42636=LINE ( 'NONE', #58839, #64135 ) ;
#42667=CARTESIAN_POINT ( 'NONE',  ( 5.947762761376476526, 4.378239541354659536, -5.416666666666666075 ) ) ;
#42688=CARTESIAN_POINT ( 'NONE',  ( 0.000000000000000000, 0.000000000000000000, 4.000000000000000000 ) ) ;
#42694=CIRCLE ( 'NONE', #58238, 4.000000000000000888 ) ;
#42706=B_SPLINE_CURVE_WITH_KNOTS ( 'NONE', 3,
 ( #52898, #97451, #73166, #6856, #45869, #106071 ),
 .UNSPECIFIED., .F., .F.,
 ( 4, 2, 4 ),
 ( 2.380733003136001779E-07, 0.001898835937927382872, 0.003797433802554452380 ),
 .UNSPECIFIED. ) ;
#42725=DIRECTION ( 'NONE',  ( 0.000000000000000000, -1.000000000000000000, 0.000000000000000000 ) ) ;
#42750=ORIENTED_EDGE ( 'NONE', *, *, #53839, .T. ) ;
#42756=AXIS2_PLACEMENT_3D ( 'NONE', #5491, #105762, #6530 ) ;
#42781=AXIS2_PLACEMENT_3D ( 'NONE', #39625, #47155, #87113 ) ;
#42782=LINE ( 'NONE', #61107, #18267 ) ;
#42795=ORIENTED_EDGE ( 'NONE', *, *, #67403, .T. ) ;
#42812=ORIENTED_EDGE ( 'NONE', *, *, #94239, .T. ) ;
#42873=CARTESIAN_POINT ( 'NONE',  ( 13.86650669486618881, 1.474610560812782335E-15, 0.000000000000000000 ) ) ;
#42895=EDGE_CURVE ( 'NONE', #95250, #55983, #64467, .T. ) ;
#42915=AXIS2_PLACEMENT_3D ( 'NONE', #34820, #50410, #83322 ) ;
#42917=CARTESIAN_POINT ( 'NONE',  ( 8.099999999999999645, 0.000000000000000000, 0.000000000000000000 ) ) ;
#42949=CYLINDRICAL_SURFACE ( 'NONE', #4228, 4.000000000000000000 ) ;
#42965=EDGE_LOOP ( 'NONE', ( #92341, #18318, #68411, #37926, #14712, #104019 ) ) ;
#42969=CARTESIAN_POINT ( 'NONE',  ( 15.11650669486618881, 1.474610560812782335E-15, 0.000000000000000000 ) ) ;
#43000=EDGE_LOOP ( 'NONE', ( #84300, #98906, #35090, #68861, #76006, #93486 ) ) ;
#43002=DIRECTION ( 'NONE',  ( -1.000000000000000000, -0.000000000000000000, -0.000000000000000000 ) ) ;
#43010=CARTESIAN_POINT ( 'NONE',  ( 31.36650669486618881, -3.999999999999998224, 0.000000000000000000 ) ) ;
#43018=CARTESIAN_POINT ( 'NONE',  ( 33.09999999999999432, 1.533819458162526451E-15, 0.000000000000000000 ) ) ;
#43036=ORIENTED_EDGE ( 'NONE', *, *, #102153, .F. ) ;
#43047=DIRECTION ( 'NONE',  ( -1.000000000000000000, -1.224606353822377258E-16, -0.000000000000000000 ) ) ;
#43085=ORIENTED_EDGE ( 'NONE', *, *, #28750, .F. ) ;
#43089=DIRECTION ( 'NONE',  ( -1.000000000000000000, -1.224606353822377258E-16, -0.000000000000000000 ) ) ;
#43096=EDGE_LOOP ( 'NONE', ( #22555, #45144, #19367, #52430, #2501, #96829 ) ) ;
#43124=DIRECTION ( 'NONE',  ( -1.000000000000000000, -1.224606353822377258E-16, -0.000000000000000000 ) ) ;
#43128=CIRCLE ( 'NONE', #53450, 4.000000000000000888 ) ;
#43166=VERTEX_POINT ( 'NONE', #100583 ) ;
#43173=CARTESIAN_POINT ( 'NONE',  ( 24.34999999999999787, 1.533819458162526451E-15, 0.000000000000000000 ) ) ;
#43174=LINE ( 'NONE', #67976, #73493 ) ;
#43195=DIRECTION ( 'NONE',  ( -1.000000000000000000, -1.224606353822377258E-16, -0.000000000000000000 ) ) ;
#43203=ORIENTED_EDGE ( 'NONE', *, *, #38615, .T. ) ;
#43209=ORIENTED_EDGE ( 'NONE', *, *, #57003, .F. ) ;
#43222=EDGE_CURVE ( 'NONE', #68944, #54096, #67010, .T. ) ;
#43240=CARTESIAN_POINT ( 'NONE',  ( 33.58349330513379982, 1.593028355512270567E-15, 0.000000000000000000 ) ) ;
#43242=DIRECTION ( 'NONE',  ( 0.000000000000000000, 0.000000000000000000, -1.000000000000000000 ) ) ;
#43253=DIRECTION ( 'NONE',  ( -1.000000000000000000, -0.000000000000000000, -0.000000000000000000 ) ) ;
#43257=EDGE_CURVE ( 'NONE', #77600, #65506, #36021, .T. ) ;
#43278=LINE ( 'NONE', #69683, #24164 ) ;
#43285=CARTESIAN_POINT ( 'NONE',  ( 0.000000000000000000, 0.000000000000000000, 4.000000000000000000 ) ) ;
#43289=CARTESIAN_POINT ( 'NONE',  ( 0.000000000000000000, 4.898587196589412829E-16, -4.000000000000000000 ) ) ;
#43292=AXIS2_PLACEMENT_3D ( 'NONE', #53384, #11302, #86301 ) ;
#43306=EDGE_CURVE ( 'NONE', #44463, #92310, #39592, .T. ) ;
#43379=ORIENTED_EDGE ( 'NONE', *, *, #71879, .T. ) ;
#43396=VERTEX_POINT ( 'NONE', #8785 ) ;
#43431=EDGE_CURVE ( 'NONE', #87415, #48447, #56257, .T. ) ;
#43441=VERTEX_POINT ( 'NONE', #32570 ) ;
#43469=EDGE_LOOP ( 'NONE', ( #29750, #61514, #31567, #59942, #60183, #73799 ) ) ;
#43480=AXIS2_PLACEMENT_3D ( 'NONE', #45502, #4492, #77321 ) ;
#43485=CARTESIAN_POINT ( 'NONE',  ( 20.11650669486618881, 1.474610560812782335E-15, 0.000000000000000000 ) ) ;
#43494=CARTESIAN_POINT ( 'NONE',  ( 6.169949891408088583, 6.308465495020067593, 2.073417244832475692 ) ) ;
#43581=ADVANCED_FACE ( 'NONE', ( #59487 ), #80529, .T. ) ;
#43591=CARTESIAN_POINT ( 'NONE',  ( 0.000000000000000000, 0.000000000000000000, -6.499999999999999112 ) ) ;
#43620=ORIENTED_EDGE ( 'NONE', *, *, #25828, .F. ) ;
#43637=CARTESIAN_POINT ( 'NONE',  ( 6.585304040558097149, -4.021874164301456389, 6.500000000000001776 ) ) ;
#43649=LINE ( 'NONE', #84113, #24935 ) ;
#43691=DIRECTION ( 'NONE',  ( -1.000000000000000000, -1.224606353822377258E-16, -0.000000000000000000 ) ) ;
#43707=ORIENTED_EDGE ( 'NONE', *, *, #21015, .T. ) ;
#43711=EDGE_CURVE ( 'NONE', #74596, #52893, #58127, .T. ) ;
#43715=FACE_OUTER_BOUND ( 'NONE', #44048, .T. ) ;
#43720=CYLINDRICAL_SURFACE ( 'NONE', #2831, 4.000000000000000000 ) ;
#43728=ORIENTED_EDGE ( 'NONE', *, *, #43222, .T. ) ;
#43736=ADVANCED_FACE ( 'NONE', ( #94516 ), #92623, .T. ) ;
#43765=CARTESIAN_POINT ( 'NONE',  ( 6.692588830498424457, -3.932766476276026157, 6.892929031562514908 ) ) ;
#43785=ORIENTED_EDGE ( 'NONE', *, *, #4671, .T. ) ;
#43816=DIRECTION ( 'NONE',  ( -1.000000000000000000, -1.224606353822377258E-16, -0.000000000000000000 ) ) ;
#43870=VECTOR ( 'NONE', #48375, 1000.000000000000000 ) ;
#43875=CARTESIAN_POINT ( 'NONE',  ( 23.86650669486618881, -3.999999999999998224, 0.000000000000000000 ) ) ;
#43888=DIRECTION ( 'NONE',  ( -1.000000000000000000, -1.224606353822377258E-16, -0.000000000000000000 ) ) ;
#43903=ORIENTED_EDGE ( 'NONE', *, *, #863, .F. ) ;
#43905=CARTESIAN_POINT ( 'NONE',  ( 5.819846122303833802, -4.937269551422769354, -4.448398286272978730 ) ) ;
#43935=CARTESIAN_POINT ( 'NONE',  ( 13.58349330513380160, 4.898587196589405926E-16, -4.000000000000001776 ) ) ;
#43939=DIRECTION ( 'NONE',  ( 0.5735764363510466035, -0.8191520442889914655, 1.003171929053524500E-16 ) ) ;
#43940=FACE_OUTER_BOUND ( 'NONE', #101336, .T. ) ;
#43952=CIRCLE ( 'NONE', #45718, 4.000000000000000888 ) ;
#43953=ORIENTED_EDGE ( 'NONE', *, *, #87105, .F. ) ;
#43960=DIRECTION ( 'NONE',  ( -1.000000000000000000, -1.224606353822377258E-16, -0.000000000000000000 ) ) ;
#43962=CIRCLE ( 'NONE', #76673, 4.000000000000000888 ) ;
#43964=CIRCLE ( 'NONE', #104242, 4.000000000000001776 ) ;
#43971=VECTOR ( 'NONE', #44336, 1000.000000000000000 ) ;
#44026=AXIS2_PLACEMENT_3D ( 'NONE', #87606, #46598, #5607 ) ;
#44040=VECTOR ( 'NONE', #3965, 1000.000000000000114 ) ;
#44043=DIRECTION ( 'NONE',  ( -1.000000000000000000, -0.000000000000000000, -0.000000000000000000 ) ) ;
#44048=EDGE_LOOP ( 'NONE', ( #97972, #96168, #23152, #92062, #5308 ) ) ;
#44053=VECTOR ( 'NONE', #9080, 1000.000000000000114 ) ;
#44065=B_SPLINE_CURVE_WITH_KNOTS ( 'NONE', 3,
 ( #38358, #88483, #29230, #21132, #21646, #87952 ),
 .UNSPECIFIED., .F., .F.,
 ( 4, 2, 4 ),
 ( 2.380733003144885302E-07, 0.001898835937927388943, 0.003797433802554463656 ),
 .UNSPECIFIED. ) ;
#44108=CARTESIAN_POINT ( 'NONE',  ( 6.443810749341193578, -2.669419465171496419, -6.839891222013547711 ) ) ;
#44128=AXIS2_PLACEMENT_3D ( 'NONE', #70091, #62025, #102994 ) ;
#44131=CARTESIAN_POINT ( 'NONE',  ( 25.11650669486618881, 1.474610560812782335E-15, 0.000000000000000000 ) ) ;
#44135=DIRECTION ( 'NONE',  ( 0.000000000000000000, -1.000000000000000000, 0.000000000000000000 ) ) ;
#44143=ORIENTED_EDGE ( 'NONE', *, *, #51641, .F. ) ;
#44144=CARTESIAN_POINT ( 'NONE',  ( 9.833493305133801599, 1.593028355512270567E-15, 0.000000000000000000 ) ) ;
#44147=DIRECTION ( 'NONE',  ( 0.000000000000000000, -1.000000000000000000, 0.000000000000000000 ) ) ;
#44181=DIRECTION ( 'NONE',  ( 0.3420201433256622736, 1.150791560227853228E-16, 0.9396926207859106484 ) ) ;
#44189=VERTEX_POINT ( 'NONE', #97525 ) ;
#44192=DIRECTION ( 'NONE',  ( 0.000000000000000000, -1.000000000000000000, 0.000000000000000000 ) ) ;
#44228=DIRECTION ( 'NONE',  ( 0.000000000000000000, -1.000000000000000000, 0.000000000000000000 ) ) ;
#44230=CARTESIAN_POINT ( 'NONE',  ( 39.83349330513380693, 1.593028355512270567E-15, 0.000000000000000000 ) ) ;
#44236=DIRECTION ( 'NONE',  ( 0.000000000000000000, -1.000000000000000000, 0.000000000000000000 ) ) ;
#44245=CONICAL_SURFACE ( 'NONE', #94136, 3.309500000000001663, 0.9599310885968770357 ) ;
#44254=DIRECTION ( 'NONE',  ( -1.000000000000000000, -0.000000000000000000, -0.000000000000000000 ) ) ;
#44258=VERTEX_POINT ( 'NONE', #10128 ) ;
#44287=DIRECTION ( 'NONE',  ( 0.000000000000000000, 1.000000000000000000, 0.000000000000000000 ) ) ;
#44294=EDGE_CURVE ( 'NONE', #80498, #7688, #20397, .T. ) ;
#44298=DIRECTION ( 'NONE',  ( 0.000000000000000000, -1.000000000000000000, 0.000000000000000000 ) ) ;
#44325=ORIENTED_EDGE ( 'NONE', *, *, #2893, .T. ) ;
#44327=EDGE_CURVE ( 'NONE', #97567, #98741, #100201, .T. ) ;
#44330=LINE ( 'NONE', #77224, #81550 ) ;
#44336=DIRECTION ( 'NONE',  ( -0.5735764363510494901, -0.8191520442889894671, 0.000000000000000000 ) ) ;
#44339=ORIENTED_EDGE ( 'NONE', *, *, #78201, .T. ) ;
#44342=CARTESIAN_POINT ( 'NONE',  ( 0.000000000000000000, 0.000000000000000000, 0.000000000000000000 ) ) ;
#44354=VERTEX_POINT ( 'NONE', #34974 ) ;
#44373=AXIS2_PLACEMENT_3D ( 'NONE', #76496, #18843, #44147 ) ;
#44378=ORIENTED_EDGE ( 'NONE', *, *, #65307, .T. ) ;
#44415=DIRECTION ( 'NONE',  ( 0.000000000000000000, 0.000000000000000000, -1.000000000000000000 ) ) ;
#44424=EDGE_CURVE ( 'NONE', #97178, #19223, #61712, .T. ) ;
#44427=AXIS2_PLACEMENT_3D ( 'NONE', #66245, #14620, #58148 ) ;
#44438=CARTESIAN_POINT ( 'NONE',  ( 13.58349330513380160, 1.593028355512270567E-15, 0.000000000000000000 ) ) ;
#44445=VERTEX_POINT ( 'NONE', #44645 ) ;
#44448=LINE ( 'NONE', #21789, #9171 ) ;
#44463=VERTEX_POINT ( 'NONE', #78572 ) ;
#44484=CIRCLE ( 'NONE', #72043, 4.000000000000001776 ) ;
#44486=CARTESIAN_POINT ( 'NONE',  ( 19.83349330513379982, 4.898587196589405926E-16, -4.000000000000001776 ) ) ;
#44488=EDGE_CURVE ( 'NONE', #57881, #92046, #16955, .T. ) ;
#44526=DIRECTION ( 'NONE',  ( 0.000000000000000000, -1.000000000000000000, 0.000000000000000000 ) ) ;
#44567=CARTESIAN_POINT ( 'NONE',  ( 6.162888688655350222, -7.505553499465148271, 0.000000000000000000 ) ) ;
#44569=DIRECTION ( 'NONE',  ( -1.000000000000000000, -0.000000000000000000, -0.000000000000000000 ) ) ;
#44578=EDGE_LOOP ( 'NONE', ( #23510, #56690, #74718, #23056, #6265 ) ) ;
#44588=CARTESIAN_POINT ( 'NONE',  ( 0.000000000000000000, 0.000000000000000000, 0.000000000000000000 ) ) ;
#44597=VECTOR ( 'NONE', #92209, 1000.000000000000114 ) ;
#44598=DIRECTION ( 'NONE',  ( 0.5735764363510462704, 0.8191520442889915765, 0.000000000000000000 ) ) ;
#44629=CYLINDRICAL_SURFACE ( 'NONE', #45166, 4.000000000000000000 ) ;
#44645=CARTESIAN_POINT ( 'NONE',  ( 28.58349330513380337, 4.898587196589405926E-16, -4.000000000000001776 ) ) ;
#44652=CARTESIAN_POINT ( 'NONE',  ( 5.974109059515367193, -2.735160444454405759, -6.499999999999999112 ) ) ;
#44661=CIRCLE ( 'NONE', #99763, 4.000000000000000888 ) ;
#44663=CIRCLE ( 'NONE', #65352, 4.000000000000000888 ) ;
#44666=ORIENTED_EDGE ( 'NONE', *, *, #94857, .F. ) ;
#44673=CARTESIAN_POINT ( 'NONE',  ( 0.2595206531159274799, 2.531175536751827604, -6.499999999999999112 ) ) ;
#44695=EDGE_LOOP ( 'NONE', ( #3080, #13069, #95434, #80648, #33074 ) ) ;
#44719=CARTESIAN_POINT ( 'NONE',  ( 6.291779652043092419, -1.386462189980837367, 6.829130021847430676 ) ) ;
#44736=AXIS2_PLACEMENT_3D ( 'NONE', #67691, #90903, #25676 ) ;
#44738=AXIS2_PLACEMENT_3D ( 'NONE', #42047, #92181, #67920 ) ;
#44749=CARTESIAN_POINT ( 'NONE',  ( 10.11650669486618881, -3.851859888774471706E-31, 4.000000000000000888 ) ) ;
#44763=AXIS2_PLACEMENT_3D ( 'NONE', #46917, #47965, #54996 ) ;
#44764=ORIENTED_EDGE ( 'NONE', *, *, #59351, .T. ) ;
#44769=CARTESIAN_POINT ( 'NONE',  ( 38.09999999999999432, 1.533819458162526451E-15, 0.000000000000000000 ) ) ;
#44771=VECTOR ( 'NONE', #83406, 1000.000000000000000 ) ;
#44791=CIRCLE ( 'NONE', #37969, 3.309500000000001663 ) ;
#44793=VERTEX_POINT ( 'NONE', #75531 ) ;
#44827=CARTESIAN_POINT ( 'NONE',  ( 21.08349330513380337, 1.593028355512270567E-15, 0.000000000000000000 ) ) ;
#44866=LINE ( 'NONE', #13528, #70785 ) ;
#44883=CARTESIAN_POINT ( 'NONE',  ( 0.000000000000000000, 4.898587196589412829E-16, -4.000000000000000000 ) ) ;
#44925=CARTESIAN_POINT ( 'NONE',  ( 8.099999999999999645, 0.000000000000000000, 8.400000000000000355 ) ) ;
#44939=VERTEX_POINT ( 'NONE', #20561 ) ;
#44969=CONICAL_SURFACE ( 'NONE', #105231, 3.309500000000001663, 0.9599310885968770357 ) ;
#44981=CARTESIAN_POINT ( 'NONE',  ( 6.162888688655350222, -7.505553499465148271, 0.000000000000000000 ) ) ;
#44991=CARTESIAN_POINT ( 'NONE',  ( 38.09999999999999432, 1.533819458162526451E-15, 0.000000000000000000 ) ) ;
#45000=ORIENTED_EDGE ( 'NONE', *, *, #54982, .F. ) ;
#45015=EDGE_CURVE ( 'NONE', #104331, #478, #13616, .T. ) ;
#45020=CARTESIAN_POINT ( 'NONE',  ( 17.61650669486618881, 4.000000000000003553, 4.898587196589414801E-16 ) ) ;
#45023=CARTESIAN_POINT ( 'NONE',  ( 43.10000000000000142, -3.309499999999999886, 0.000000000000000000 ) ) ;
#45039=VECTOR ( 'NONE', #36226, 1000.000000000000000 ) ;
#45041=EDGE_CURVE ( 'NONE', #93508, #673, #65290, .T. ) ;
#45050=ORIENTED_EDGE ( 'NONE', *, *, #28962, .T. ) ;
#45056=CONICAL_SURFACE ( 'NONE', #15685, 4.000000000000001776, 0.9599310885968808105 ) ;
#45075=CARTESIAN_POINT ( 'NONE',  ( 28.58349330513380337, 1.593028355512270567E-15, 0.000000000000000000 ) ) ;
#45081=ORIENTED_EDGE ( 'NONE', *, *, #25237, .F. ) ;
#45110=EDGE_CURVE ( 'NONE', #32012, #76213, #102549, .T. ) ;
#45122=CARTESIAN_POINT ( 'NONE',  ( 21.08349330513380337, -4.000000000000000888, 4.898587196589416773E-16 ) ) ;
#45136=ORIENTED_EDGE ( 'NONE', *, *, #25828, .T. ) ;
#45144=ORIENTED_EDGE ( 'NONE', *, *, #80694, .T. ) ;
#45147=EDGE_CURVE ( 'NONE', #70292, #57113, #22288, .T. ) ;
#45149=CARTESIAN_POINT ( 'NONE',  ( 17.33349330513380337, 1.593028355512270567E-15, 0.000000000000000000 ) ) ;
#45155=DIRECTION ( 'NONE',  ( 0.000000000000000000, -1.000000000000000000, 0.000000000000000000 ) ) ;
#45166=AXIS2_PLACEMENT_3D ( 'NONE', #3630, #12231, #27950 ) ;
#45189=CIRCLE ( 'NONE', #43480, 4.000000000000000888 ) ;
#45253=ORIENTED_EDGE ( 'NONE', *, *, #59985, .T. ) ;
#45262=DIRECTION ( 'NONE',  ( 0.000000000000000000, -1.000000000000000000, 0.000000000000000000 ) ) ;
#45285=ADVANCED_FACE ( 'NONE', ( #46761 ), #61915, .T. ) ;
#45301=EDGE_CURVE ( 'NONE', #55816, #72001, #69458, .T. ) ;
#45302=VERTEX_POINT ( 'NONE', #87767 ) ;
#45306=VERTEX_POINT ( 'NONE', #28490 ) ;
#45348=ORIENTED_EDGE ( 'NONE', *, *, #29529, .F. ) ;
#45387=CARTESIAN_POINT ( 'NONE',  ( 26.84999999999999787, 1.533819458162526451E-15, 0.000000000000000000 ) ) ;
#45397=EDGE_LOOP ( 'NONE', ( #95330, #33704, #96627, #5518, #15328, #59928 ) ) ;
#45404=AXIS2_PLACEMENT_3D ( 'NONE', #6357, #39298, #80789 ) ;
#45417=DIRECTION ( 'NONE',  ( -1.000000000000000000, -1.224606353822377258E-16, -0.000000000000000000 ) ) ;
#45426=LINE ( 'NONE', #19594, #31945 ) ;
#45458=EDGE_CURVE ( 'NONE', #43396, #77668, #47803, .T. ) ;
#45468=VERTEX_POINT ( 'NONE', #89357 ) ;
#45473=VERTEX_POINT ( 'NONE', #57487 ) ;
#45499=CARTESIAN_POINT ( 'NONE',  ( 38.86650669486618881, 1.474610560812782335E-15, 0.000000000000000000 ) ) ;
#45502=CARTESIAN_POINT ( 'NONE',  ( 25.11650669486618881, 1.474610560812782335E-15, 0.000000000000000000 ) ) ;
#45510=VERTEX_POINT ( 'NONE', #74737 ) ;
#45521=DIRECTION ( 'NONE',  ( 0.000000000000000000, -1.000000000000000000, 0.000000000000000000 ) ) ;
#45551=CARTESIAN_POINT ( 'NONE',  ( 0.000000000000000000, 0.000000000000000000, 0.000000000000000000 ) ) ;
#45565=FACE_OUTER_BOUND ( 'NONE', #97844, .T. ) ;
#45589=CARTESIAN_POINT ( 'NONE',  ( 39.83349330513380693, -4.000000000000000000, 4.898587196589415787E-16 ) ) ;
#45595=AXIS2_PLACEMENT_3D ( 'NONE', #53209, #27919, #60782 ) ;
#45601=AXIS2_PLACEMENT_3D ( 'NONE', #23058, #22540, #89374 ) ;
#45604=ORIENTED_EDGE ( 'NONE', *, *, #15815, .T. ) ;
#45640=CARTESIAN_POINT ( 'NONE',  ( 46.36650669486618881, 1.474610560812782335E-15, 0.000000000000000000 ) ) ;
#45654=CARTESIAN_POINT ( 'NONE',  ( 6.683837171061809634, -7.911893696991943337, -3.558927330633863411E-17 ) ) ;
#45666=CIRCLE ( 'NONE', #102472, 4.000000000000001776 ) ;
#45712=ADVANCED_FACE ( 'NONE', ( #10019 ), #67735, .T. ) ;
#45718=AXIS2_PLACEMENT_3D ( 'NONE', #69127, #95000, #51314 ) ;
#45719=DIRECTION ( 'NONE',  ( -0.5735764363510497121, 0.8191520442889892450, 1.003171929053521665E-16 ) ) ;
#45750=VERTEX_POINT ( 'NONE', #76875 ) ;
#45764=CARTESIAN_POINT ( 'NONE',  ( 0.000000000000000000, 0.000000000000000000, 0.000000000000000000 ) ) ;
#45767=DIRECTION ( 'NONE',  ( 0.000000000000000000, -1.000000000000000000, 0.000000000000000000 ) ) ;
#45768=( BOUNDED_SURFACE ( )  B_SPLINE_SURFACE ( 3, 2, ( 
 ( #34398, #879, #25235 ),
 ( #26843, #24697, #99070 ),
 ( #59180, #91021, #67793 ),
 ( #74799, #83435, #17127 ),
 ( #16580, #18196, #33858 ),
 ( #16042, #9007, #99614 ) ),
 .UNSPECIFIED., .F., .F., .F. ) 
 B_SPLINE_SURFACE_WITH_KNOTS ( ( 4, 2, 4 ),
 ( 3, 3 ),
 ( 0.003199762745115997641, 0.007302762474435750203, 0.01140576220375550190 ),
 ( 0.000000000000000000, 1.000000000000000000 ),
 .UNSPECIFIED. ) 
 GEOMETRIC_REPRESENTATION_ITEM ( )  RATIONAL_B_SPLINE_SURFACE ( (
 ( 1.000000000000000000, 0.8047731410850428313, 1.000000000000000000),
 ( 1.000000000000000000, 0.8125552299159717329, 1.000000000000000000),
 ( 1.000000000000000000, 0.8191520442885290576, 1.000000000000000000),
 ( 1.000000000000000000, 0.8191520442894507648, 1.000000000000000000),
 ( 1.000000000000000000, 0.8125552299152797309, 1.000000000000000000),
 ( 1.000000000000000000, 0.8047731410850426093, 1.000000000000000000) ) ) 
 REPRESENTATION_ITEM ( '' )  SURFACE ( )  );
#45796=DIRECTION ( 'NONE',  ( -1.000000000000000000, -0.000000000000000000, -0.000000000000000000 ) ) ;
#45822=DIRECTION ( 'NONE',  ( 0.000000000000000000, -1.000000000000000000, 0.000000000000000000 ) ) ;
#45830=ORIENTED_EDGE ( 'NONE', *, *, #65176, .F. ) ;
#45844=AXIS2_PLACEMENT_3D ( 'NONE', #80461, #63780, #13070 ) ;
#45869=CARTESIAN_POINT ( 'NONE',  ( -4.545178794966575619E-15, 5.948846446048900560, -2.696295709017757503 ) ) ;
#45870=DIRECTION ( 'NONE',  ( -1.000000000000000000, -1.224606353822377258E-16, -0.000000000000000000 ) ) ;
#45917=DIRECTION ( 'NONE',  ( 0.000000000000000000, -1.000000000000000000, 0.000000000000000000 ) ) ;
#45922=CIRCLE ( 'NONE', #87269, 3.309500000000001663 ) ;
#45930=DIRECTION ( 'NONE',  ( -1.000000000000000000, -1.224606353822377258E-16, -0.000000000000000000 ) ) ;
#45943=AXIS2_PLACEMENT_3D ( 'NONE', #12595, #87573, #54638 ) ;
#45952=EDGE_LOOP ( 'NONE', ( #68848, #95264, #10613, #88956, #93136 ) ) ;
#46000=DIRECTION ( 'NONE',  ( 0.000000000000000000, -1.000000000000000000, 0.000000000000000000 ) ) ;
#46048=AXIS2_PLACEMENT_3D ( 'NONE', #93931, #69658, #102550 ) ;
#46049=VECTOR ( 'NONE', #77394, 1000.000000000000000 ) ;
#46061=EDGE_CURVE ( 'NONE', #86885, #98395, #58736, .T. ) ;
#46099=VECTOR ( 'NONE', #95283, 1000.000000000000000 ) ;
#46114=VERTEX_POINT ( 'NONE', #52750 ) ;
#46151=EDGE_LOOP ( 'NONE', ( #73936, #44325, #72372, #41899, #5300 ) ) ;
#46166=TOROIDAL_SURFACE ( 'NONE', #16903, 8.400000000000000355, 0.5999999999999978684 ) ;
#46188=ADVANCED_FACE ( 'NONE', ( #3687 ), #27614, .T. ) ;
#46195=CARTESIAN_POINT ( 'NONE',  ( 33.58349330513379982, -7.703719777548943412E-31, 4.000000000000001776 ) ) ;
#46198=AXIS2_PLACEMENT_3D ( 'NONE', #32059, #23446, #7218 ) ;
#46202=EDGE_CURVE ( 'NONE', #63953, #51686, #25925, .T. ) ;
#46229=CARTESIAN_POINT ( 'NONE',  ( 20.11650669486618881, 1.474610560812782335E-15, 0.000000000000000000 ) ) ;
#46231=CARTESIAN_POINT ( 'NONE',  ( 0.000000000000000000, 4.898587196589412829E-16, -4.000000000000000000 ) ) ;
#46271=AXIS2_PLACEMENT_3D ( 'NONE', #23796, #98692, #89564 ) ;
#46303=AXIS2_PLACEMENT_3D ( 'NONE', #41594, #65868, #9737 ) ;
#46331=CARTESIAN_POINT ( 'NONE',  ( 5.691929483231186637, -5.637851296924623057E-15, -6.499999999999999112 ) ) ;
#46349=DIRECTION ( 'NONE',  ( 0.000000000000000000, -1.000000000000000000, 0.000000000000000000 ) ) ;
#46396=AXIS2_PLACEMENT_3D ( 'NONE', #2818, #92354, #67043 ) ;
#46400=CARTESIAN_POINT ( 'NONE',  ( 37.33349330513379982, 1.593028355512270567E-15, 0.000000000000000000 ) ) ;
#46402=CARTESIAN_POINT ( 'NONE',  ( 6.162888688655344005, -3.752776749732561257, 6.500000000000000000 ) ) ;
#46438=DIRECTION ( 'NONE',  ( 0.000000000000000000, -1.000000000000000000, 0.000000000000000000 ) ) ;
#46446=FACE_OUTER_BOUND ( 'NONE', #13108, .T. ) ;
#46450=DIRECTION ( 'NONE',  ( 0.5735764363510462704, 0.8191520442889915765, 0.000000000000000000 ) ) ;
#46478=CARTESIAN_POINT ( 'NONE',  ( 6.575925811255156184, 3.850887307289501571, 6.669932470447524686 ) ) ;
#46479=ORIENTED_EDGE ( 'NONE', *, *, #66582, .T. ) ;
#46481=VERTEX_POINT ( 'NONE', #67236 ) ;
#46491=EDGE_CURVE ( 'NONE', #27869, #55349, #96558, .T. ) ;
#46501=FACE_OUTER_BOUND ( 'NONE', #60168, .T. ) ;
#46523=CARTESIAN_POINT ( 'NONE',  ( 46.84999999999999432, 1.533819458162526451E-15, 0.000000000000000000 ) ) ;
#46529=PLANE ( 'NONE',  #40974 ) ;
#46554=CYLINDRICAL_SURFACE ( 'NONE', #7741, 4.000000000000000000 ) ;
#46583=ADVANCED_FACE ( 'NONE', ( #37420 ), #17332, .T. ) ;
#46598=DIRECTION ( 'NONE',  ( -1.000000000000000000, -1.224606353822377258E-16, -0.000000000000000000 ) ) ;
#46610=AXIS2_PLACEMENT_3D ( 'NONE', #12463, #4929, #29245 ) ;
#46611=CARTESIAN_POINT ( 'NONE',  ( 7.500000000000001776, 1.028703311283776783E-15, -8.400000000000000355 ) ) ;
#46626=DIRECTION ( 'NONE',  ( 0.000000000000000000, 0.000000000000000000, 1.000000000000000000 ) ) ;
#46671=ORIENTED_EDGE ( 'NONE', *, *, #104431, .F. ) ;
#46691=CARTESIAN_POINT ( 'NONE',  ( 35.59999999999999432, -3.309499999999999886, 0.000000000000000000 ) ) ;
#46706=CARTESIAN_POINT ( 'NONE',  ( 0.000000000000000000, 0.000000000000000000, 4.000000000000000000 ) ) ;
#46719=EDGE_CURVE ( 'NONE', #89196, #29099, #49709, .T. ) ;
#46731=VECTOR ( 'NONE', #96317, 1000.000000000000000 ) ;
#46732=DIRECTION ( 'NONE',  ( -1.000000000000000000, -1.224606353822377258E-16, -0.000000000000000000 ) ) ;
#46761=FACE_OUTER_BOUND ( 'NONE', #82309, .T. ) ;
#46780=EDGE_CURVE ( 'NONE', #55990, #74465, #55187, .T. ) ;
#46783=CARTESIAN_POINT ( 'NONE',  ( 6.281175601187038993, 3.752776749732557704, -6.500000000000006217 ) ) ;
#46788=EDGE_CURVE ( 'NONE', #99943, #49522, #72447, .T. ) ;
#46807=ORIENTED_EDGE ( 'NONE', *, *, #36730, .F. ) ;
#46831=DIRECTION ( 'NONE',  ( -1.000000000000000000, -0.000000000000000000, -0.000000000000000000 ) ) ;
#46843=DIRECTION ( 'NONE',  ( -1.000000000000000000, -1.224606353822377258E-16, -0.000000000000000000 ) ) ;
#46848=CARTESIAN_POINT ( 'NONE',  ( 5.947762761376472973, 2.501851166488370914, -6.500000000000000000 ) ) ;
#46850=ORIENTED_EDGE ( 'NONE', *, *, #92660, .F. ) ;
#46852=CIRCLE ( 'NONE', #48543, 3.309500000000001663 ) ;
#46907=ORIENTED_EDGE ( 'NONE', *, *, #16840, .T. ) ;
#46917=CARTESIAN_POINT ( 'NONE',  ( 11.84999999999999787, 1.533819458162526451E-15, 0.000000000000000000 ) ) ;
#46924=ORIENTED_EDGE ( 'NONE', *, *, #99371, .F. ) ;
#46941=AXIS2_PLACEMENT_3D ( 'NONE', #61715, #21264, #103733 ) ;
#46944=ORIENTED_EDGE ( 'NONE', *, *, #73074, .T. ) ;
#46976=CIRCLE ( 'NONE', #86593, 4.000000000000000888 ) ;
#46996=ORIENTED_EDGE ( 'NONE', *, *, #33260, .T. ) ;
#47000=CARTESIAN_POINT ( 'NONE',  ( 6.449780583204264062, 2.701143306766772945, -6.840188146835520122 ) ) ;
#47018=DIRECTION ( 'NONE',  ( 0.000000000000000000, -1.000000000000000000, 0.000000000000000000 ) ) ;
#47067=VECTOR ( 'NONE', #60648, 1000.000000000000000 ) ;
#47071=MECHANICAL_DESIGN_GEOMETRIC_PRESENTATION_REPRESENTATION('',(#62657),#67803);
#47074=ORIENTED_EDGE ( 'NONE', *, *, #27017, .F. ) ;
#47083=DIRECTION ( 'NONE',  ( -0.5735764363510497121, 0.8191520442889892450, 1.003171929053521665E-16 ) ) ;
#47103=CARTESIAN_POINT ( 'NONE',  ( 10.59999999999999609, 3.309500000000003439, 0.000000000000000000 ) ) ;
#47108=AXIS2_PLACEMENT_3D ( 'NONE', #11299, #93310, #44228 ) ;
#47116=EDGE_LOOP ( 'NONE', ( #573, #81737, #37550, #15567, #82266 ) ) ;
#47129=EDGE_CURVE ( 'NONE', #52930, #6711, #57656, .T. ) ;
#47131=B_SPLINE_CURVE_WITH_KNOTS ( 'NONE', 3,
 ( #13560, #29796, #38924, #46478, #22759, #95562 ),
 .UNSPECIFIED., .F., .F.,
 ( 4, 2, 4 ),
 ( 0.000000000000000000, 0.0003491763592121711088, 0.0006983527184243422175 ),
 .UNSPECIFIED. ) ;
#47149=CARTESIAN_POINT ( 'NONE',  ( 34.83349330513379982, 1.593028355512270567E-15, 0.000000000000000000 ) ) ;
#47152=DIRECTION ( 'NONE',  ( -1.000000000000000000, -1.224606353822377258E-16, -0.000000000000000000 ) ) ;
#47155=DIRECTION ( 'NONE',  ( -1.000000000000000000, -0.000000000000000000, -0.000000000000000000 ) ) ;
#47176=DIRECTION ( 'NONE',  ( 0.000000000000000000, 0.000000000000000000, -1.000000000000000000 ) ) ;
#47191=DIRECTION ( 'NONE',  ( -1.000000000000000000, -0.000000000000000000, -0.000000000000000000 ) ) ;
#47198=DIRECTION ( 'NONE',  ( -0.000000000000000000, 0.000000000000000000, -1.000000000000000000 ) ) ;
#47210=CARTESIAN_POINT ( 'NONE',  ( 6.289572920342628493, -6.243622107253699482, 2.843693100100563420 ) ) ;
#47222=DIRECTION ( 'NONE',  ( 0.000000000000000000, -1.000000000000000000, 0.000000000000000000 ) ) ;
#47224=CIRCLE ( 'NONE', #50588, 4.000000000000001776 ) ;
#47227=ADVANCED_FACE ( 'NONE', ( #94311 ), #84079, .T. ) ;
#47244=LINE ( 'NONE', #23541, #26489 ) ;
#47254=EDGE_CURVE ( 'NONE', #21068, #55816, #82836, .T. ) ;
#47271=ORIENTED_EDGE ( 'NONE', *, *, #11747, .T. ) ;
#47272=DIRECTION ( 'NONE',  ( 0.000000000000000000, -1.000000000000000000, 0.000000000000000000 ) ) ;
#47291=DIRECTION ( 'NONE',  ( -1.000000000000000000, -0.000000000000000000, -0.000000000000000000 ) ) ;
#47293=EDGE_LOOP ( 'NONE', ( #81075, #34223, #53937, #91860, #33195 ) ) ;
#47355=CARTESIAN_POINT ( 'NONE',  ( 15.59999999999999787, 1.533819458162526451E-15, 0.000000000000000000 ) ) ;
#47386=LINE ( 'NONE', #72722, #82129 ) ;
#47400=DIRECTION ( 'NONE',  ( 0.000000000000000000, -1.000000000000000000, 0.000000000000000000 ) ) ;
#47407=AXIS2_PLACEMENT_3D ( 'NONE', #12779, #36054, #37646 ) ;
#47411=ORIENTED_EDGE ( 'NONE', *, *, #60102, .T. ) ;
#47434=ORIENTED_EDGE ( 'NONE', *, *, #61037, .F. ) ;
#47437=ORIENTED_EDGE ( 'NONE', *, *, #35901, .T. ) ;
#47451=VERTEX_POINT ( 'NONE', #102922 ) ;
#47452=ORIENTED_EDGE ( 'NONE', *, *, #71268, .F. ) ;
#47461=CARTESIAN_POINT ( 'NONE',  ( 28.86650669486618881, 1.474610560812782335E-15, 0.000000000000000000 ) ) ;
#47488=DIRECTION ( 'NONE',  ( 0.000000000000000000, -1.000000000000000000, 0.000000000000000000 ) ) ;
#47511=ADVANCED_FACE ( 'NONE', ( #13357 ), #45056, .T. ) ;
#47536=DIRECTION ( 'NONE',  ( -1.000000000000000000, -1.224606353822377258E-16, -0.000000000000000000 ) ) ;
#47565=DIRECTION ( 'NONE',  ( 1.000000000000000000, 1.224606353822377258E-16, 0.000000000000000000 ) ) ;
#47600=DIRECTION ( 'NONE',  ( 0.5735764363510462704, 0.8191520442889915765, 0.000000000000000000 ) ) ;
#47611=CARTESIAN_POINT ( 'NONE',  ( 0.000000000000000000, 0.000000000000000000, 0.000000000000000000 ) ) ;
#47668=ORIENTED_EDGE ( 'NONE', *, *, #50411, .F. ) ;
#47683=ORIENTED_EDGE ( 'NONE', *, *, #97287, .F. ) ;
#47721=DIRECTION ( 'NONE',  ( 0.5735764363510462704, 0.8191520442889915765, 0.000000000000000000 ) ) ;
#47728=VERTEX_POINT ( 'NONE', #13767 ) ;
#47732=DIRECTION ( 'NONE',  ( 0.000000000000000000, -1.000000000000000000, 0.000000000000000000 ) ) ;
#47752=CARTESIAN_POINT ( 'NONE',  ( 0.06682554136338431094, -6.264794173742282091, -2.149058192116895416 ) ) ;
#47772=CIRCLE ( 'NONE', #96002, 4.000000000000001776 ) ;
#47778=AXIS2_PLACEMENT_3D ( 'NONE', #79471, #10614, #26859 ) ;
#47785=EDGE_LOOP ( 'NONE', ( #8841, #50174, #6683, #13315, #93467, #26507 ) ) ;
#47788=VECTOR ( 'NONE', #19226, 1000.000000000000000 ) ;
#47789=DIRECTION ( 'NONE',  ( -1.000000000000000000, -1.224606353822377258E-16, -0.000000000000000000 ) ) ;
#47790=DIRECTION ( 'NONE',  ( 0.000000000000000000, -1.000000000000000000, 0.000000000000000000 ) ) ;
#47803=LINE ( 'NONE', #6283, #75669 ) ;
#47813=CARTESIAN_POINT ( 'NONE',  ( 44.83349330513380693, 4.000000000000003553, 0.000000000000000000 ) ) ;
#47816=EDGE_CURVE ( 'NONE', #103256, #24472, #28965, .T. ) ;
#47823=DIRECTION ( 'NONE',  ( -1.000000000000000000, -1.224606353822377258E-16, -0.000000000000000000 ) ) ;
#47831=CARTESIAN_POINT ( 'NONE',  ( 33.09999999999999432, -3.309499999999999886, 4.475777889183790779E-16 ) ) ;
#47849=EDGE_LOOP ( 'NONE', ( #17311, #60751, #26314, #41382, #68226 ) ) ;
#47878=DIRECTION ( 'NONE',  ( 1.000000000000000000, 0.000000000000000000, 0.000000000000000000 ) ) ;
#47887=EDGE_CURVE ( 'NONE', #72001, #63698, #17493, .T. ) ;
#47900=CARTESIAN_POINT ( 'NONE',  ( 42.61650669486618881, 1.474610560812782335E-15, 0.000000000000000000 ) ) ;
#47918=ORIENTED_EDGE ( 'NONE', *, *, #5247, .F. ) ;
#47922=AXIS2_PLACEMENT_3D ( 'NONE', #66324, #57157, #90070 ) ;
#47932=CARTESIAN_POINT ( 'NONE',  ( 8.099999999999999645, 3.752776749732565253, 6.499999999999997335 ) ) ;
#47965=DIRECTION ( 'NONE',  ( -1.000000000000000000, -1.224606353822377258E-16, -0.000000000000000000 ) ) ;
#48010=AXIS2_PLACEMENT_3D ( 'NONE', #47355, #7951, #106647 ) ;
#48038=ORIENTED_EDGE ( 'NONE', *, *, #52938, .F. ) ;
#48045=ORIENTED_EDGE ( 'NONE', *, *, #66520, .F. ) ;
#48047=DIRECTION ( 'NONE',  ( 0.000000000000000000, -1.000000000000000000, 0.000000000000000000 ) ) ;
#48058=DIRECTION ( 'NONE',  ( 0.000000000000000000, -1.000000000000000000, 0.000000000000000000 ) ) ;
#48085=CONICAL_SURFACE ( 'NONE', #98068, 4.000000000000001776, 0.9599310885968808105 ) ;
#48108=EDGE_LOOP ( 'NONE', ( #96504, #61041, #69355, #29352, #49672 ) ) ;
#48123=AXIS2_PLACEMENT_3D ( 'NONE', #72776, #90035, #16143 ) ;
#48126=DIRECTION ( 'NONE',  ( -0.5735764363510494901, -0.8191520442889894671, 0.000000000000000000 ) ) ;
#48137=FACE_OUTER_BOUND ( 'NONE', #12211, .T. ) ;
#48138=DIRECTION ( 'NONE',  ( -1.000000000000000000, -1.224606353822377258E-16, -0.000000000000000000 ) ) ;
#48156=ORIENTED_EDGE ( 'NONE', *, *, #21466, .T. ) ;
#48160=DIRECTION ( 'NONE',  ( 0.5735764363510462704, 0.8191520442889915765, 0.000000000000000000 ) ) ;
#48174=VERTEX_POINT ( 'NONE', #18049 ) ;
#48230=CARTESIAN_POINT ( 'NONE',  ( 46.08349330513379982, 1.593028355512270567E-15, 0.000000000000000000 ) ) ;
#48231=VERTEX_POINT ( 'NONE', #9927 ) ;
#48251=DIRECTION ( 'NONE',  ( 0.000000000000000000, -1.000000000000000000, 0.000000000000000000 ) ) ;
#48253=DIRECTION ( 'NONE',  ( 0.000000000000000000, -1.000000000000000000, 0.000000000000000000 ) ) ;
#48260=CARTESIAN_POINT ( 'NONE',  ( 0.000000000000000000, 0.000000000000000000, 0.000000000000000000 ) ) ;
#48294=CIRCLE ( 'NONE', #99966, 4.000000000000001776 ) ;
#48314=LINE ( 'NONE', #99526, #53727 ) ;
#48322=DIRECTION ( 'NONE',  ( -1.000000000000000000, -0.000000000000000000, -0.000000000000000000 ) ) ;
#48323=EDGE_CURVE ( 'NONE', #53830, #20373, #53063, .T. ) ;
#48328=DIRECTION ( 'NONE',  ( -1.000000000000000000, -1.224606353822377258E-16, -0.000000000000000000 ) ) ;
#48375=DIRECTION ( 'NONE',  ( -1.000000000000000000, -0.000000000000000000, -0.000000000000000000 ) ) ;
#48377=EDGE_LOOP ( 'NONE', ( #1432, #3943, #5402, #25706, #33465 ) ) ;
#48383=EDGE_CURVE ( 'NONE', #79906, #70259, #78766, .T. ) ;
#48386=DIRECTION ( 'NONE',  ( 1.000000000000000000, 1.224606353822377258E-16, 0.000000000000000000 ) ) ;
#48427=VERTEX_POINT ( 'NONE', #72418 ) ;
#48447=VERTEX_POINT ( 'NONE', #14697 ) ;
#48459=EDGE_CURVE ( 'NONE', #57765, #24986, #39005, .T. ) ;
#48462=CARTESIAN_POINT ( 'NONE',  ( 16.84999999999999787, 1.533819458162526451E-15, 0.000000000000000000 ) ) ;
#48499=DIRECTION ( 'NONE',  ( -1.000000000000000000, -1.224606353822377258E-16, -0.000000000000000000 ) ) ;
#48543=AXIS2_PLACEMENT_3D ( 'NONE', #447, #32889, #80333 ) ;
#48547=DIRECTION ( 'NONE',  ( 0.000000000000000000, -1.000000000000000000, 0.000000000000000000 ) ) ;
#48558=ADVANCED_FACE ( 'NONE', ( #76526 ), #96035, .T. ) ;
#48580=AXIS2_PLACEMENT_3D ( 'NONE', #94595, #35301, #69250 ) ;
#48595=ADVANCED_FACE ( 'NONE', ( #92716 ), #16483, .F. ) ;
#48618=DIRECTION ( 'NONE',  ( 0.000000000000000000, -1.000000000000000000, 0.000000000000000000 ) ) ;
#48660=ORIENTED_EDGE ( 'NONE', *, *, #66248, .T. ) ;
#48669=CYLINDRICAL_SURFACE ( 'NONE', #96047, 4.000000000000000000 ) ;
#48686=AXIS2_PLACEMENT_3D ( 'NONE', #20068, #102532, #94457 ) ;
#48689=EDGE_CURVE ( 'NONE', #103256, #70516, #105050, .T. ) ;
#48724=ORIENTED_EDGE ( 'NONE', *, *, #62915, .T. ) ;
#48725=DIRECTION ( 'NONE',  ( -1.000000000000000000, -1.224606353822377258E-16, -0.000000000000000000 ) ) ;
#48749=CARTESIAN_POINT ( 'NONE',  ( 44.35000000000000142, -3.309499999999999886, 0.000000000000000000 ) ) ;
#48766=ORIENTED_EDGE ( 'NONE', *, *, #17646, .F. ) ;
#48778=CARTESIAN_POINT ( 'NONE',  ( 38.09999999999999432, 3.309500000000003439, 0.000000000000000000 ) ) ;
#48826=CIRCLE ( 'NONE', #71250, 4.000000000000001776 ) ;
#48836=EDGE_CURVE ( 'NONE', #66259, #8430, #81792, .T. ) ;
#48858=CARTESIAN_POINT ( 'NONE',  ( 22.61650669486618526, 1.474610560812782335E-15, 0.000000000000000000 ) ) ;
#48864=DIRECTION ( 'NONE',  ( -0.5735764363510497121, 0.8191520442889892450, 1.003171929053521665E-16 ) ) ;
#48889=EDGE_CURVE ( 'NONE', #31781, #57508, #26290, .T. ) ;
#48922=CARTESIAN_POINT ( 'NONE',  ( 6.162888688655344005, 3.752776749732565253, 6.499999999999997335 ) ) ;
#48968=VECTOR ( 'NONE', #54929, 1000.000000000000000 ) ;
#48976=EDGE_CURVE ( 'NONE', #13541, #52531, #51667, .T. ) ;
#48988=CARTESIAN_POINT ( 'NONE',  ( 0.01372220897661846455, -5.309964801958114933, 3.802871176606136050 ) ) ;
#48996=EDGE_LOOP ( 'NONE', ( #82470, #81802, #58316, #90857, #47074 ) ) ;
#49002=CONICAL_SURFACE ( 'NONE', #66266, 3.309500000000001663, 0.9599310885968770357 ) ;
#49013=ADVANCED_FACE ( 'NONE', ( #90986 ), #61883, .F. ) ;
#49016=ORIENTED_EDGE ( 'NONE', *, *, #70293, .T. ) ;
#49019=AXIS2_PLACEMENT_3D ( 'NONE', #19081, #84835, #83755 ) ;
#49031=CARTESIAN_POINT ( 'NONE',  ( 41.08349330513380693, -4.000000000000000000, 4.898587196589415787E-16 ) ) ;
#49034=EDGE_CURVE ( 'NONE', #35387, #56862, #103363, .T. ) ;
#49045=DIRECTION ( 'NONE',  ( 0.000000000000000000, -1.000000000000000000, 0.000000000000000000 ) ) ;
#49053=CARTESIAN_POINT ( 'NONE',  ( 6.289812543865804351, 5.581224740283310837, -3.991031161979334385 ) ) ;
#49056=AXIS2_PLACEMENT_3D ( 'NONE', #24067, #73628, #41275 ) ;
#49097=ORIENTED_EDGE ( 'NONE', *, *, #73346, .T. ) ;
#49104=CARTESIAN_POINT ( 'NONE',  ( 0.000000000000000000, 0.000000000000000000, 4.000000000000000000 ) ) ;
#49131=DIRECTION ( 'NONE',  ( 0.000000000000000000, -1.000000000000000000, 0.000000000000000000 ) ) ;
#49162=AXIS2_PLACEMENT_3D ( 'NONE', #57550, #90477, #16584 ) ;
#49204=ORIENTED_EDGE ( 'NONE', *, *, #57974, .T. ) ;
#49207=VERTEX_POINT ( 'NONE', #104922 ) ;
#49237=LINE ( 'NONE', #40627, #84199 ) ;
#49264=CARTESIAN_POINT ( 'NONE',  ( 6.463647488011505793, 2.646730816809989673, -6.840026438643558748 ) ) ;
#49307=AXIS2_PLACEMENT_3D ( 'NONE', #92593, #101231, #75881 ) ;
#49327=ORIENTED_EDGE ( 'NONE', *, *, #43257, .F. ) ;
#49348=LINE ( 'NONE', #42326, #64410 ) ;
#49361=DIRECTION ( 'NONE',  ( -1.000000000000000000, -1.224606353822377258E-16, -0.000000000000000000 ) ) ;
#49380=ORIENTED_EDGE ( 'NONE', *, *, #103768, .T. ) ;
#49381=DIRECTION ( 'NONE',  ( 0.000000000000000000, -1.000000000000000000, 0.000000000000000000 ) ) ;
#49405=CONICAL_SURFACE ( 'NONE', #75205, 6.500000000000000000, 1.047197551196600296 ) ;
#49408=ADVANCED_FACE ( 'NONE', ( #68167 ), #24225, .T. ) ;
#49413=AXIS2_PLACEMENT_3D ( 'NONE', #35402, #68270, #75279 ) ;
#49459=VECTOR ( 'NONE', #92674, 1000.000000000000000 ) ;
#49461=DIRECTION ( 'NONE',  ( -1.000000000000000000, -1.224606353822377258E-16, -0.000000000000000000 ) ) ;
#49469=AXIS2_PLACEMENT_3D ( 'NONE', #81072, #56793, #105879 ) ;
#49474=DIRECTION ( 'NONE',  ( 0.000000000000000000, -1.000000000000000000, 0.000000000000000000 ) ) ;
#49482=DIRECTION ( 'NONE',  ( 1.000000000000000000, 1.224606353822377258E-16, 0.000000000000000000 ) ) ;
#49511=CYLINDRICAL_SURFACE ( 'NONE', #94557, 4.000000000000000000 ) ;
#49522=VERTEX_POINT ( 'NONE', #84357 ) ;
#49537=EDGE_CURVE ( 'NONE', #81845, #53956, #3497, .T. ) ;
#49555=CONICAL_SURFACE ( 'NONE', #63369, 4.000000000000001776, 0.9599310885968808105 ) ;
#49559=FACE_OUTER_BOUND ( 'NONE', #57132, .T. ) ;
#49562=EDGE_LOOP ( 'NONE', ( #88723, #78345, #5444, #24228, #36910 ) ) ;
#49567=ORIENTED_EDGE ( 'NONE', *, *, #2403, .F. ) ;
#49580=EDGE_LOOP ( 'NONE', ( #75295, #66320, #103062, #71745, #49097 ) ) ;
#49588=ORIENTED_EDGE ( 'NONE', *, *, #99878, .T. ) ;
#49622=CARTESIAN_POINT ( 'NONE',  ( 19.34999999999999787, 1.533819458162526451E-15, 0.000000000000000000 ) ) ;
#49652=CARTESIAN_POINT ( 'NONE',  ( 22.61650669486618526, -3.851859888774471706E-31, 4.000000000000000888 ) ) ;
#49658=CARTESIAN_POINT ( 'NONE',  ( 6.936184427528457874, 0.000000000000000000, -8.605212085995399107 ) ) ;
#49672=ORIENTED_EDGE ( 'NONE', *, *, #46061, .F. ) ;
#49673=DIRECTION ( 'NONE',  ( -1.000000000000000000, -1.224606353822377258E-16, -0.000000000000000000 ) ) ;
#49694=AXIS2_PLACEMENT_3D ( 'NONE', #22077, #9566, #17689 ) ;
#49696=VERTEX_POINT ( 'NONE', #87029 ) ;
#49709=LINE ( 'NONE', #77720, #91403 ) ;
#49714=ORIENTED_EDGE ( 'NONE', *, *, #18724, .F. ) ;
#49725=DIRECTION ( 'NONE',  ( 0.5735764363510462704, 0.8191520442889915765, 0.000000000000000000 ) ) ;
#49815=ORIENTED_EDGE ( 'NONE', *, *, #100102, .F. ) ;
#49822=CARTESIAN_POINT ( 'NONE',  ( 9.349999999999997868, 1.533819458162526451E-15, 0.000000000000000000 ) ) ;
#49856=ORIENTED_EDGE ( 'NONE', *, *, #83486, .T. ) ;
#49862=CARTESIAN_POINT ( 'NONE',  ( 6.333820801331254913, -4.275724398228172518, -5.594228103109054828 ) ) ;
#49863=CARTESIAN_POINT ( 'NONE',  ( 0.5805565836007602343, 3.752776749732561257, -6.499999999999999112 ) ) ;
#49899=VERTEX_POINT ( 'NONE', #13504 ) ;
#49912=FACE_OUTER_BOUND ( 'NONE', #59250, .T. ) ;
#49935=EDGE_CURVE ( 'NONE', #22614, #32012, #44065, .T. ) ;
#49966=CIRCLE ( 'NONE', #77539, 4.000000000000001776 ) ;
#49968=DIRECTION ( 'NONE',  ( 0.000000000000000000, 0.000000000000000000, 1.000000000000000000 ) ) ;
#49981=AXIS2_PLACEMENT_3D ( 'NONE', #84571, #12251, #36053 ) ;
#49986=ORIENTED_EDGE ( 'NONE', *, *, #85143, .T. ) ;
#49995=EDGE_CURVE ( 'NONE', #45750, #31200, #66724, .T. ) ;
#50002=VERTEX_POINT ( 'NONE', #100146 ) ;
#50013=CARTESIAN_POINT ( 'NONE',  ( 31.84999999999999787, 3.309500000000003439, 0.000000000000000000 ) ) ;
#50022=CYLINDRICAL_SURFACE ( 'NONE', #31246, 4.000000000000000000 ) ;
#50047=DIRECTION ( 'NONE',  ( -1.000000000000000000, -1.224606353822377258E-16, -0.000000000000000000 ) ) ;
#50048=DIRECTION ( 'NONE',  ( 0.000000000000000000, 0.000000000000000000, 1.000000000000000000 ) ) ;
#50073=EDGE_CURVE ( 'NONE', #54290, #83253, #31156, .T. ) ;
#50077=DIRECTION ( 'NONE',  ( -1.000000000000000000, -1.224606353822377258E-16, -0.000000000000000000 ) ) ;
#50105=DIRECTION ( 'NONE',  ( 0.000000000000000000, -1.000000000000000000, 0.000000000000000000 ) ) ;
#50157=CARTESIAN_POINT ( 'NONE',  ( 41.08349330513380693, 4.000000000000002665, 0.000000000000000000 ) ) ;
#50174=ORIENTED_EDGE ( 'NONE', *, *, #32198, .T. ) ;
#50215=AXIS2_PLACEMENT_3D ( 'NONE', #62442, #86202, #69994 ) ;
#50250=EDGE_CURVE ( 'NONE', #11128, #87415, #70772, .T. ) ;
#50264=FACE_OUTER_BOUND ( 'NONE', #6416, .T. ) ;
#50265=EDGE_CURVE ( 'NONE', #6164, #13541, #31599, .T. ) ;
#50292=DIRECTION ( 'NONE',  ( -0.5735764363510494901, -0.8191520442889894671, 0.000000000000000000 ) ) ;
#50296=LINE ( 'NONE', #40613, #65398 ) ;
#50313=AXIS2_PLACEMENT_3D ( 'NONE', #73389, #106290, #48058 ) ;
#50323=EDGE_CURVE ( 'NONE', #84503, #43166, #81279, .T. ) ;
#50324=EDGE_LOOP ( 'NONE', ( #34205, #47434, #103067, #75758, #11473 ) ) ;
#50331=CARTESIAN_POINT ( 'NONE',  ( 32.33349330513379982, 1.593028355512270567E-15, 0.000000000000000000 ) ) ;
#50341=DIRECTION ( 'NONE',  ( 0.000000000000000000, -1.000000000000000000, 0.000000000000000000 ) ) ;
#50342=DIRECTION ( 'NONE',  ( 0.000000000000000000, -1.000000000000000000, 0.000000000000000000 ) ) ;
#50383=FACE_OUTER_BOUND ( 'NONE', #35222, .T. ) ;
#50393=ORIENTED_EDGE ( 'NONE', *, *, #43257, .T. ) ;
#50404=EDGE_CURVE ( 'NONE', #40876, #98370, #51898, .T. ) ;
#50410=DIRECTION ( 'NONE',  ( -1.000000000000000000, -1.224606353822377258E-16, -0.000000000000000000 ) ) ;
#50411=EDGE_CURVE ( 'NONE', #8490, #74905, #103858, .T. ) ;
#50459=CARTESIAN_POINT ( 'NONE',  ( 10.59999999999999609, 1.533819458162526451E-15, 0.000000000000000000 ) ) ;
#50477=DIRECTION ( 'NONE',  ( 0.000000000000000000, -1.000000000000000000, 0.000000000000000000 ) ) ;
#50494=CARTESIAN_POINT ( 'NONE',  ( 6.585468679846621320, 3.617797563910810865, 6.733790807807553236 ) ) ;
#50548=CARTESIAN_POINT ( 'NONE',  ( 0.2573354458087814822, 4.368923434677189022, 5.432802636760777126 ) ) ;
#50550=CARTESIAN_POINT ( 'NONE',  ( 40.11650669486618881, -3.851859888774471706E-31, 4.000000000000000888 ) ) ;
#50560=AXIS2_PLACEMENT_3D ( 'NONE', #46611, #79507, #30996 ) ;
#50583=ORIENTED_EDGE ( 'NONE', *, *, #32011, .F. ) ;
#50588=AXIS2_PLACEMENT_3D ( 'NONE', #87712, #4669, #104403 ) ;
#50594=CARTESIAN_POINT ( 'NONE',  ( 6.289812543865802574, 6.246946743711088601, 2.837966828325882318 ) ) ;
#50609=EDGE_LOOP ( 'NONE', ( #68328, #532, #78571, #102092, #60976, #76999 ) ) ;
#50618=LINE ( 'NONE', #9637, #64812 ) ;
#50647=FACE_OUTER_BOUND ( 'NONE', #89629, .T. ) ;
#50659=CONICAL_SURFACE ( 'NONE', #95506, 3.309500000000001663, 0.9599310885968770357 ) ;
#50666=AXIS2_PLACEMENT_3D ( 'NONE', #90759, #83186, #75078 ) ;
#50783=FACE_OUTER_BOUND ( 'NONE', #93195, .T. ) ;
#50787=EDGE_CURVE ( 'NONE', #24472, #73965, #39838, .T. ) ;
#50791=CIRCLE ( 'NONE', #69770, 4.000000000000000888 ) ;
#50796=TOROIDAL_SURFACE ( 'NONE', #80064, 8.400000000000000355, 0.5999999999999978684 ) ;
#50822=DIRECTION ( 'NONE',  ( 1.000000000000000000, 1.224606353822377258E-16, 0.000000000000000000 ) ) ;
#50826=ORIENTED_EDGE ( 'NONE', *, *, #56516, .F. ) ;
#50830=ORIENTED_EDGE ( 'NONE', *, *, #45147, .F. ) ;
#50838=DIRECTION ( 'NONE',  ( -1.000000000000000000, -1.224606353822377258E-16, -0.000000000000000000 ) ) ;
#50840=DIRECTION ( 'NONE',  ( -1.000000000000000000, -0.000000000000000000, -0.000000000000000000 ) ) ;
#50851=DIRECTION ( 'NONE',  ( -1.000000000000000000, -1.224606353822377258E-16, -0.000000000000000000 ) ) ;
#50868=CIRCLE ( 'NONE', #26847, 4.000000000000000888 ) ;
#50875=DIRECTION ( 'NONE',  ( -1.000000000000000000, -1.224606353822377258E-16, -0.000000000000000000 ) ) ;
#50894=DIRECTION ( 'NONE',  ( -1.000000000000000000, -1.224606353822377258E-16, -0.000000000000000000 ) ) ;
#50906=AXIS2_PLACEMENT_3D ( 'NONE', #41953, #17171, #10121 ) ;
#50913=CARTESIAN_POINT ( 'NONE',  ( 6.289692432696772251, -6.589071317540681427, -2.245373559998993684 ) ) ;
#50918=DIRECTION ( 'NONE',  ( 0.000000000000000000, -0.5000000000000011102, -0.8660254037844379305 ) ) ;
#50923=ORIENTED_EDGE ( 'NONE', *, *, #34599, .T. ) ;
#50940=CARTESIAN_POINT ( 'NONE',  ( 41.08349330513380693, 4.898587196589405926E-16, -4.000000000000001776 ) ) ;
#50954=AXIS2_PLACEMENT_3D ( 'NONE', #44230, #52842, #78694 ) ;
#50975=DIRECTION ( 'NONE',  ( -1.000000000000000000, -0.000000000000000000, -0.000000000000000000 ) ) ;
#51011=AXIS2_PLACEMENT_3D ( 'NONE', #91177, #26462, #99225 ) ;
#51021=STYLED_ITEM ( 'NONE', ( #64483 ), #88996 ) ;
#51040=ORIENTED_EDGE ( 'NONE', *, *, #82674, .T. ) ;
#51041=ORIENTED_EDGE ( 'NONE', *, *, #51124, .T. ) ;
#51050=ORIENTED_EDGE ( 'NONE', *, *, #27558, .T. ) ;
#51062=DIRECTION ( 'NONE',  ( -1.000000000000000000, -0.000000000000000000, -0.000000000000000000 ) ) ;
#51065=CARTESIAN_POINT ( 'NONE',  ( 0.000000000000000000, 0.000000000000000000, 0.000000000000000000 ) ) ;
#51102=CONICAL_SURFACE ( 'NONE', #49413, 3.309500000000001663, 0.9599310885968770357 ) ;
#51124=EDGE_CURVE ( 'NONE', #21525, #60365, #17271, .T. ) ;
#51157=CARTESIAN_POINT ( 'NONE',  ( 42.61650669486618881, 1.474610560812782335E-15, 0.000000000000000000 ) ) ;
#51160=CARTESIAN_POINT ( 'NONE',  ( 0.000000000000000000, 0.000000000000000000, 0.000000000000000000 ) ) ;
#51162=ORIENTED_EDGE ( 'NONE', *, *, #14040, .T. ) ;
#51186=ADVANCED_FACE ( 'NONE', ( #106115 ), #65769, .T. ) ;
#51233=ORIENTED_EDGE ( 'NONE', *, *, #16782, .F. ) ;
#51252=DIRECTION ( 'NONE',  ( -1.000000000000000000, -1.224606353822377258E-16, -0.000000000000000000 ) ) ;
#51289=CARTESIAN_POINT ( 'NONE',  ( 37.33349330513379982, 1.593028355512270567E-15, 0.000000000000000000 ) ) ;
#51292=DIRECTION ( 'NONE',  ( -1.000000000000000000, -0.000000000000000000, -0.000000000000000000 ) ) ;
#51312=AXIS2_PLACEMENT_3D ( 'NONE', #63455, #63983, #22478 ) ;
#51314=DIRECTION ( 'NONE',  ( 0.000000000000000000, -1.000000000000000000, 0.000000000000000000 ) ) ;
#51319=ORIENTED_EDGE ( 'NONE', *, *, #82674, .F. ) ;
#51341=EDGE_LOOP ( 'NONE', ( #53780, #94647, #18604, #12959, #12540 ) ) ;
#51397=AXIS2_PLACEMENT_3D ( 'NONE', #51605, #51062, #92065 ) ;
#51414=CARTESIAN_POINT ( 'NONE',  ( 33.86650669486618881, -3.851859888774471706E-31, 4.000000000000000888 ) ) ;
#51415=VERTEX_POINT ( 'NONE', #67288 ) ;
#51457=CARTESIAN_POINT ( 'NONE',  ( 6.585468679846627538, -7.640532685286901327, 0.2337908078075560669 ) ) ;
#51467=EDGE_CURVE ( 'NONE', #51686, #68449, #81298, .T. ) ;
#51488=CONICAL_SURFACE ( 'NONE', #13527, 3.309500000000001663, 0.9599310885968770357 ) ;
#51502=ORIENTED_EDGE ( 'NONE', *, *, #99016, .T. ) ;
#51507=ORIENTED_EDGE ( 'NONE', *, *, #56637, .F. ) ;
#51537=EDGE_LOOP ( 'NONE', ( #65079, #10852, #38389, #98763, #27961 ) ) ;
#51554=ORIENTED_EDGE ( 'NONE', *, *, #79646, .F. ) ;
#51566=VECTOR ( 'NONE', #96625, 1000.000000000000000 ) ;
#51570=CARTESIAN_POINT ( 'NONE',  ( 6.445370176741849200, 7.262437273738760801, 1.101027156348632685 ) ) ;
#51574=ORIENTED_EDGE ( 'NONE', *, *, #476, .F. ) ;
#51598=CIRCLE ( 'NONE', #3408, 4.000000000000001776 ) ;
#51605=CARTESIAN_POINT ( 'NONE',  ( 0.000000000000000000, 0.000000000000000000, 0.000000000000000000 ) ) ;
#51609=PLANE ( 'NONE',  #47778 ) ;
#51610=FACE_OUTER_BOUND ( 'NONE', #56957, .T. ) ;
#51612=FACE_OUTER_BOUND ( 'NONE', #87247, .T. ) ;
#51622=ORIENTED_EDGE ( 'NONE', *, *, #34419, .F. ) ;
#51625=DIRECTION ( 'NONE',  ( -1.000000000000000000, -1.224606353822377258E-16, -0.000000000000000000 ) ) ;
#51630=FACE_OUTER_BOUND ( 'NONE', #11258, .T. ) ;
#51641=EDGE_CURVE ( 'NONE', #68449, #38628, #18485, .T. ) ;
#51647=FACE_OUTER_BOUND ( 'NONE', #101574, .T. ) ;
#51663=ORIENTED_EDGE ( 'NONE', *, *, #98009, .F. ) ;
#51667=CIRCLE ( 'NONE', #29323, 4.000000000000000888 ) ;
#51686=VERTEX_POINT ( 'NONE', #66285 ) ;
#51732=LINE ( 'NONE', #76537, #89797 ) ;
#51791=EDGE_LOOP ( 'NONE', ( #62059, #84591, #41437, #102429, #81941 ) ) ;
#51826=FACE_OUTER_BOUND ( 'NONE', #48996, .T. ) ;
#51836=AXIS2_PLACEMENT_3D ( 'NONE', #63637, #96526, #22658 ) ;
#51853=DIRECTION ( 'NONE',  ( 0.000000000000000000, -1.000000000000000000, 0.000000000000000000 ) ) ;
#51885=ADVANCED_FACE ( 'NONE', ( #58694 ), #65715, .T. ) ;
#51886=DIRECTION ( 'NONE',  ( -0.5735764363510494901, -0.8191520442889894671, 0.000000000000000000 ) ) ;
#51895=ADVANCED_FACE ( 'NONE', ( #81341 ), #59000, .T. ) ;
#51898=CIRCLE ( 'NONE', #101797, 4.000000000000001776 ) ;
#51900=CARTESIAN_POINT ( 'NONE',  ( 44.35000000000000142, 1.533819458162526451E-15, 0.000000000000000000 ) ) ;
#51902=CIRCLE ( 'NONE', #27798, 3.309500000000001663 ) ;
#51914=FACE_OUTER_BOUND ( 'NONE', #56477, .T. ) ;
#51922=DIRECTION ( 'NONE',  ( 0.000000000000000000, 0.000000000000000000, 1.000000000000000000 ) ) ;
#51985=CARTESIAN_POINT ( 'NONE',  ( 5.819846122303833802, -6.321060697774956161, -2.051601713727018161 ) ) ;
#51991=PLANE ( 'NONE',  #35308 ) ;
#52010=CIRCLE ( 'NONE', #67507, 3.309500000000001663 ) ;
#52018=DIRECTION ( 'NONE',  ( 1.000000000000000000, 1.224606353822377258E-16, 0.000000000000000000 ) ) ;
#52122=ORIENTED_EDGE ( 'NONE', *, *, #84834, .T. ) ;
#52130=CIRCLE ( 'NONE', #62535, 3.309500000000001663 ) ;
#52139=ORIENTED_EDGE ( 'NONE', *, *, #16953, .T. ) ;
#52155=DIRECTION ( 'NONE',  ( 0.5735764363510462704, 0.8191520442889915765, 0.000000000000000000 ) ) ;
#52186=CARTESIAN_POINT ( 'NONE',  ( 0.4053525175236804556, 3.145852061456246851, 6.499999999999998224 ) ) ;
#52187=ORIENTED_EDGE ( 'NONE', *, *, #72556, .F. ) ;
#52189=DIRECTION ( 'NONE',  ( 0.5735764363510466035, -0.8191520442889914655, 1.003171929053524500E-16 ) ) ;
#52211=AXIS2_PLACEMENT_3D ( 'NONE', #3181, #26438, #18874 ) ;
#52219=CARTESIAN_POINT ( 'NONE',  ( 25.11650669486618881, -3.999999999999998224, 0.000000000000000000 ) ) ;
#52221=CARTESIAN_POINT ( 'NONE',  ( 6.458251213448832573, 3.357560920637069568, 6.499999999999997335 ) ) ;
#52239=CIRCLE ( 'NONE', #55685, 3.309500000000001663 ) ;
#52252=DIRECTION ( 'NONE',  ( 1.000000000000000000, 1.224606353822377258E-16, 0.000000000000000000 ) ) ;
#52263=CARTESIAN_POINT ( 'NONE',  ( 0.000000000000000000, 0.000000000000000000, 0.000000000000000000 ) ) ;
#52276=FACE_OUTER_BOUND ( 'NONE', #16873, .T. ) ;
#52310=ORIENTED_EDGE ( 'NONE', *, *, #72954, .T. ) ;
#52384=DIRECTION ( 'NONE',  ( -1.000000000000000000, -1.224606353822377258E-16, -0.000000000000000000 ) ) ;
#52393=DIRECTION ( 'NONE',  ( 0.000000000000000000, 1.000000000000000000, 0.000000000000000000 ) ) ;
#52410=( NAMED_UNIT ( * ) PLANE_ANGLE_UNIT ( ) SI_UNIT ( $, .RADIAN. ) );
#52430=ORIENTED_EDGE ( 'NONE', *, *, #26199, .T. ) ;
#52511=DIRECTION ( 'NONE',  ( -0.7071067811865530128, 8.659560562354868763E-17, -0.7071067811865421326 ) ) ;
#52527=EDGE_LOOP ( 'NONE', ( #100240, #99865, #30354, #65247, #17072, #78868 ) ) ;
#52531=VERTEX_POINT ( 'NONE', #88550 ) ;
#52536=AXIS2_PLACEMENT_3D ( 'NONE', #29645, #85743, #29134 ) ;
#52545=CARTESIAN_POINT ( 'NONE',  ( 32.61650669486618881, 1.474610560812782335E-15, 0.000000000000000000 ) ) ;
#52552=CONICAL_SURFACE ( 'NONE', #54460, 3.309499999999999886, 0.7853981633974407295 ) ;
#52583=FACE_OUTER_BOUND ( 'NONE', #875, .T. ) ;
#52597=DIRECTION ( 'NONE',  ( 0.000000000000000000, -1.000000000000000000, 0.000000000000000000 ) ) ;
#52600=DIRECTION ( 'NONE',  ( 1.000000000000000000, 1.224606353822377258E-16, 0.000000000000000000 ) ) ;
#52601=VERTEX_POINT ( 'NONE', #25440 ) ;
#52628=LINE ( 'NONE', #11636, #31475 ) ;
#52633=VECTOR ( 'NONE', #61622, 1000.000000000000000 ) ;
#52644=CARTESIAN_POINT ( 'NONE',  ( 22.33349330513380337, -4.000000000000000888, 4.898587196589416773E-16 ) ) ;
#52651=DIRECTION ( 'NONE',  ( 0.000000000000000000, 0.000000000000000000, 1.000000000000000000 ) ) ;
#52657=DIRECTION ( 'NONE',  ( 0.000000000000000000, -1.000000000000000000, 0.000000000000000000 ) ) ;
#52660=AXIS2_PLACEMENT_3D ( 'NONE', #44131, #50077, #101303 ) ;
#52661=VECTOR ( 'NONE', #40523, 1000.000000000000000 ) ;
#52664=ORIENTED_EDGE ( 'NONE', *, *, #56058, .T. ) ;
#52703=AXIS2_PLACEMENT_3D ( 'NONE', #96088, #22754, #55071 ) ;
#52715=ORIENTED_EDGE ( 'NONE', *, *, #31090, .T. ) ;
#52721=ORIENTED_EDGE ( 'NONE', *, *, #67922, .F. ) ;
#52723=CIRCLE ( 'NONE', #104393, 4.000000000000000888 ) ;
#52750=CARTESIAN_POINT ( 'NONE',  ( 18.86650669486618881, -3.851859888774471706E-31, 4.000000000000000888 ) ) ;
#52760=CARTESIAN_POINT ( 'NONE',  ( 6.352644769543418946, 2.685840869108941931, 6.500000000000298428 ) ) ;
#52762=ORIENTED_EDGE ( 'NONE', *, *, #64402, .T. ) ;
#52764=ORIENTED_EDGE ( 'NONE', *, *, #8547, .F. ) ;
#52774=ORIENTED_EDGE ( 'NONE', *, *, #43711, .T. ) ;
#52775=ORIENTED_EDGE ( 'NONE', *, *, #38834, .F. ) ;
#52776=VERTEX_POINT ( 'NONE', #100087 ) ;
#52779=DIRECTION ( 'NONE',  ( 0.000000000000000000, -1.000000000000000000, 0.000000000000000000 ) ) ;
#52798=DIRECTION ( 'NONE',  ( -1.000000000000000000, -1.224606353822377258E-16, -0.000000000000000000 ) ) ;
#52802=DIRECTION ( 'NONE',  ( -1.000000000000000000, -0.000000000000000000, -0.000000000000000000 ) ) ;
#52808=AXIS2_PLACEMENT_3D ( 'NONE', #24739, #16621, #106142 ) ;
#52811=ORIENTED_EDGE ( 'NONE', *, *, #85297, .T. ) ;
#52836=CONICAL_SURFACE ( 'NONE', #87344, 3.309500000000001663, 0.9599310885968770357 ) ;
#52842=DIRECTION ( 'NONE',  ( -1.000000000000000000, -1.224606353822377258E-16, -0.000000000000000000 ) ) ;
#52852=PRODUCT_DEFINITION ( 'UNKNOWN', '', #66325, #1392 ) ;
#52856=CARTESIAN_POINT ( 'NONE',  ( 11.36650669486618881, 1.474610560812782335E-15, 0.000000000000000000 ) ) ;
#52874=CARTESIAN_POINT ( 'NONE',  ( 33.58349330513379982, 1.593028355512270567E-15, 0.000000000000000000 ) ) ;
#52875=CIRCLE ( 'NONE', #40867, 3.309500000000001663 ) ;
#52893=VERTEX_POINT ( 'NONE', #102223 ) ;
#52898=CARTESIAN_POINT ( 'NONE',  ( 0.5805565836007654523, 7.505553499465140277, 2.211437577243512467E-16 ) ) ;
#52905=ADVANCED_FACE ( 'NONE', ( #60724 ), #21301, .T. ) ;
#52930=VERTEX_POINT ( 'NONE', #36475 ) ;
#52935=DIRECTION ( 'NONE',  ( -0.5735764363510497121, 0.8191520442889892450, 1.003171929053521665E-16 ) ) ;
#52938=EDGE_CURVE ( 'NONE', #33104, #7789, #7453, .T. ) ;
#52954=ORIENTED_EDGE ( 'NONE', *, *, #95578, .F. ) ;
#52960=CARTESIAN_POINT ( 'NONE',  ( 0.000000000000000000, 0.000000000000000000, 0.000000000000000000 ) ) ;
#52988=DIRECTION ( 'NONE',  ( 0.5735764363510466035, -0.8191520442889914655, 1.003171929053524500E-16 ) ) ;
#52993=CARTESIAN_POINT ( 'NONE',  ( 22.33349330513380337, 1.593028355512270567E-15, 0.000000000000000000 ) ) ;
#53059=CARTESIAN_POINT ( 'NONE',  ( 31.08349330513380337, 1.593028355512270567E-15, 0.000000000000000000 ) ) ;
#53063=LINE ( 'NONE', #29351, #1298 ) ;
#53080=DIRECTION ( 'NONE',  ( -0.5735764363510494901, -0.8191520442889894671, 0.000000000000000000 ) ) ;
#53084=ORIENTED_EDGE ( 'NONE', *, *, #70607, .F. ) ;
#53113=DIRECTION ( 'NONE',  ( 0.000000000000000000, 0.000000000000000000, 1.000000000000000000 ) ) ;
#53138=CARTESIAN_POINT ( 'NONE',  ( 6.162888688655350222, -7.505553499465148271, 0.000000000000000000 ) ) ;
#53154=CARTESIAN_POINT ( 'NONE',  ( -3.601054696133250315E-15, 5.788408252967898626, 2.974182810908597929 ) ) ;
#53188=AXIS2_PLACEMENT_3D ( 'NONE', #5090, #12627, #78432 ) ;
#53196=ORIENTED_EDGE ( 'NONE', *, *, #13466, .T. ) ;
#53209=CARTESIAN_POINT ( 'NONE',  ( 31.84999999999999787, 1.533819458162526451E-15, 0.000000000000000000 ) ) ;
#53242=FACE_OUTER_BOUND ( 'NONE', #103351, .T. ) ;
#53254=CONICAL_SURFACE ( 'NONE', #75640, 3.309500000000001663, 0.9599310885968770357 ) ;
#53284=CARTESIAN_POINT ( 'NONE',  ( 22.61650669486618526, 1.474610560812782335E-15, 0.000000000000000000 ) ) ;
#53301=DIRECTION ( 'NONE',  ( 0.000000000000000000, -1.000000000000000000, 0.000000000000000000 ) ) ;
#53303=ADVANCED_FACE ( 'NONE', ( #8166 ), #53815, .T. ) ;
#53343=CARTESIAN_POINT ( 'NONE',  ( 34.83349330513379982, -7.703719777548943412E-31, 4.000000000000001776 ) ) ;
#53384=CARTESIAN_POINT ( 'NONE',  ( 26.08349330513380337, 1.593028355512270567E-15, 0.000000000000000000 ) ) ;
#53417=FACE_OUTER_BOUND ( 'NONE', #79524, .T. ) ;
#53450=AXIS2_PLACEMENT_3D ( 'NONE', #84422, #10516, #93040 ) ;
#53491=EDGE_CURVE ( 'NONE', #29335, #25223, #71701, .T. ) ;
#53530=CARTESIAN_POINT ( 'NONE',  ( 7.500000000000001776, 0.000000000000000000, 8.400000000000000355 ) ) ;
#53564=CARTESIAN_POINT ( 'NONE',  ( 6.936184427528457874, 0.000000000000000000, 0.000000000000000000 ) ) ;
#53574=DIRECTION ( 'NONE',  ( -1.000000000000000000, -1.224606353822377258E-16, -0.000000000000000000 ) ) ;
#53592=EDGE_LOOP ( 'NONE', ( #60162, #103992, #63872, #63851, #73717 ) ) ;
#53621=CYLINDRICAL_SURFACE ( 'NONE', #55594, 4.000000000000000000 ) ;
#53631=ADVANCED_FACE ( 'NONE', ( #49559 ), #81436, .T. ) ;
#53637=CIRCLE ( 'NONE', #39945, 4.000000000000000888 ) ;
#53662=DIRECTION ( 'NONE',  ( 0.5735764363510466035, -0.8191520442889914655, 1.003171929053524500E-16 ) ) ;
#53674=LINE ( 'NONE', #54187, #77096 ) ;
#53702=CARTESIAN_POINT ( 'NONE',  ( 6.169949891409287623, 4.949864754176874548, 4.426582755168845473 ) ) ;
#53717=DIRECTION ( 'NONE',  ( -1.000000000000000000, -1.224606353822377258E-16, -0.000000000000000000 ) ) ;
#53722=EDGE_CURVE ( 'NONE', #39800, #48174, #28072, .T. ) ;
#53723=FACE_OUTER_BOUND ( 'NONE', #72155, .T. ) ;
#53727=VECTOR ( 'NONE', #73111, 1000.000000000000000 ) ;
#53756=CARTESIAN_POINT ( 'NONE',  ( 40.11650669486618881, 1.474610560812782335E-15, 0.000000000000000000 ) ) ;
#53780=ORIENTED_EDGE ( 'NONE', *, *, #100437, .F. ) ;
#53785=EDGE_CURVE ( 'NONE', #75857, #38628, #102088, .T. ) ;
#53815=CONICAL_SURFACE ( 'NONE', #67839, 3.309500000000001663, 0.9599310885968770357 ) ;
#53830=VERTEX_POINT ( 'NONE', #25881 ) ;
#53839=EDGE_CURVE ( 'NONE', #61668, #1636, #71139, .T. ) ;
#53849=CARTESIAN_POINT ( 'NONE',  ( 21.08349330513380337, 1.593028355512270567E-15, 0.000000000000000000 ) ) ;
#53854=CIRCLE ( 'NONE', #93446, 4.000000000000001776 ) ;
#53855=CARTESIAN_POINT ( 'NONE',  ( 6.162888688655347558, 7.505553499465140277, 0.000000000000000000 ) ) ;
#53869=CARTESIAN_POINT ( 'NONE',  ( 15.59999999999999787, 3.309500000000003439, 0.000000000000000000 ) ) ;
#53870=EDGE_LOOP ( 'NONE', ( #73183, #86273, #10626, #26589, #32086, #55050 ) ) ;
#53907=DIRECTION ( 'NONE',  ( 0.000000000000000000, -1.000000000000000000, 0.000000000000000000 ) ) ;
#53917=AXIS2_PLACEMENT_3D ( 'NONE', #34249, #74129, #67121 ) ;
#53934=ORIENTED_EDGE ( 'NONE', *, *, #30725, .T. ) ;
#53937=ORIENTED_EDGE ( 'NONE', *, *, #92660, .T. ) ;
#53956=VERTEX_POINT ( 'NONE', #101836 ) ;
#53988=VECTOR ( 'NONE', #61328, 1000.000000000000000 ) ;
#54016=DIRECTION ( 'NONE',  ( -1.000000000000000000, -1.224606353822377258E-16, -0.000000000000000000 ) ) ;
#54043=VERTEX_POINT ( 'NONE', #13342 ) ;
#54076=ORIENTED_EDGE ( 'NONE', *, *, #57683, .T. ) ;
#54081=CARTESIAN_POINT ( 'NONE',  ( 42.33349330513380693, 4.000000000000003553, 0.000000000000000000 ) ) ;
#54096=VERTEX_POINT ( 'NONE', #81263 ) ;
#54102=CARTESIAN_POINT ( 'NONE',  ( 0.000000000000000000, 0.000000000000000000, 4.000000000000000000 ) ) ;
#54123=DIRECTION ( 'NONE',  ( 0.000000000000000000, -1.000000000000000000, 0.000000000000000000 ) ) ;
#54163=AXIS2_PLACEMENT_3D ( 'NONE', #74381, #17244, #24286 ) ;
#54183=CONICAL_SURFACE ( 'NONE', #16315, 4.000000000000001776, 0.9599310885968808105 ) ;
#54187=CARTESIAN_POINT ( 'NONE',  ( 28.58349330513380337, -4.000000000000000000, 4.898587196589415787E-16 ) ) ;
#54193=AXIS2_PLACEMENT_3D ( 'NONE', #33082, #98826, #38644 ) ;
#54206=ORIENTED_EDGE ( 'NONE', *, *, #37517, .T. ) ;
#54223=VERTEX_POINT ( 'NONE', #47831 ) ;
#54290=VERTEX_POINT ( 'NONE', #59677 ) ;
#54297=AXIS2_PLACEMENT_3D ( 'NONE', #27682, #93444, #61079 ) ;
#54298=ADVANCED_FACE ( 'NONE', ( #35424 ), #90980, .T. ) ;
#54299=VERTEX_POINT ( 'NONE', #17627 ) ;
#54306=AXIS2_PLACEMENT_3D ( 'NONE', #32253, #25242, #49474 ) ;
#54323=CONICAL_SURFACE ( 'NONE', #95705, 3.309500000000001663, 0.9599310885968770357 ) ;
#54329=ORIENTED_EDGE ( 'NONE', *, *, #21272, .F. ) ;
#54347=ORIENTED_EDGE ( 'NONE', *, *, #23274, .T. ) ;
#54351=CARTESIAN_POINT ( 'NONE',  ( 6.169949891408688991, -6.308465495018778846, 2.073417244831591955 ) ) ;
#54365=CARTESIAN_POINT ( 'NONE',  ( 26.84999999999999787, -3.309499999999999886, 4.475777889183790779E-16 ) ) ;
#54371=VERTEX_POINT ( 'NONE', #1398 ) ;
#54375=VECTOR ( 'NONE', #2039, 1000.000000000000000 ) ;
#54396=AXIS2_PLACEMENT_3D ( 'NONE', #66409, #58324, #48618 ) ;
#54415=DIRECTION ( 'NONE',  ( 0.000000000000000000, -1.000000000000000000, 0.000000000000000000 ) ) ;
#54421=CARTESIAN_POINT ( 'NONE',  ( 13.58349330513380160, 1.593028355512270567E-15, 0.000000000000000000 ) ) ;
#54460=AXIS2_PLACEMENT_3D ( 'NONE', #34831, #66624, #68228 ) ;
#54463=ORIENTED_EDGE ( 'NONE', *, *, #60113, .F. ) ;
#54471=CIRCLE ( 'NONE', #20066, 3.309499999999999886 ) ;
#54473=CONICAL_SURFACE ( 'NONE', #64814, 3.309500000000001663, 0.9599310885968770357 ) ;
#54518=EDGE_CURVE ( 'NONE', #21525, #2814, #21291, .T. ) ;
#54521=CARTESIAN_POINT ( 'NONE',  ( 31.08349330513380337, 1.593028355512270567E-15, 0.000000000000000000 ) ) ;
#54540=CIRCLE ( 'NONE', #76898, 4.000000000000000888 ) ;
#54543=LINE ( 'NONE', #87486, #16166 ) ;
#54564=DIRECTION ( 'NONE',  ( 0.000000000000000000, -1.000000000000000000, 0.000000000000000000 ) ) ;
#54590=FACE_OUTER_BOUND ( 'NONE', #49562, .T. ) ;
#54601=ADVANCED_FACE ( 'NONE', ( #60949 ), #74591, .T. ) ;
#54605=DIRECTION ( 'NONE',  ( -1.000000000000000000, -0.000000000000000000, -0.000000000000000000 ) ) ;
#54609=CONICAL_SURFACE ( 'NONE', #87364, 4.000000000000001776, 0.9599310885968808105 ) ;
#54617=ORIENTED_EDGE ( 'NONE', *, *, #52938, .T. ) ;
#54623=DIRECTION ( 'NONE',  ( 0.000000000000000000, -1.000000000000000000, 0.000000000000000000 ) ) ;
#54630=DIRECTION ( 'NONE',  ( 0.000000000000000000, -1.000000000000000000, 0.000000000000000000 ) ) ;
#54637=CONICAL_SURFACE ( 'NONE', #28924, 4.000000000000001776, 0.9599310885968808105 ) ;
#54638=DIRECTION ( 'NONE',  ( 0.000000000000000000, -1.000000000000000000, 0.000000000000000000 ) ) ;
#54644=CONICAL_SURFACE ( 'NONE', #68459, 3.309500000000001663, 0.9599310885968770357 ) ;
#54660=VECTOR ( 'NONE', #91115, 1000.000000000000000 ) ;
#54684=LINE ( 'NONE', #78445, #82206 ) ;
#54713=CONICAL_SURFACE ( 'NONE', #32431, 4.000000000000001776, 0.9599310885968808105 ) ;
#54716=CARTESIAN_POINT ( 'NONE',  ( 0.000000000000000000, 0.000000000000000000, -6.499999999999999112 ) ) ;
#54717=ORIENTED_EDGE ( 'NONE', *, *, #14774, .F. ) ;
#54718=CARTESIAN_POINT ( 'NONE',  ( 41.85000000000000142, -3.309499999999999886, 4.475777889183790779E-16 ) ) ;
#54726=CARTESIAN_POINT ( 'NONE',  ( 9.349999999999997868, 1.533819458162526451E-15, 0.000000000000000000 ) ) ;
#54765=CARTESIAN_POINT ( 'NONE',  ( 6.562934840145646653, -7.579717272840345466, 0.5631738335430743758 ) ) ;
#54773=DIRECTION ( 'NONE',  ( 0.000000000000000000, 0.000000000000000000, 1.000000000000000000 ) ) ;
#54785=ORIENTED_EDGE ( 'NONE', *, *, #56927, .T. ) ;
#54787=CARTESIAN_POINT ( 'NONE',  ( 29.83349330513380337, -4.000000000000000000, 4.898587196589415787E-16 ) ) ;
#54801=VERTEX_POINT ( 'NONE', #106553 ) ;
#54820=DIRECTION ( 'NONE',  ( 1.000000000000000000, 1.224606353822377258E-16, 0.000000000000000000 ) ) ;
#54837=ORIENTED_EDGE ( 'NONE', *, *, #72954, .F. ) ;
#54838=CARTESIAN_POINT ( 'NONE',  ( 0.000000000000000000, 0.000000000000000000, 4.000000000000000000 ) ) ;
#54856=DIRECTION ( 'NONE',  ( 0.5735764363510466035, -0.8191520442889914655, 1.003171929053524500E-16 ) ) ;
#54858=AXIS2_PLACEMENT_3D ( 'NONE', #106176, #56027, #98625 ) ;
#54868=CIRCLE ( 'NONE', #27385, 4.000000000000001776 ) ;
#54875=DIRECTION ( 'NONE',  ( -1.000000000000000000, -0.000000000000000000, -0.000000000000000000 ) ) ;
#54876=DIRECTION ( 'NONE',  ( -1.000000000000000000, -1.224606353822377258E-16, -0.000000000000000000 ) ) ;
#54883=ORIENTED_EDGE ( 'NONE', *, *, #28750, .T. ) ;
#54885=CARTESIAN_POINT ( 'NONE',  ( 14.83349330513380337, 1.593028355512270567E-15, 0.000000000000000000 ) ) ;
#54894=FACE_OUTER_BOUND ( 'NONE', #69446, .T. ) ;
#54900=CIRCLE ( 'NONE', #46303, 4.000000000000001776 ) ;
#54905=EDGE_LOOP ( 'NONE', ( #43036, #90735, #21400, #79347, #47271 ) ) ;
#54929=DIRECTION ( 'NONE',  ( -0.5735764363510497121, 0.8191520442889892450, 1.003171929053521665E-16 ) ) ;
#54946=EDGE_CURVE ( 'NONE', #74465, #87270, #91934, .T. ) ;
#54964=PLANE ( 'NONE',  #32352 ) ;
#54971=FACE_OUTER_BOUND ( 'NONE', #51341, .T. ) ;
#54982=EDGE_CURVE ( 'NONE', #59572, #63953, #67833, .T. ) ;
#54984=AXIS2_PLACEMENT_3D ( 'NONE', #46523, #63786, #69748 ) ;
#54996=DIRECTION ( 'NONE',  ( 0.000000000000000000, -1.000000000000000000, 0.000000000000000000 ) ) ;
#55005=EDGE_LOOP ( 'NONE', ( #66777, #14855, #20109, #68964, #85093 ) ) ;
#55050=ORIENTED_EDGE ( 'NONE', *, *, #19197, .F. ) ;
#55071=DIRECTION ( 'NONE',  ( 0.000000000000000000, -1.000000000000000000, 0.000000000000000000 ) ) ;
#55072=DIRECTION ( 'NONE',  ( 0.000000000000000000, -1.000000000000000000, 0.000000000000000000 ) ) ;
#55086=CARTESIAN_POINT ( 'NONE',  ( 6.692429545713704186, 4.002214399422197033, -6.852332219948823244 ) ) ;
#55094=VERTEX_POINT ( 'NONE', #70231 ) ;
#55097=CARTESIAN_POINT ( 'NONE',  ( 24.83349330513380337, 1.593028355512270567E-15, 0.000000000000000000 ) ) ;
#55107=VECTOR ( 'NONE', #80677, 1000.000000000000000 ) ;
#55121=CARTESIAN_POINT ( 'NONE',  ( 27.33349330513380337, 1.593028355512270567E-15, 0.000000000000000000 ) ) ;
#55152=CYLINDRICAL_SURFACE ( 'NONE', #2152, 4.000000000000000000 ) ;
#55159=EDGE_CURVE ( 'NONE', #44939, #98423, #54543, .T. ) ;
#55168=VECTOR ( 'NONE', #94510, 1000.000000000000000 ) ;
#55173=ORIENTED_EDGE ( 'NONE', *, *, #65392, .F. ) ;
#55187=CIRCLE ( 'NONE', #32821, 8.400000000000000355 ) ;
#55196=CARTESIAN_POINT ( 'NONE',  ( 8.099999999999999645, 1.041268927496807532E-15, -8.400000000000000355 ) ) ;
#55200=DIRECTION ( 'NONE',  ( -1.000000000000000000, -1.224606353822377258E-16, -0.000000000000000000 ) ) ;
#55208=DIRECTION ( 'NONE',  ( -0.5735764363510497121, 0.8191520442889892450, 1.003171929053521665E-16 ) ) ;
#55234=DIRECTION ( 'NONE',  ( 0.000000000000000000, -1.000000000000000000, 0.000000000000000000 ) ) ;
#55260=DIRECTION ( 'NONE',  ( 0.000000000000000000, -1.000000000000000000, 0.000000000000000000 ) ) ;
#55265=VERTEX_POINT ( 'NONE', #49652 ) ;
#55282=CIRCLE ( 'NONE', #105260, 4.000000000000000888 ) ;
#55297=DIRECTION ( 'NONE',  ( 0.000000000000000000, -1.000000000000000000, 0.000000000000000000 ) ) ;
#55299=DIRECTION ( 'NONE',  ( -1.000000000000000000, -0.000000000000000000, -0.000000000000000000 ) ) ;
#55340=EDGE_CURVE ( 'NONE', #55094, #72439, #18383, .T. ) ;
#55349=VERTEX_POINT ( 'NONE', #2154 ) ;
#55354=DIRECTION ( 'NONE',  ( -1.000000000000000000, -1.224606353822377258E-16, -0.000000000000000000 ) ) ;
#55379=CARTESIAN_POINT ( 'NONE',  ( 6.936184427528457874, 0.000000000000000000, 0.000000000000000000 ) ) ;
#55417=ORIENTED_EDGE ( 'NONE', *, *, #23345, .T. ) ;
#55450=ORIENTED_EDGE ( 'NONE', *, *, #65172, .F. ) ;
#55455=CONICAL_SURFACE ( 'NONE', #5589, 4.000000000000001776, 0.9599310885968808105 ) ;
#55456=VECTOR ( 'NONE', #18447, 1000.000000000000000 ) ;
#55459=CARTESIAN_POINT ( 'NONE',  ( 31.36650669486618881, 1.474610560812782335E-15, 0.000000000000000000 ) ) ;
#55486=EDGE_CURVE ( 'NONE', #79845, #49899, #105515, .T. ) ;
#55530=ORIENTED_EDGE ( 'NONE', *, *, #34724, .F. ) ;
#55532=AXIS2_PLACEMENT_3D ( 'NONE', #105827, #101990, #35709 ) ;
#55566=AXIS2_PLACEMENT_3D ( 'NONE', #40944, #88970, #57636 ) ;
#55569=CARTESIAN_POINT ( 'NONE',  ( 37.61650669486618881, 4.898587196589411843E-16, -4.000000000000000888 ) ) ;
#55571=ORIENTED_EDGE ( 'NONE', *, *, #54518, .F. ) ;
#55591=LINE ( 'NONE', #39973, #104288 ) ;
#55594=AXIS2_PLACEMENT_3D ( 'NONE', #45551, #71931, #95161 ) ;
#55616=EDGE_CURVE ( 'NONE', #45510, #31296, #85161, .T. ) ;
#55619=CARTESIAN_POINT ( 'NONE',  ( 36.08349330513379982, 1.593028355512270567E-15, 0.000000000000000000 ) ) ;
#55646=DIRECTION ( 'NONE',  ( 0.000000000000000000, 1.000000000000000000, 0.000000000000000000 ) ) ;
#55660=EDGE_LOOP ( 'NONE', ( #38901, #41280, #21501, #65200, #98525 ) ) ;
#55666=LINE ( 'NONE', #73995, #79083 ) ;
#55675=EDGE_CURVE ( 'NONE', #91175, #30104, #98913, .T. ) ;
#55677=CONICAL_SURFACE ( 'NONE', #89733, 4.000000000000001776, 0.9599310885968808105 ) ;
#55685=AXIS2_PLACEMENT_3D ( 'NONE', #101358, #52798, #18883 ) ;
#55694=ORIENTED_EDGE ( 'NONE', *, *, #98224, .F. ) ;
#55696=LINE ( 'NONE', #15264, #23093 ) ;
#55750=CARTESIAN_POINT ( 'NONE',  ( 42.61650669486618881, 4.898587196589411843E-16, -4.000000000000000888 ) ) ;
#55764=CARTESIAN_POINT ( 'NONE',  ( 0.06682554136337939821, 6.264794173742277650, 2.149058192116895860 ) ) ;
#55766=CARTESIAN_POINT ( 'NONE',  ( 0.4042117618287688896, -3.141900367811087502, -6.500000000000000000 ) ) ;
#55798=CIRCLE ( 'NONE', #23132, 4.000000000000001776 ) ;
#55816=VERTEX_POINT ( 'NONE', #27309 ) ;
#55821=AXIS2_PLACEMENT_3D ( 'NONE', #36684, #102438, #29136 ) ;
#55823=CARTESIAN_POINT ( 'NONE',  ( 31.36650669486618881, 1.474610560812782335E-15, 0.000000000000000000 ) ) ;
#55824=CARTESIAN_POINT ( 'NONE',  ( 1.235538725728271446E-15, -5.788408252967909284, -2.974182810908597929 ) ) ;
#55830=CIRCLE ( 'NONE', #100667, 4.000000000000000888 ) ;
#55835=B_SPLINE_CURVE_WITH_KNOTS ( 'NONE', 3,
 ( #68957, #36613, #29578, #11741, #46783, #94826 ),
 .UNSPECIFIED., .F., .F.,
 ( 4, 2, 4 ),
 ( -4.698498716302674511E-06, 0.0003457374136927991335, 0.0006961733261019009255 ),
 .UNSPECIFIED. ) ;
#55843=CARTESIAN_POINT ( 'NONE',  ( 26.36650669486618881, 4.898587196589411843E-16, -4.000000000000000888 ) ) ;
#55862=VERTEX_POINT ( 'NONE', #19750 ) ;
#55873=FACE_OUTER_BOUND ( 'NONE', #33511, .T. ) ;
#55889=VERTEX_POINT ( 'NONE', #40652 ) ;
#55891=VECTOR ( 'NONE', #27271, 1000.000000000000114 ) ;
#55892=LINE ( 'NONE', #47813, #102628 ) ;
#55893=DIRECTION ( 'NONE',  ( 0.000000000000000000, 0.000000000000000000, 1.000000000000000000 ) ) ;
#55928=DIRECTION ( 'NONE',  ( 0.000000000000000000, -1.000000000000000000, 0.000000000000000000 ) ) ;
#55954=ADVANCED_FACE ( 'NONE', ( #8811 ), #106436, .T. ) ;
#55983=VERTEX_POINT ( 'NONE', #102070 ) ;
#55989=CIRCLE ( 'NONE', #44026, 4.000000000000000888 ) ;
#55990=VERTEX_POINT ( 'NONE', #44925 ) ;
#55992=CARTESIAN_POINT ( 'NONE',  ( 23.58349330513380337, 4.898587196589405926E-16, -4.000000000000001776 ) ) ;
#56000=EDGE_CURVE ( 'NONE', #93546, #32972, #24971, .T. ) ;
#56002=CARTESIAN_POINT ( 'NONE',  ( 36.36650669486618881, 1.474610560812782335E-15, 0.000000000000000000 ) ) ;
#56005=ORIENTED_EDGE ( 'NONE', *, *, #68111, .F. ) ;
#56012=DIRECTION ( 'NONE',  ( 0.000000000000000000, 0.000000000000000000, 1.000000000000000000 ) ) ;
#56027=DIRECTION ( 'NONE',  ( -1.000000000000000000, -1.224606353822377258E-16, -0.000000000000000000 ) ) ;
#56044=CARTESIAN_POINT ( 'NONE',  ( 25.11650669486618881, 1.474610560812782335E-15, 0.000000000000000000 ) ) ;
#56058=EDGE_CURVE ( 'NONE', #55990, #58778, #71435, .T. ) ;
#56067=DIRECTION ( 'NONE',  ( 0.000000000000000000, -1.000000000000000000, 0.000000000000000000 ) ) ;
#56075=VECTOR ( 'NONE', #44181, 1000.000000000000114 ) ;
#56077=ORIENTED_EDGE ( 'NONE', *, *, #23603, .F. ) ;
#56086=EDGE_CURVE ( 'NONE', #86709, #77600, #71514, .T. ) ;
#56100=DIRECTION ( 'NONE',  ( 0.000000000000000000, -1.000000000000000000, 0.000000000000000000 ) ) ;
#56142=VECTOR ( 'NONE', #45796, 1000.000000000000000 ) ;
#56157=ORIENTED_EDGE ( 'NONE', *, *, #98829, .T. ) ;
#56186=FACE_OUTER_BOUND ( 'NONE', #4770, .T. ) ;
#56192=DIRECTION ( 'NONE',  ( 0.000000000000000000, -1.000000000000000000, 0.000000000000000000 ) ) ;
#56204=EDGE_CURVE ( 'NONE', #61302, #79890, #81487, .T. ) ;
#56208=CARTESIAN_POINT ( 'NONE',  ( 26.36650669486618881, -3.999999999999998224, 0.000000000000000000 ) ) ;
#56236=AXIS2_PLACEMENT_3D ( 'NONE', #69331, #78464, #61237 ) ;
#56245=CIRCLE ( 'NONE', #37376, 4.000000000000001776 ) ;
#56257=LINE ( 'NONE', #74578, #94589 ) ;
#56261=ORIENTED_EDGE ( 'NONE', *, *, #71720, .F. ) ;
#56313=AXIS2_PLACEMENT_3D ( 'NONE', #106302, #97159, #30880 ) ;
#56323=CARTESIAN_POINT ( 'NONE',  ( 28.58349330513380337, -7.703719777548943412E-31, 4.000000000000001776 ) ) ;
#56387=CONICAL_SURFACE ( 'NONE', #65032, 3.309500000000001663, 0.9599310885968770357 ) ;
#56398=AXIS2_PLACEMENT_3D ( 'NONE', #105131, #87366, #56012 ) ;
#56407=CARTESIAN_POINT ( 'NONE',  ( 0.000000000000000000, 4.898587196589412829E-16, -4.000000000000000000 ) ) ;
#56436=DIRECTION ( 'NONE',  ( 0.000000000000000000, -1.000000000000000000, 0.000000000000000000 ) ) ;
#56439=ADVANCED_FACE ( 'NONE', ( #54971 ), #19915, .T. ) ;
#56446=DIRECTION ( 'NONE',  ( -1.000000000000000000, -1.224606353822377258E-16, -0.000000000000000000 ) ) ;
#56452=CIRCLE ( 'NONE', #99494, 4.000000000000000888 ) ;
#56477=EDGE_LOOP ( 'NONE', ( #11035, #77885, #30656, #24123, #91901, #78628 ) ) ;
#56479=CIRCLE ( 'NONE', #71967, 4.000000000000000888 ) ;
#56484=EDGE_LOOP ( 'NONE', ( #79933, #102080, #4214, #15726, #92550 ) ) ;
#56487=LINE ( 'NONE', #23630, #22502 ) ;
#56502=CARTESIAN_POINT ( 'NONE',  ( 37.33349330513379982, 4.898587196589405926E-16, -4.000000000000001776 ) ) ;
#56503=DIRECTION ( 'NONE',  ( -1.000000000000000000, -1.224606353822377258E-16, -0.000000000000000000 ) ) ;
#56507=FACE_OUTER_BOUND ( 'NONE', #18662, .T. ) ;
#56508=AXIS2_PLACEMENT_3D ( 'NONE', #59960, #68574, #44287 ) ;
#56516=EDGE_CURVE ( 'NONE', #29715, #100266, #100769, .T. ) ;
#56530=LINE ( 'NONE', #35499, #28850 ) ;
#56544=CIRCLE ( 'NONE', #23888, 4.000000000000001776 ) ;
#56637=EDGE_CURVE ( 'NONE', #55094, #52776, #50868, .T. ) ;
#56646=EDGE_CURVE ( 'NONE', #478, #18278, #92128, .T. ) ;
#56662=VERTEX_POINT ( 'NONE', #18276 ) ;
#56672=CARTESIAN_POINT ( 'NONE',  ( 9.833493305133801599, 4.000000000000002665, 0.000000000000000000 ) ) ;
#56690=ORIENTED_EDGE ( 'NONE', *, *, #104668, .T. ) ;
#56695=LINE ( 'NONE', #89086, #1179 ) ;
#56716=LINE ( 'NONE', #15204, #42021 ) ;
#56723=CARTESIAN_POINT ( 'NONE',  ( 22.33349330513380337, -7.703719777548943412E-31, 4.000000000000001776 ) ) ;
#56771=ORIENTED_EDGE ( 'NONE', *, *, #33542, .F. ) ;
#56781=B_SPLINE_CURVE_WITH_KNOTS ( 'NONE', 3,
 ( #21902, #87678, #13230, #38091, #44567 ),
 .UNSPECIFIED., .F., .F.,
 ( 4, 1, 4 ),
 ( 0.000000000000000000, 0.003752776749732567897, 0.007505553499465135794 ),
 .UNSPECIFIED. ) ;
#56793=DIRECTION ( 'NONE',  ( -1.000000000000000000, -0.000000000000000000, -0.000000000000000000 ) ) ;
#56798=DIRECTION ( 'NONE',  ( -1.000000000000000000, -0.000000000000000000, -0.000000000000000000 ) ) ;
#56845=DIRECTION ( 'NONE',  ( 0.5735764363510466035, -0.8191520442889914655, 1.003171929053524500E-16 ) ) ;
#56846=VERTEX_POINT ( 'NONE', #5262 ) ;
#56862=VERTEX_POINT ( 'NONE', #103940 ) ;
#56876=ORIENTED_EDGE ( 'NONE', *, *, #41468, .T. ) ;
#56888=AXIS2_PLACEMENT_3D ( 'NONE', #88269, #79101, #5225 ) ;
#56892=DIRECTION ( 'NONE',  ( 0.000000000000000000, -1.000000000000000000, 0.000000000000000000 ) ) ;
#56900=CARTESIAN_POINT ( 'NONE',  ( 0.5805565836007701153, -7.505553499465148271, -1.383738442504732931E-16 ) ) ;
#56904=B_SPLINE_CURVE_WITH_KNOTS ( 'NONE', 3,
 ( #73871, #16167, #65257, #72800, #49053, #66316, #81949, #32386, #1004, #82504 ),
 .UNSPECIFIED., .F., .F.,
 ( 4, 2, 2, 2, 4 ),
 ( 0.000000000000000000, 0.001993803085173304328, 0.003987606170346608657, 0.005981409255519914286, 0.007975212340693219049 ),
 .UNSPECIFIED. ) ;
#56915=FACE_OUTER_BOUND ( 'NONE', #30806, .T. ) ;
#56918=ORIENTED_EDGE ( 'NONE', *, *, #64914, .F. ) ;
#56927=EDGE_CURVE ( 'NONE', #77149, #19064, #946, .T. ) ;
#56929=VECTOR ( 'NONE', #63013, 1000.000000000000000 ) ;
#56957=EDGE_LOOP ( 'NONE', ( #5729, #64221, #80229, #15265, #97695, #86184 ) ) ;
#56968=CONICAL_SURFACE ( 'NONE', #13934, 4.000000000000001776, 0.9599310885968808105 ) ;
#56975=CYLINDRICAL_SURFACE ( 'NONE', #105269, 4.000000000000000000 ) ;
#56987=AXIS2_PLACEMENT_3D ( 'NONE', #83179, #26586, #42725 ) ;
#56998=EDGE_CURVE ( 'NONE', #87270, #58778, #99139, .T. ) ;
#57003=EDGE_CURVE ( 'NONE', #6290, #28486, #55892, .T. ) ;
#57033=DIRECTION ( 'NONE',  ( 0.000000000000000000, 0.000000000000000000, 1.000000000000000000 ) ) ;
#57071=CARTESIAN_POINT ( 'NONE',  ( 32.33349330513379982, 1.593028355512270567E-15, 0.000000000000000000 ) ) ;
#57079=ORIENTED_EDGE ( 'NONE', *, *, #39815, .F. ) ;
#57096=EDGE_CURVE ( 'NONE', #82432, #75817, #3942, .T. ) ;
#57107=DIRECTION ( 'NONE',  ( -1.000000000000000000, -1.224606353822377258E-16, -0.000000000000000000 ) ) ;
#57113=VERTEX_POINT ( 'NONE', #51414 ) ;
#57132=EDGE_LOOP ( 'NONE', ( #51622, #326, #65074, #102457, #16287 ) ) ;
#57157=DIRECTION ( 'NONE',  ( -1.000000000000000000, -1.224606353822377258E-16, -0.000000000000000000 ) ) ;
#57175=CARTESIAN_POINT ( 'NONE',  ( 6.289692432696780244, -0.6618655008720318866, 6.828989928337167115 ) ) ;
#57177=CARTESIAN_POINT ( 'NONE',  ( 31.08349330513380337, -4.000000000000000888, 4.898587196589416773E-16 ) ) ;
#57201=ORIENTED_EDGE ( 'NONE', *, *, #70494, .T. ) ;
#57216=EDGE_LOOP ( 'NONE', ( #101744, #15430, #71026, #92650, #42344 ) ) ;
#57241=CARTESIAN_POINT ( 'NONE',  ( 24.34999999999999787, -3.309499999999999886, 4.475777889183790779E-16 ) ) ;
#57256=LINE ( 'NONE', #42688, #81735 ) ;
#57303=FACE_OUTER_BOUND ( 'NONE', #31814, .T. ) ;
#57309=B_SPLINE_CURVE_WITH_KNOTS ( 'NONE', 3,
 ( #766, #17011, #25667, #66610, #10490, #91434 ),
 .UNSPECIFIED., .F., .F.,
 ( 4, 2, 4 ),
 ( -4.698498718846532140E-06, 0.0003457374136903327362, 0.0006961733260995119944 ),
 .UNSPECIFIED. ) ;
#57342=VECTOR ( 'NONE', #100867, 1000.000000000000114 ) ;
#57351=CARTESIAN_POINT ( 'NONE',  ( 16.08349330513380337, 4.898587196589405926E-16, -4.000000000000001776 ) ) ;
#57354=VECTOR ( 'NONE', #101085, 1000.000000000000000 ) ;
#57355=DIRECTION ( 'NONE',  ( 0.000000000000000000, -1.000000000000000000, 0.000000000000000000 ) ) ;
#57378=EDGE_CURVE ( 'NONE', #46114, #8430, #100932, .T. ) ;
#57447=ORIENTED_EDGE ( 'NONE', *, *, #27938, .T. ) ;
#57451=CONICAL_SURFACE ( 'NONE', #10947, 3.309500000000001663, 0.9599310885968770357 ) ;
#57460=DIRECTION ( 'NONE',  ( 0.000000000000000000, 0.000000000000000000, 1.000000000000000000 ) ) ;
#57472=DIRECTION ( 'NONE',  ( 0.000000000000000000, 1.000000000000000000, 0.000000000000000000 ) ) ;
#57487=CARTESIAN_POINT ( 'NONE',  ( 21.08349330513380337, -7.703719777548943412E-31, 4.000000000000001776 ) ) ;
#57498=ORIENTED_EDGE ( 'NONE', *, *, #92875, .F. ) ;
#57508=VERTEX_POINT ( 'NONE', #59406 ) ;
#57526=ORIENTED_EDGE ( 'NONE', *, *, #27868, .F. ) ;
#57550=CARTESIAN_POINT ( 'NONE',  ( 17.33349330513380337, 1.593028355512270567E-15, 0.000000000000000000 ) ) ;
#57552=ADVANCED_FACE ( 'NONE', ( #26011 ), #61455, .T. ) ;
#57556=CARTESIAN_POINT ( 'NONE',  ( 6.575925811255157072, 7.701774614579013800, -1.127145213565506199E-15 ) ) ;
#57588=DIRECTION ( 'NONE',  ( -0.5735764363510497121, 0.8191520442889892450, 1.003171929053521665E-16 ) ) ;
#57636=DIRECTION ( 'NONE',  ( 0.000000000000000000, 1.000000000000000000, 0.000000000000000000 ) ) ;
#57637=CONICAL_SURFACE ( 'NONE', #19840, 8.605212085995399107, 1.221730476396037490 ) ;
#57656=LINE ( 'NONE', #33425, #77689 ) ;
#57675=EDGE_CURVE ( 'NONE', #77299, #77294, #102788, .T. ) ;
#57683=EDGE_CURVE ( 'NONE', #32972, #24986, #83044, .T. ) ;
#57691=DIRECTION ( 'NONE',  ( -1.000000000000000000, -1.224606353822377258E-16, -0.000000000000000000 ) ) ;
#57692=VERTEX_POINT ( 'NONE', #89977 ) ;
#57695=CARTESIAN_POINT ( 'NONE',  ( 46.36650669486618881, 1.474610560812782335E-15, 0.000000000000000000 ) ) ;
#57715=DIRECTION ( 'NONE',  ( -0.5735764363510497121, 0.8191520442889892450, 1.003171929053521665E-16 ) ) ;
#57716=CIRCLE ( 'NONE', #88777, 4.000000000000000888 ) ;
#57726=LINE ( 'NONE', #49104, #1930 ) ;
#57736=DIRECTION ( 'NONE',  ( 0.000000000000000000, 0.000000000000000000, 1.000000000000000000 ) ) ;
#57738=DIRECTION ( 'NONE',  ( 0.000000000000000000, -1.000000000000000000, 0.000000000000000000 ) ) ;
#57742=EDGE_LOOP ( 'NONE', ( #4179, #88284, #21503, #83432, #23844 ) ) ;
#57765=VERTEX_POINT ( 'NONE', #96491 ) ;
#57791=AXIS2_PLACEMENT_3D ( 'NONE', #98522, #96940, #82345 ) ;
#57794=ORIENTED_EDGE ( 'NONE', *, *, #26870, .F. ) ;
#57805=CARTESIAN_POINT ( 'NONE',  ( 27.61650669486618881, 4.898587196589411843E-16, -4.000000000000000888 ) ) ;
#57823=DIRECTION ( 'NONE',  ( 0.000000000000000000, 0.000000000000000000, 1.000000000000000000 ) ) ;
#57834=AXIS2_PLACEMENT_3D ( 'NONE', #82952, #9047, #59221 ) ;
#57835=LINE ( 'NONE', #79606, #11156 ) ;
#57869=COLOUR_RGB ( '', 0.31764706, 0.68627451, 0.89019608) ;
#57872=AXIS2_PLACEMENT_3D ( 'NONE', #22831, #65385, #56192 ) ;
#57881=VERTEX_POINT ( 'NONE', #62533 ) ;
#57888=ORIENTED_EDGE ( 'NONE', *, *, #27558, .F. ) ;
#57905=CONICAL_SURFACE ( 'NONE', #81996, 4.000000000000001776, 0.9599310885968808105 ) ;
#57972=ADVANCED_FACE ( 'NONE', ( #80816 ), #16623, .T. ) ;
#57974=EDGE_CURVE ( 'NONE', #2814, #7688, #32300, .T. ) ;
#57980=DIRECTION ( 'NONE',  ( -1.000000000000000000, -1.224606353822377258E-16, -0.000000000000000000 ) ) ;
#58025=FACE_OUTER_BOUND ( 'NONE', #56484, .T. ) ;
#58031=DIRECTION ( 'NONE',  ( -1.000000000000000000, -1.224606353822377258E-16, -0.000000000000000000 ) ) ;
#58055=EDGE_CURVE ( 'NONE', #57692, #74342, #47386, .T. ) ;
#58070=CARTESIAN_POINT ( 'NONE',  ( 40.59999999999999432, 1.533819458162526451E-15, 0.000000000000000000 ) ) ;
#58076=VERTEX_POINT ( 'NONE', #15017 ) ;
#58092=CARTESIAN_POINT ( 'NONE',  ( 5.947762761376477414, 2.501851166488378908, 6.500000000000000000 ) ) ;
#58100=EDGE_CURVE ( 'NONE', #62536, #40876, #56530, .T. ) ;
#58104=EDGE_CURVE ( 'NONE', #35426, #63670, #11168, .T. ) ;
#58105=DIRECTION ( 'NONE',  ( -1.000000000000000000, -1.224606353822377258E-16, -0.000000000000000000 ) ) ;
#58114=CARTESIAN_POINT ( 'NONE',  ( 0.000000000000000000, 0.000000000000000000, 0.000000000000000000 ) ) ;
#58115=CIRCLE ( 'NONE', #61699, 3.309500000000001663 ) ;
#58120=CARTESIAN_POINT ( 'NONE',  ( 36.36650669486618881, 4.898587196589411843E-16, -4.000000000000000888 ) ) ;
#58122=EDGE_CURVE ( 'NONE', #6711, #3694, #104542, .T. ) ;
#58127=CIRCLE ( 'NONE', #20323, 4.000000000000000888 ) ;
#58130=CARTESIAN_POINT ( 'NONE',  ( 35.59999999999999432, -3.309499999999999886, 4.475777889183790779E-16 ) ) ;
#58148=DIRECTION ( 'NONE',  ( 0.000000000000000000, -1.000000000000000000, 0.000000000000000000 ) ) ;
#58162=ORIENTED_EDGE ( 'NONE', *, *, #77990, .T. ) ;
#58172=DIRECTION ( 'NONE',  ( 0.000000000000000000, -1.000000000000000000, 0.000000000000000000 ) ) ;
#58178=CARTESIAN_POINT ( 'NONE',  ( 13.58349330513380160, 4.000000000000003553, 0.000000000000000000 ) ) ;
#58213=CONICAL_SURFACE ( 'NONE', #72003, 8.605212085995399107, 1.221730476396037490 ) ;
#58215=DIRECTION ( 'NONE',  ( -1.000000000000000000, -1.224606353822377258E-16, -0.000000000000000000 ) ) ;
#58238=AXIS2_PLACEMENT_3D ( 'NONE', #42969, #859, #41892 ) ;
#58240=ORIENTED_EDGE ( 'NONE', *, *, #71398, .T. ) ;
#58293=ORIENTED_EDGE ( 'NONE', *, *, #65113, .T. ) ;
#58305=CARTESIAN_POINT ( 'NONE',  ( 46.08349330513379982, 1.593028355512270567E-15, 0.000000000000000000 ) ) ;
#58309=AXIS2_PLACEMENT_3D ( 'NONE', #30393, #103203, #78914 ) ;
#58316=ORIENTED_EDGE ( 'NONE', *, *, #95625, .T. ) ;
#58324=DIRECTION ( 'NONE',  ( -1.000000000000000000, -1.224606353822377258E-16, -0.000000000000000000 ) ) ;
#58325=ORIENTED_EDGE ( 'NONE', *, *, #55675, .T. ) ;
#58362=ORIENTED_EDGE ( 'NONE', *, *, #12233, .T. ) ;
#58395=LINE ( 'NONE', #17949, #63000 ) ;
#58501=EDGE_LOOP ( 'NONE', ( #83998, #96230, #40646, #39504, #63772, #43903 ) ) ;
#58533=EDGE_CURVE ( 'NONE', #444, #31074, #32273, .T. ) ;
#58553=CIRCLE ( 'NONE', #105053, 4.000000000000000888 ) ;
#58558=CIRCLE ( 'NONE', #41293, 4.000000000000001776 ) ;
#58560=CYLINDRICAL_SURFACE ( 'NONE', #102912, 4.000000000000000000 ) ;
#58580=DIRECTION ( 'NONE',  ( 0.000000000000000000, -1.000000000000000000, 0.000000000000000000 ) ) ;
#58594=DIRECTION ( 'NONE',  ( 0.000000000000000000, 1.000000000000000000, 0.000000000000000000 ) ) ;
#58600=CARTESIAN_POINT ( 'NONE',  ( 46.36650669486618881, -3.851859888774471706E-31, 4.000000000000000888 ) ) ;
#58613=ORIENTED_EDGE ( 'NONE', *, *, #42895, .F. ) ;
#58675=EDGE_CURVE ( 'NONE', #21525, #42491, #61767, .T. ) ;
#58688=CARTESIAN_POINT ( 'NONE',  ( 46.08349330513379982, -4.000000000000000000, 4.898587196589415787E-16 ) ) ;
#58694=FACE_OUTER_BOUND ( 'NONE', #37775, .T. ) ;
#58696=DIRECTION ( 'NONE',  ( 0.000000000000000000, 0.000000000000000000, 1.000000000000000000 ) ) ;
#58703=FACE_OUTER_BOUND ( 'NONE', #12139, .T. ) ;
#58706=VECTOR ( 'NONE', #104596, 1000.000000000000000 ) ;
#58711=CARTESIAN_POINT ( 'NONE',  ( 28.58349330513380337, -4.000000000000000888, 4.898587196589416773E-16 ) ) ;
#58715=B_SPLINE_CURVE_WITH_KNOTS ( 'NONE', 3,
 ( #54716, #38066, #15335, #32075, #55766, #96283 ),
 .UNSPECIFIED., .F., .F.,
 ( 4, 2, 4 ),
 ( 0.02294124189192014995, 0.02484059228024679961, 0.02673994266857345273 ),
 .UNSPECIFIED. ) ;
#58721=CARTESIAN_POINT ( 'NONE',  ( 29.83349330513380337, 4.898587196589405926E-16, -4.000000000000001776 ) ) ;
#58727=AXIS2_PLACEMENT_3D ( 'NONE', #6539, #79902, #32452 ) ;
#58733=AXIS2_PLACEMENT_3D ( 'NONE', #62323, #5137, #22934 ) ;
#58736=LINE ( 'NONE', #3146, #31073 ) ;
#58749=DIRECTION ( 'NONE',  ( 0.000000000000000000, -1.000000000000000000, 0.000000000000000000 ) ) ;
#58757=ORIENTED_EDGE ( 'NONE', *, *, #104559, .F. ) ;
#58764=VERTEX_POINT ( 'NONE', #86573 ) ;
#58778=VERTEX_POINT ( 'NONE', #37505 ) ;
#58794=ORIENTED_EDGE ( 'NONE', *, *, #82665, .F. ) ;
#58806=EDGE_CURVE ( 'NONE', #30981, #105946, #54684, .T. ) ;
#58810=AXIS2_PLACEMENT_3D ( 'NONE', #105288, #94568, #22806 ) ;
#58828=ORIENTED_EDGE ( 'NONE', *, *, #49537, .F. ) ;
#58839=CARTESIAN_POINT ( 'NONE',  ( 33.58349330513379982, -4.000000000000000000, 4.898587196589415787E-16 ) ) ;
#58847=AXIS2_PLACEMENT_3D ( 'NONE', #101884, #2648, #45262 ) ;
#58853=EDGE_LOOP ( 'NONE', ( #77009, #37930, #79690, #45000, #27654 ) ) ;
#58863=CIRCLE ( 'NONE', #79483, 4.000000000000001776 ) ;
#58904=CARTESIAN_POINT ( 'NONE',  ( 8.866506694866188809, 1.474610560812782335E-15, 0.000000000000000000 ) ) ;
#58908=LINE ( 'NONE', #91799, #32189 ) ;
#58938=CARTESIAN_POINT ( 'NONE',  ( 34.35000000000000142, -3.309499999999999886, 0.000000000000000000 ) ) ;
#58967=AXIS2_PLACEMENT_3D ( 'NONE', #48260, #96840, #89279 ) ;
#58995=DIRECTION ( 'NONE',  ( 0.000000000000000000, 1.000000000000000000, 0.000000000000000000 ) ) ;
#58997=CARTESIAN_POINT ( 'NONE',  ( 13.09999999999999787, -3.309499999999999886, 0.000000000000000000 ) ) ;
#59000=CONICAL_SURFACE ( 'NONE', #17662, 4.000000000000001776, 0.9599310885968808105 ) ;
#59039=CARTESIAN_POINT ( 'NONE',  ( 39.34999999999999432, -3.309499999999999886, 4.475777889183790779E-16 ) ) ;
#59068=CARTESIAN_POINT ( 'NONE',  ( 38.58349330513380693, 1.593028355512270567E-15, 0.000000000000000000 ) ) ;
#59081=ORIENTED_EDGE ( 'NONE', *, *, #42553, .T. ) ;
#59090=CARTESIAN_POINT ( 'NONE',  ( 21.08349330513380337, 1.593028355512270567E-15, 0.000000000000000000 ) ) ;
#59093=LINE ( 'NONE', #69317, #67513 ) ;
#59096=EDGE_CURVE ( 'NONE', #64859, #18717, #89234, .T. ) ;
#59100=DIRECTION ( 'NONE',  ( -1.000000000000000000, -0.000000000000000000, -0.000000000000000000 ) ) ;
#59102=CIRCLE ( 'NONE', #36734, 4.000000000000000888 ) ;
#59135=VERTEX_POINT ( 'NONE', #41439 ) ;
#59139=DIRECTION ( 'NONE',  ( 0.000000000000000000, 0.000000000000000000, 1.000000000000000000 ) ) ;
#59157=AXIS2_PLACEMENT_3D ( 'NONE', #92234, #34051, #57736 ) ;
#59164=ADVANCED_FACE ( 'NONE', ( #22236 ), #81343, .F. ) ;
#59169=CARTESIAN_POINT ( 'NONE',  ( 21.36650669486618881, 1.474610560812782335E-15, 0.000000000000000000 ) ) ;
#59177=VERTEX_POINT ( 'NONE', #2034 ) ;
#59180=CARTESIAN_POINT ( 'NONE',  ( 5.819846122303830249, 6.321060697775074289, -2.051601713726794785 ) ) ;
#59183=AXIS2_PLACEMENT_3D ( 'NONE', #10616, #58105, #74811 ) ;
#59209=CARTESIAN_POINT ( 'NONE',  ( 0.000000000000000000, 0.000000000000000000, 4.000000000000000000 ) ) ;
#59218=B_SPLINE_CURVE_WITH_KNOTS ( 'NONE', 3,
 ( #12900, #79244, #272, #87355, #15434, #97949 ),
 .UNSPECIFIED., .F., .F.,
 ( 4, 2, 4 ),
 ( 2.380733003139562229E-07, 0.001898835937927373114, 0.003797433802554431997 ),
 .UNSPECIFIED. ) ;
#59221=DIRECTION ( 'NONE',  ( 0.000000000000000000, -1.000000000000000000, 0.000000000000000000 ) ) ;
#59228=ADVANCED_FACE ( 'NONE', ( #58703 ), #65129, .T. ) ;
#59250=EDGE_LOOP ( 'NONE', ( #28887, #67511, #79948, #42795, #57526, #14404 ) ) ;
#59258=CARTESIAN_POINT ( 'NONE',  ( -4.336808689942017736E-16, 0.6351314446054990848, -6.500000000000000000 ) ) ;
#59265=CARTESIAN_POINT ( 'NONE',  ( 47.33349330513379982, 1.593028355512270567E-15, 0.000000000000000000 ) ) ;
#59289=ORIENTED_EDGE ( 'NONE', *, *, #80046, .T. ) ;
#59297=CARTESIAN_POINT ( 'NONE',  ( 39.83349330513380693, 1.593028355512270567E-15, 0.000000000000000000 ) ) ;
#59324=ORIENTED_EDGE ( 'NONE', *, *, #53722, .F. ) ;
#59344=EDGE_CURVE ( 'NONE', #6924, #79431, #13216, .T. ) ;
#59351=EDGE_CURVE ( 'NONE', #54223, #87110, #17591, .T. ) ;
#59352=ORIENTED_EDGE ( 'NONE', *, *, #29778, .T. ) ;
#59361=AXIS2_PLACEMENT_3D ( 'NONE', #29096, #38222, #63546 ) ;
#59405=CYLINDRICAL_SURFACE ( 'NONE', #71274, 4.000000000000000000 ) ;
#59406=CARTESIAN_POINT ( 'NONE',  ( 14.83349330513380337, 4.898587196589405926E-16, -4.000000000000001776 ) ) ;
#59469=AXIS2_PLACEMENT_3D ( 'NONE', #30292, #45930, #62653 ) ;
#59479=CARTESIAN_POINT ( 'NONE',  ( 0.000000000000000000, 0.000000000000000000, 0.000000000000000000 ) ) ;
#59487=FACE_OUTER_BOUND ( 'NONE', #98605, .T. ) ;
#59496=FACE_OUTER_BOUND ( 'NONE', #64502, .T. ) ;
#59509=CARTESIAN_POINT ( 'NONE',  ( 0.000000000000000000, 0.000000000000000000, 0.000000000000000000 ) ) ;
#59528=ORIENTED_EDGE ( 'NONE', *, *, #79860, .F. ) ;
#59544=ADVANCED_FACE ( 'NONE', ( #28359 ), #97588, .T. ) ;
#59552=VERTEX_POINT ( 'NONE', #53138 ) ;
#59572=VERTEX_POINT ( 'NONE', #86056 ) ;
#59616=DIRECTION ( 'NONE',  ( 0.000000000000000000, -1.000000000000000000, 0.000000000000000000 ) ) ;
#59636=FACE_OUTER_BOUND ( 'NONE', #69463, .T. ) ;
#59656=EDGE_CURVE ( 'NONE', #13309, #44189, #90766, .T. ) ;
#59674=DIRECTION ( 'NONE',  ( -1.000000000000000000, -0.000000000000000000, -0.000000000000000000 ) ) ;
#59677=CARTESIAN_POINT ( 'NONE',  ( 38.86650669486618881, 4.898587196589411843E-16, -4.000000000000000888 ) ) ;
#59686=CARTESIAN_POINT ( 'NONE',  ( 6.333820801329741457, 6.982605850968585770, 0.9057718968909901358 ) ) ;
#59699=ORIENTED_EDGE ( 'NONE', *, *, #50323, .F. ) ;
#59707=ADVANCED_FACE ( 'NONE', ( #7744 ), #105396, .T. ) ;
#59722=DIRECTION ( 'NONE',  ( -1.000000000000000000, -1.224606353822377258E-16, -0.000000000000000000 ) ) ;
#59727=ORIENTED_EDGE ( 'NONE', *, *, #62626, .T. ) ;
#59744=EDGE_CURVE ( 'NONE', #56662, #54299, #1257, .T. ) ;
#59761=CIRCLE ( 'NONE', #28766, 4.000000000000000888 ) ;
#59763=CARTESIAN_POINT ( 'NONE',  ( 37.61650669486618881, 1.474610560812782335E-15, 0.000000000000000000 ) ) ;
#59773=VERTEX_POINT ( 'NONE', #57351 ) ;
#59793=ADVANCED_FACE ( 'NONE', ( #67600 ), #104606, .T. ) ;
#59794=ADVANCED_FACE ( 'NONE', ( #100478 ), #9329, .T. ) ;
#59795=CARTESIAN_POINT ( 'NONE',  ( 17.61650669486618881, -3.851859888774471706E-31, 4.000000000000000888 ) ) ;
#59805=DIRECTION ( 'NONE',  ( -1.000000000000000000, -1.224606353822377258E-16, -0.000000000000000000 ) ) ;
#59861=AXIS2_PLACEMENT_3D ( 'NONE', #13107, #5042, #99749 ) ;
#59896=ADVANCED_FACE ( 'NONE', ( #4444 ), #35755, .T. ) ;
#59897=ORIENTED_EDGE ( 'NONE', *, *, #83486, .F. ) ;
#59907=CARTESIAN_POINT ( 'NONE',  ( 17.61650669486618881, 4.898587196589411843E-16, -4.000000000000000888 ) ) ;
#59912=CARTESIAN_POINT ( 'NONE',  ( 6.289692432696789126, 0.6629690750393447685, 6.828989928337166226 ) ) ;
#59928=ORIENTED_EDGE ( 'NONE', *, *, #4941, .F. ) ;
#59942=ORIENTED_EDGE ( 'NONE', *, *, #23113, .F. ) ;
#59960=CARTESIAN_POINT ( 'NONE',  ( 26.08349330513380337, 1.593028355512270567E-15, 0.000000000000000000 ) ) ;
#59971=EDGE_CURVE ( 'NONE', #49207, #101661, #71895, .T. ) ;
#59984=FACE_OUTER_BOUND ( 'NONE', #88404, .T. ) ;
#59985=EDGE_CURVE ( 'NONE', #62536, #73940, #8128, .T. ) ;
#59996=AXIS2_PLACEMENT_3D ( 'NONE', #89492, #82453, #9609 ) ;
#60019=CARTESIAN_POINT ( 'NONE',  ( 22.33349330513380337, 1.593028355512270567E-15, 0.000000000000000000 ) ) ;
#60020=DIRECTION ( 'NONE',  ( 0.000000000000000000, 0.000000000000000000, 1.000000000000000000 ) ) ;
#60051=ADVANCED_FACE ( 'NONE', ( #39485 ), #94319, .T. ) ;
#60053=CONICAL_SURFACE ( 'NONE', #49694, 3.309500000000001663, 0.9599310885968770357 ) ;
#60062=DIRECTION ( 'NONE',  ( -1.000000000000000000, -0.000000000000000000, -0.000000000000000000 ) ) ;
#60068=ORIENTED_EDGE ( 'NONE', *, *, #34746, .F. ) ;
#60085=CARTESIAN_POINT ( 'NONE',  ( 29.83349330513380337, 1.593028355512270567E-15, 0.000000000000000000 ) ) ;
#60099=EDGE_CURVE ( 'NONE', #33845, #98395, #47772, .T. ) ;
#60100=CARTESIAN_POINT ( 'NONE',  ( 14.83349330513380337, -7.703719777548943412E-31, 4.000000000000001776 ) ) ;
#60102=EDGE_CURVE ( 'NONE', #86885, #6164, #61606, .T. ) ;
#60105=CARTESIAN_POINT ( 'NONE',  ( 9.349999999999997868, -3.309499999999999886, 4.475777889183790779E-16 ) ) ;
#60113=EDGE_CURVE ( 'NONE', #103513, #9744, #102854, .T. ) ;
#60121=VERTEX_POINT ( 'NONE', #80970 ) ;
#60123=CARTESIAN_POINT ( 'NONE',  ( 6.692588830498428010, -3.932766476276041256, -6.892929031562515796 ) ) ;
#60137=CARTESIAN_POINT ( 'NONE',  ( 11.08349330513380160, 4.000000000000003553, 0.000000000000000000 ) ) ;
#60138=ORIENTED_EDGE ( 'NONE', *, *, #86349, .F. ) ;
#60146=EDGE_LOOP ( 'NONE', ( #21882, #104956, #61943, #104792, #98169, #21332 ) ) ;
#60152=EDGE_CURVE ( 'NONE', #57765, #52893, #56695, .T. ) ;
#60156=VECTOR ( 'NONE', #17696, 1000.000000000000000 ) ;
#60162=ORIENTED_EDGE ( 'NONE', *, *, #8255, .T. ) ;
#60168=EDGE_LOOP ( 'NONE', ( #84388, #32780, #79983, #6956, #30372 ) ) ;
#60173=DIRECTION ( 'NONE',  ( 0.000000000000000000, -1.000000000000000000, 0.000000000000000000 ) ) ;
#60183=ORIENTED_EDGE ( 'NONE', *, *, #9605, .F. ) ;
#60237=VERTEX_POINT ( 'NONE', #32466 ) ;
#60265=AXIS2_PLACEMENT_3D ( 'NONE', #95611, #3952, #30365 ) ;
#60301=DIRECTION ( 'NONE',  ( -1.000000000000000000, -0.000000000000000000, -0.000000000000000000 ) ) ;
#60303=EDGE_CURVE ( 'NONE', #32012, #76835, #80574, .T. ) ;
#60318=CARTESIAN_POINT ( 'NONE',  ( -7.585180042662256578E-16, 0.6351314446025488891, 6.500000000000000000 ) ) ;
#60336=CARTESIAN_POINT ( 'NONE',  ( 39.34999999999999432, 1.533819458162526451E-15, 0.000000000000000000 ) ) ;
#60363=CARTESIAN_POINT ( 'NONE',  ( 43.86650669486618881, 1.474610560812782335E-15, 0.000000000000000000 ) ) ;
#60365=VERTEX_POINT ( 'NONE', #35127 ) ;
#60381=DIRECTION ( 'NONE',  ( 0.000000000000000000, 1.000000000000000000, 0.000000000000000000 ) ) ;
#60385=EDGE_CURVE ( 'NONE', #2149, #76395, #68517, .T. ) ;
#60399=CARTESIAN_POINT ( 'NONE',  ( 24.83349330513380337, 4.898587196589405926E-16, -4.000000000000001776 ) ) ;
#60421=CIRCLE ( 'NONE', #36340, 4.000000000000001776 ) ;
#60425=DIRECTION ( 'NONE',  ( -1.000000000000000000, -0.000000000000000000, -0.000000000000000000 ) ) ;
#60439=CARTESIAN_POINT ( 'NONE',  ( 18.09999999999999787, 1.533819458162526451E-15, 0.000000000000000000 ) ) ;
#60457=VERTEX_POINT ( 'NONE', #95456 ) ;
#60487=CIRCLE ( 'NONE', #58847, 4.000000000000000888 ) ;
#60545=CARTESIAN_POINT ( 'NONE',  ( 45.11650669486618881, 4.898587196589411843E-16, -4.000000000000000888 ) ) ;
#60560=AXIS2_PLACEMENT_3D ( 'NONE', #72611, #24100, #73122 ) ;
#60577=ADVANCED_FACE ( 'NONE', ( #43715 ), #49555, .T. ) ;
#60586=CARTESIAN_POINT ( 'NONE',  ( 11.08349330513380160, 4.000000000000002665, 0.000000000000000000 ) ) ;
#60604=ORIENTED_EDGE ( 'NONE', *, *, #57675, .T. ) ;
#60648=DIRECTION ( 'NONE',  ( -1.000000000000000000, -0.000000000000000000, -0.000000000000000000 ) ) ;
#60649=DIRECTION ( 'NONE',  ( -1.000000000000000000, -1.224606353822377258E-16, -0.000000000000000000 ) ) ;
#60652=DIRECTION ( 'NONE',  ( 0.000000000000000000, -0.8660254037844380415, 0.5000000000000012212 ) ) ;
#60661=LINE ( 'NONE', #104266, #32164 ) ;
#60678=LINE ( 'NONE', #45023, #12065 ) ;
#60692=DIRECTION ( 'NONE',  ( -1.000000000000000000, -1.224606353822377258E-16, -0.000000000000000000 ) ) ;
#60724=FACE_OUTER_BOUND ( 'NONE', #32483, .T. ) ;
#60742=ORIENTED_EDGE ( 'NONE', *, *, #13559, .T. ) ;
#60751=ORIENTED_EDGE ( 'NONE', *, *, #102647, .T. ) ;
#60768=ORIENTED_EDGE ( 'NONE', *, *, #39167, .F. ) ;
#60776=DIRECTION ( 'NONE',  ( -1.000000000000000000, -0.000000000000000000, -0.000000000000000000 ) ) ;
#60782=DIRECTION ( 'NONE',  ( 0.000000000000000000, -1.000000000000000000, 0.000000000000000000 ) ) ;
#60784=AXIS2_PLACEMENT_3D ( 'NONE', #18291, #91112, #1526 ) ;
#60786=LINE ( 'NONE', #36536, #37278 ) ;
#60806=CARTESIAN_POINT ( 'NONE',  ( 27.33349330513380337, 4.000000000000003553, 0.000000000000000000 ) ) ;
#60841=CARTESIAN_POINT ( 'NONE',  ( 0.000000000000000000, 0.000000000000000000, 0.000000000000000000 ) ) ;
#60855=DIRECTION ( 'NONE',  ( 0.000000000000000000, -1.000000000000000000, 0.000000000000000000 ) ) ;
#60861=FACE_OUTER_BOUND ( 'NONE', #34996, .T. ) ;
#60886=ORIENTED_EDGE ( 'NONE', *, *, #83556, .T. ) ;
#60903=CARTESIAN_POINT ( 'NONE',  ( 6.172110426326448795, -1.395451528107565675, 6.499999999999999112 ) ) ;
#60917=CARTESIAN_POINT ( 'NONE',  ( 0.000000000000000000, 0.000000000000000000, 4.000000000000000000 ) ) ;
#60923=DIRECTION ( 'NONE',  ( 0.000000000000000000, 1.000000000000000000, 0.000000000000000000 ) ) ;
#60931=CARTESIAN_POINT ( 'NONE',  ( 8.099999999999999645, -7.505553499465148271, 0.000000000000000000 ) ) ;
#60949=FACE_OUTER_BOUND ( 'NONE', #19699, .T. ) ;
#60963=DIRECTION ( 'NONE',  ( 0.000000000000000000, -1.000000000000000000, 0.000000000000000000 ) ) ;
#60970=DIRECTION ( 'NONE',  ( -1.000000000000000000, -1.224606353822377258E-16, -0.000000000000000000 ) ) ;
#60976=ORIENTED_EDGE ( 'NONE', *, *, #40478, .F. ) ;
#60986=CARTESIAN_POINT ( 'NONE',  ( 21.08349330513380337, 4.898587196589405926E-16, -4.000000000000001776 ) ) ;
#60988=DIRECTION ( 'NONE',  ( -1.000000000000000000, -0.000000000000000000, -0.000000000000000000 ) ) ;
#60996=ORIENTED_EDGE ( 'NONE', *, *, #24281, .F. ) ;
#61023=ORIENTED_EDGE ( 'NONE', *, *, #48976, .F. ) ;
#61032=DIRECTION ( 'NONE',  ( 1.000000000000000000, 0.000000000000000000, 0.000000000000000000 ) ) ;
#61037=EDGE_CURVE ( 'NONE', #30981, #80889, #32421, .T. ) ;
#61041=ORIENTED_EDGE ( 'NONE', *, *, #34419, .T. ) ;
#61044=FACE_OUTER_BOUND ( 'NONE', #92459, .T. ) ;
#61064=FILL_AREA_STYLE ('',( #35752 ) ) ;
#61078=ORIENTED_EDGE ( 'NONE', *, *, #88829, .T. ) ;
#61079=DIRECTION ( 'NONE',  ( 0.000000000000000000, -1.000000000000000000, 0.000000000000000000 ) ) ;
#61083=ORIENTED_EDGE ( 'NONE', *, *, #56058, .F. ) ;
#61104=DIRECTION ( 'NONE',  ( 0.000000000000000000, 1.000000000000000000, 0.000000000000000000 ) ) ;
#61107=CARTESIAN_POINT ( 'NONE',  ( 0.000000000000000000, 4.898587196589412829E-16, -4.000000000000000000 ) ) ;
#61193=DIRECTION ( 'NONE',  ( -1.000000000000000000, -1.224606353822377258E-16, -0.000000000000000000 ) ) ;
#61237=DIRECTION ( 'NONE',  ( 0.000000000000000000, -1.000000000000000000, 0.000000000000000000 ) ) ;
#61302=VERTEX_POINT ( 'NONE', #34750 ) ;
#61305=ORIENTED_EDGE ( 'NONE', *, *, #11543, .F. ) ;
#61314=CARTESIAN_POINT ( 'NONE',  ( 6.683837171061805194, -3.955946848495972556, -6.851900933636989599 ) ) ;
#61328=DIRECTION ( 'NONE',  ( 0.5735764363510466035, -0.8191520442889914655, 1.003171929053524500E-16 ) ) ;
#61347=EDGE_CURVE ( 'NONE', #3694, #100024, #40247, .T. ) ;
#61349=DIRECTION ( 'NONE',  ( -0.5735764363510494901, -0.8191520442889894671, 0.000000000000000000 ) ) ;
#61364=AXIS2_PLACEMENT_3D ( 'NONE', #1984, #69407, #92597 ) ;
#61370=CARTESIAN_POINT ( 'NONE',  ( 28.09999999999999787, -3.309499999999999886, 0.000000000000000000 ) ) ;
#61380=ORIENTED_EDGE ( 'NONE', *, *, #32550, .T. ) ;
#61382=ORIENTED_EDGE ( 'NONE', *, *, #72780, .T. ) ;
#61386=DIRECTION ( 'NONE',  ( -1.000000000000000000, -1.224606353822377258E-16, -0.000000000000000000 ) ) ;
#61426=EDGE_CURVE ( 'NONE', #44463, #45750, #66117, .T. ) ;
#61427=ORIENTED_EDGE ( 'NONE', *, *, #10621, .F. ) ;
#61455=CONICAL_SURFACE ( 'NONE', #14911, 3.309500000000001663, 0.9599310885968770357 ) ;
#61482=ORIENTED_EDGE ( 'NONE', *, *, #26457, .T. ) ;
#61492=EDGE_CURVE ( 'NONE', #76319, #77337, #56716, .T. ) ;
#61498=ORIENTED_EDGE ( 'NONE', *, *, #7883, .T. ) ;
#61500=CARTESIAN_POINT ( 'NONE',  ( 34.83349330513379982, 1.593028355512270567E-15, 0.000000000000000000 ) ) ;
#61508=B_SPLINE_CURVE_WITH_KNOTS ( 'NONE', 3,
 ( #44981, #102668, #77864, #1821, #104785 ),
 .UNSPECIFIED., .F., .F.,
 ( 4, 1, 4 ),
 ( 6.258780363497294494E-20, 0.003752776749732572668, 0.007505553499465145335 ),
 .UNSPECIFIED. ) ;
#61514=ORIENTED_EDGE ( 'NONE', *, *, #105270, .T. ) ;
#61527=AXIS2_PLACEMENT_3D ( 'NONE', #28773, #29297, #61652 ) ;
#61532=ORIENTED_EDGE ( 'NONE', *, *, #45301, .T. ) ;
#61534=CONICAL_SURFACE ( 'NONE', #46048, 4.000000000000001776, 0.9599310885968808105 ) ;
#61569=VECTOR ( 'NONE', #36754, 1000.000000000000000 ) ;
#61589=ORIENTED_EDGE ( 'NONE', *, *, #61426, .F. ) ;
#61594=VERTEX_POINT ( 'NONE', #76090 ) ;
#61603=ORIENTED_EDGE ( 'NONE', *, *, #99371, .T. ) ;
#61604=( NAMED_UNIT ( * ) PLANE_ANGLE_UNIT ( ) SI_UNIT ( $, .RADIAN. ) );
#61606=CIRCLE ( 'NONE', #89064, 3.309500000000001663 ) ;
#61610=CYLINDRICAL_SURFACE ( 'NONE', #13799, 4.000000000000000000 ) ;
#61611=FACE_OUTER_BOUND ( 'NONE', #1878, .T. ) ;
#61618=LINE ( 'NONE', #85338, #55168 ) ;
#61622=DIRECTION ( 'NONE',  ( -1.000000000000000000, -0.000000000000000000, -0.000000000000000000 ) ) ;
#61652=DIRECTION ( 'NONE',  ( 0.000000000000000000, -1.000000000000000000, 0.000000000000000000 ) ) ;
#61657=EDGE_CURVE ( 'NONE', #89196, #5935, #68467, .T. ) ;
#61668=VERTEX_POINT ( 'NONE', #68010 ) ;
#61672=ORIENTED_EDGE ( 'NONE', *, *, #37648, .T. ) ;
#61677=ADVANCED_FACE ( 'NONE', ( #1662 ), #59405, .T. ) ;
#61695=DIRECTION ( 'NONE',  ( 0.000000000000000000, 0.000000000000000000, 1.000000000000000000 ) ) ;
#61697=DIRECTION ( 'NONE',  ( -1.000000000000000000, -1.224606353822377258E-16, -0.000000000000000000 ) ) ;
#61699=AXIS2_PLACEMENT_3D ( 'NONE', #88213, #32649, #48253 ) ;
#61702=DIRECTION ( 'NONE',  ( -1.000000000000000000, -1.224606353822377258E-16, -0.000000000000000000 ) ) ;
#61704=ORIENTED_EDGE ( 'NONE', *, *, #70250, .F. ) ;
#61712=CIRCLE ( 'NONE', #15160, 4.000000000000001776 ) ;
#61715=CARTESIAN_POINT ( 'NONE',  ( 45.11650669486618881, 1.474610560812782335E-15, 0.000000000000000000 ) ) ;
#61767=LINE ( 'NONE', #93583, #46049 ) ;
#61788=ADVANCED_FACE ( 'NONE', ( #10567 ), #42949, .T. ) ;
#61798=CARTESIAN_POINT ( 'NONE',  ( 42.33349330513380693, 4.898587196589405926E-16, -4.000000000000001776 ) ) ;
#61806=VERTEX_POINT ( 'NONE', #20329 ) ;
#61841=CARTESIAN_POINT ( 'NONE',  ( 31.84999999999999787, -3.309499999999999886, 0.000000000000000000 ) ) ;
#61850=DIRECTION ( 'NONE',  ( -1.000000000000000000, -1.224606353822377258E-16, -0.000000000000000000 ) ) ;
#61854=DIRECTION ( 'NONE',  ( 0.000000000000000000, -1.000000000000000000, 0.000000000000000000 ) ) ;
#61864=CARTESIAN_POINT ( 'NONE',  ( 24.34999999999999787, 1.533819458162526451E-15, 0.000000000000000000 ) ) ;
#61883=( BOUNDED_SURFACE ( )  B_SPLINE_SURFACE ( 3, 2, ( 
 ( #17634, #50494, #10579 ),
 ( #67765, #34900, #86101 ),
 ( #100652, #53702, #94172 ),
 ( #26812, #43494, #20869 ),
 ( #20337, #59686, #51570 ),
 ( #68303, #76371, #101722 ) ),
 .UNSPECIFIED., .F., .F., .F. ) 
 B_SPLINE_SURFACE_WITH_KNOTS ( ( 4, 2, 4 ),
 ( 3, 3 ),
 ( 0.003199762745115999809, 0.007302762474435751071, 0.01140576220375550190 ),
 ( 0.000000000000000000, 1.000000000000000000 ),
 .UNSPECIFIED. ) 
 GEOMETRIC_REPRESENTATION_ITEM ( )  RATIONAL_B_SPLINE_SURFACE ( (
 ( 1.000000000000000000, 0.8047731410850422762, 1.000000000000000000),
 ( 1.000000000000000000, 0.8125552299159720659, 1.000000000000000000),
 ( 1.000000000000000000, 0.8191520442885290576, 1.000000000000000000),
 ( 1.000000000000000000, 0.8191520442894507648, 1.000000000000000000),
 ( 1.000000000000000000, 0.8125552299152799529, 1.000000000000000000),
 ( 1.000000000000000000, 0.8047731410850428313, 1.000000000000000000) ) ) 
 REPRESENTATION_ITEM ( '' )  SURFACE ( )  );
#61915=CYLINDRICAL_SURFACE ( 'NONE', #98011, 4.000000000000000000 ) ;
#61929=ORIENTED_EDGE ( 'NONE', *, *, #103217, .T. ) ;
#61943=ORIENTED_EDGE ( 'NONE', *, *, #34908, .T. ) ;
#61946=CARTESIAN_POINT ( 'NONE',  ( 6.222803527742077456, 4.089662073612390536, 6.499999999999997335 ) ) ;
#61949=EDGE_LOOP ( 'NONE', ( #44143, #66306, #2507, #86203, #105489, #11075 ) ) ;
#61958=EDGE_CURVE ( 'NONE', #105946, #54290, #14508, .T. ) ;
#61990=DIRECTION ( 'NONE',  ( -1.000000000000000000, -1.224606353822377258E-16, -0.000000000000000000 ) ) ;
#62001=FACE_OUTER_BOUND ( 'NONE', #31530, .T. ) ;
#62021=CARTESIAN_POINT ( 'NONE',  ( 16.36650669486618881, 1.474610560812782335E-15, 0.000000000000000000 ) ) ;
#62025=DIRECTION ( 'NONE',  ( 1.000000000000000000, 1.224606353822377258E-16, 0.000000000000000000 ) ) ;
#62042=CARTESIAN_POINT ( 'NONE',  ( 14.34999999999999787, 1.533819458162526451E-15, 0.000000000000000000 ) ) ;
#62054=ORIENTED_EDGE ( 'NONE', *, *, #84517, .F. ) ;
#62059=ORIENTED_EDGE ( 'NONE', *, *, #58806, .F. ) ;
#62077=ORIENTED_EDGE ( 'NONE', *, *, #59096, .T. ) ;
#62083=FACE_OUTER_BOUND ( 'NONE', #13746, .T. ) ;
#62101=CARTESIAN_POINT ( 'NONE',  ( 34.35000000000000142, 3.309500000000003439, 0.000000000000000000 ) ) ;
#62111=ADVANCED_FACE ( 'NONE', ( #77187 ), #64596, .T. ) ;
#62140=( LENGTH_UNIT ( ) NAMED_UNIT ( * ) SI_UNIT ( .MILLI., .METRE. ) );
#62165=CARTESIAN_POINT ( 'NONE',  ( 0.000000000000000000, 4.898587196589412829E-16, -4.000000000000000000 ) ) ;
#62184=DIRECTION ( 'NONE',  ( -1.000000000000000000, -1.224606353822377258E-16, -0.000000000000000000 ) ) ;
#62240=CARTESIAN_POINT ( 'NONE',  ( -7.284483346386982916E-16, -0.6346842323187733559, 6.500000000000000000 ) ) ;
#62255=CARTESIAN_POINT ( 'NONE',  ( 36.36650669486618881, -3.851859888774471706E-31, 4.000000000000000888 ) ) ;
#62297=ORIENTED_EDGE ( 'NONE', *, *, #84920, .F. ) ;
#62323=CARTESIAN_POINT ( 'NONE',  ( 42.33349330513380693, 1.593028355512270567E-15, 0.000000000000000000 ) ) ;
#62328=EDGE_CURVE ( 'NONE', #49522, #79906, #79826, .T. ) ;
#62360=AXIS2_PLACEMENT_3D ( 'NONE', #4990, #71302, #47018 ) ;
#62373=VECTOR ( 'NONE', #33232, 1000.000000000000000 ) ;
#62389=FACE_OUTER_BOUND ( 'NONE', #92017, .T. ) ;
#62397=CARTESIAN_POINT ( 'NONE',  ( 17.33349330513380337, 1.593028355512270567E-15, 0.000000000000000000 ) ) ;
#62421=EDGE_CURVE ( 'NONE', #65506, #73382, #37065, .T. ) ;
#62432=CARTESIAN_POINT ( 'NONE',  ( 44.83349330513380693, -4.000000000000000000, 4.898587196589415787E-16 ) ) ;
#62442=CARTESIAN_POINT ( 'NONE',  ( 20.59999999999999787, 1.533819458162526451E-15, 0.000000000000000000 ) ) ;
#62461=CARTESIAN_POINT ( 'NONE',  ( 5.856349485908422636, 1.359279156792593701, 6.499999999999999112 ) ) ;
#62466=FACE_OUTER_BOUND ( 'NONE', #73055, .T. ) ;
#62496=AXIS2_PLACEMENT_3D ( 'NONE', #41936, #74297, #903 ) ;
#62507=DIRECTION ( 'NONE',  ( 0.000000000000000000, -1.000000000000000000, 0.000000000000000000 ) ) ;
#62533=CARTESIAN_POINT ( 'NONE',  ( 28.09999999999999787, -3.309499999999999886, 4.475777889183790779E-16 ) ) ;
#62534=DIRECTION ( 'NONE',  ( -1.000000000000000000, -1.224606353822377258E-16, -0.000000000000000000 ) ) ;
#62535=AXIS2_PLACEMENT_3D ( 'NONE', #85070, #86683, #12754 ) ;
#62536=VERTEX_POINT ( 'NONE', #72148 ) ;
#62542=EDGE_CURVE ( 'NONE', #94111, #4931, #67968, .T. ) ;
#62545=DIRECTION ( 'NONE',  ( 1.000000000000000000, 1.224606353822377258E-16, 0.000000000000000000 ) ) ;
#62557=CYLINDRICAL_SURFACE ( 'NONE', #56398, 4.000000000000000000 ) ;
#62568=EDGE_CURVE ( 'NONE', #86482, #27869, #94854, .T. ) ;
#62574=DIRECTION ( 'NONE',  ( 0.000000000000000000, 1.000000000000000000, 0.000000000000000000 ) ) ;
#62613=CARTESIAN_POINT ( 'NONE',  ( 26.08349330513380337, 4.000000000000003553, 0.000000000000000000 ) ) ;
#62626=EDGE_CURVE ( 'NONE', #52893, #61806, #12831, .T. ) ;
#62639=DIRECTION ( 'NONE',  ( -0.5735764363510494901, -0.8191520442889894671, 0.000000000000000000 ) ) ;
#62649=ADVANCED_FACE ( 'NONE', ( #70570 ), #49002, .T. ) ;
#62653=DIRECTION ( 'NONE',  ( 0.000000000000000000, -1.000000000000000000, 0.000000000000000000 ) ) ;
#62656=ORIENTED_EDGE ( 'NONE', *, *, #21037, .T. ) ;
#62657=STYLED_ITEM ( 'NONE', ( #94499 ), #88554 ) ;
#62677=ORIENTED_EDGE ( 'NONE', *, *, #37179, .F. ) ;
#62686=DIRECTION ( 'NONE',  ( 1.000000000000000000, 1.224606353822377258E-16, 0.000000000000000000 ) ) ;
#62764=CARTESIAN_POINT ( 'NONE',  ( 13.86650669486618881, 1.474610560812782335E-15, 0.000000000000000000 ) ) ;
#62781=CARTESIAN_POINT ( 'NONE',  ( 10.11650669486618881, 1.474610560812782335E-15, 0.000000000000000000 ) ) ;
#62785=CARTESIAN_POINT ( 'NONE',  ( 43.86650669486618881, 1.474610560812782335E-15, 0.000000000000000000 ) ) ;
#62791=FACE_OUTER_BOUND ( 'NONE', #51791, .T. ) ;
#62803=DIRECTION ( 'NONE',  ( 0.000000000000000000, -1.000000000000000000, 0.000000000000000000 ) ) ;
#62828=CARTESIAN_POINT ( 'NONE',  ( 0.000000000000000000, 0.000000000000000000, 0.000000000000000000 ) ) ;
#62843=CARTESIAN_POINT ( 'NONE',  ( 0.000000000000000000, 0.000000000000000000, 4.000000000000000000 ) ) ;
#62869=ORIENTED_EDGE ( 'NONE', *, *, #45015, .T. ) ;
#62886=ORIENTED_EDGE ( 'NONE', *, *, #43306, .F. ) ;
#62894=CARTESIAN_POINT ( 'NONE',  ( 6.562974947121709590, -4.277474787035884241, 6.282829635893500964 ) ) ;
#62898=CARTESIAN_POINT ( 'NONE',  ( 16.36650669486618881, 1.474610560812782335E-15, 0.000000000000000000 ) ) ;
#62908=EDGE_CURVE ( 'NONE', #29102, #26216, #70835, .T. ) ;
#62911=ORIENTED_EDGE ( 'NONE', *, *, #73074, .F. ) ;
#62915=EDGE_CURVE ( 'NONE', #65538, #45473, #97214, .T. ) ;
#62922=AXIS2_PLACEMENT_3D ( 'NONE', #102743, #68799, #18668 ) ;
#62935=ADVANCED_FACE ( 'NONE', ( #13640 ), #46554, .T. ) ;
#62982=ADVANCED_FACE ( 'NONE', ( #50264 ), #18180, .T. ) ;
#62988=CONICAL_SURFACE ( 'NONE', #102556, 3.309500000000001663, 0.9599310885968770357 ) ;
#63000=VECTOR ( 'NONE', #50292, 1000.000000000000000 ) ;
#63006=ORIENTED_EDGE ( 'NONE', *, *, #105521, .T. ) ;
#63007=FACE_OUTER_BOUND ( 'NONE', #78173, .T. ) ;
#63013=DIRECTION ( 'NONE',  ( 0.5735764363510466035, -0.8191520442889914655, 1.003171929053524500E-16 ) ) ;
#63021=CONICAL_SURFACE ( 'NONE', #94046, 4.000000000000001776, 0.9599310885968808105 ) ;
#63025=EDGE_CURVE ( 'NONE', #60365, #22876, #95617, .T. ) ;
#63041=CARTESIAN_POINT ( 'NONE',  ( 23.58349330513380337, -7.703719777548943412E-31, 4.000000000000001776 ) ) ;
#63049=DIRECTION ( 'NONE',  ( 0.000000000000000000, -1.000000000000000000, 0.000000000000000000 ) ) ;
#63103=EDGE_CURVE ( 'NONE', #83331, #31200, #43952, .T. ) ;
#63115=DIRECTION ( 'NONE',  ( -1.000000000000000000, -1.224606353822377258E-16, -0.000000000000000000 ) ) ;
#63131=CONICAL_SURFACE ( 'NONE', #18340, 3.309500000000001663, 0.9599310885968770357 ) ;
#63133=CARTESIAN_POINT ( 'NONE',  ( 27.33349330513380337, 1.593028355512270567E-15, 0.000000000000000000 ) ) ;
#63135=MECHANICAL_DESIGN_GEOMETRIC_PRESENTATION_REPRESENTATION('',(#51021),#76906);
#63155=EDGE_CURVE ( 'NONE', #79845, #82202, #73181, .T. ) ;
#63156=DIRECTION ( 'NONE',  ( -1.000000000000000000, -1.224606353822377258E-16, -0.000000000000000000 ) ) ;
#63167=DIRECTION ( 'NONE',  ( -1.000000000000000000, -1.224606353822377258E-16, -0.000000000000000000 ) ) ;
#63171=DIRECTION ( 'NONE',  ( -1.000000000000000000, -1.224606353822377258E-16, -0.000000000000000000 ) ) ;
#63224=CARTESIAN_POINT ( 'NONE',  ( 15.11650669486618881, -3.999999999999998224, 0.000000000000000000 ) ) ;
#63225=ADVANCED_FACE ( 'NONE', ( #19547 ), #74955, .T. ) ;
#63283=ORIENTED_EDGE ( 'NONE', *, *, #106561, .F. ) ;
#63284=ADVANCED_FACE ( 'NONE', ( #39930 ), #6055, .T. ) ;
#63293=AXIS2_PLACEMENT_3D ( 'NONE', #59509, #92918, #51922 ) ;
#63301=AXIS2_PLACEMENT_3D ( 'NONE', #59090, #43960, #26229 ) ;
#63332=DIRECTION ( 'NONE',  ( 0.000000000000000000, -1.000000000000000000, 0.000000000000000000 ) ) ;
#63352=AXIS2_PLACEMENT_3D ( 'NONE', #1344, #65575, #100063 ) ;
#63369=AXIS2_PLACEMENT_3D ( 'NONE', #19494, #76605, #2719 ) ;
#63371=LINE ( 'NONE', #45589, #95004 ) ;
#63389=DIRECTION ( 'NONE',  ( 0.000000000000000000, 1.000000000000000000, 0.000000000000000000 ) ) ;
#63402=ORIENTED_EDGE ( 'NONE', *, *, #89462, .F. ) ;
#63417=AXIS2_PLACEMENT_3D ( 'NONE', #105058, #103979, #29097 ) ;
#63432=LINE ( 'NONE', #61841, #70402 ) ;
#63433=SURFACE_STYLE_USAGE ( .BOTH. , #31598 ) ;
#63435=ORIENTED_EDGE ( 'NONE', *, *, #64517, .T. ) ;
#63437=EDGE_CURVE ( 'NONE', #17581, #58778, #18328, .T. ) ;
#63442=CARTESIAN_POINT ( 'NONE',  ( 6.289812543865807015, -6.246946743711094818, -2.837966828325884538 ) ) ;
#63444=AXIS2_PLACEMENT_3D ( 'NONE', #21687, #103110, #95032 ) ;
#63451=VERTEX_POINT ( 'NONE', #77070 ) ;
#63455=CARTESIAN_POINT ( 'NONE',  ( 47.33349330513379982, 1.593028355512270567E-15, 0.000000000000000000 ) ) ;
#63499=CIRCLE ( 'NONE', #25658, 4.000000000000001776 ) ;
#63504=ADVANCED_FACE ( 'NONE', ( #100278 ), #26440, .T. ) ;
#63546=DIRECTION ( 'NONE',  ( 0.000000000000000000, -1.000000000000000000, 0.000000000000000000 ) ) ;
#63550=CARTESIAN_POINT ( 'NONE',  ( 21.36650669486618881, -3.999999999999998224, 0.000000000000000000 ) ) ;
#63585=VECTOR ( 'NONE', #35227, 1000.000000000000000 ) ;
#63596=EDGE_CURVE ( 'NONE', #102391, #4391, #76726, .T. ) ;
#63633=ORIENTED_EDGE ( 'NONE', *, *, #20515, .F. ) ;
#63634=CARTESIAN_POINT ( 'NONE',  ( 41.36650669486618881, 4.898587196589411843E-16, -4.000000000000000888 ) ) ;
#63635=EDGE_CURVE ( 'NONE', #16749, #47728, #932, .T. ) ;
#63637=CARTESIAN_POINT ( 'NONE',  ( 48.10000000000000142, 0.000000000000000000, 0.000000000000000000 ) ) ;
#63659=FACE_OUTER_BOUND ( 'NONE', #41138, .T. ) ;
#63670=VERTEX_POINT ( 'NONE', #66194 ) ;
#63698=VERTEX_POINT ( 'NONE', #9540 ) ;
#63723=CIRCLE ( 'NONE', #36182, 4.000000000000000888 ) ;
#63733=AXIS2_PLACEMENT_3D ( 'NONE', #62828, #104873, #46626 ) ;
#63772=ORIENTED_EDGE ( 'NONE', *, *, #101380, .F. ) ;
#63780=DIRECTION ( 'NONE',  ( -1.000000000000000000, -1.224606353822377258E-16, -0.000000000000000000 ) ) ;
#63786=DIRECTION ( 'NONE',  ( -1.000000000000000000, -1.224606353822377258E-16, -0.000000000000000000 ) ) ;
#63803=ORIENTED_EDGE ( 'NONE', *, *, #72083, .F. ) ;
#63814=CARTESIAN_POINT ( 'NONE',  ( 0.05458999538772730392, -1.264741368073330818, 6.499999999999999112 ) ) ;
#63835=ORIENTED_EDGE ( 'NONE', *, *, #56646, .T. ) ;
#63841=DIRECTION ( 'NONE',  ( 0.000000000000000000, -1.000000000000000000, 0.000000000000000000 ) ) ;
#63849=ADVANCED_FACE ( 'NONE', ( #76948 ), #92355, .T. ) ;
#63851=ORIENTED_EDGE ( 'NONE', *, *, #4671, .F. ) ;
#63872=ORIENTED_EDGE ( 'NONE', *, *, #79278, .F. ) ;
#63894=DIRECTION ( 'NONE',  ( -1.000000000000000000, -1.224606353822377258E-16, -0.000000000000000000 ) ) ;
#63932=ORIENTED_EDGE ( 'NONE', *, *, #96025, .F. ) ;
#63938=CARTESIAN_POINT ( 'NONE',  ( 37.33349330513379982, 1.593028355512270567E-15, 0.000000000000000000 ) ) ;
#63939=DIRECTION ( 'NONE',  ( -0.5735764363510494901, -0.8191520442889894671, 0.000000000000000000 ) ) ;
#63953=VERTEX_POINT ( 'NONE', #44749 ) ;
#63965=ORIENTED_EDGE ( 'NONE', *, *, #97368, .T. ) ;
#63966=DIRECTION ( 'NONE',  ( 0.000000000000000000, -1.000000000000000000, 0.000000000000000000 ) ) ;
#63976=EDGE_CURVE ( 'NONE', #92028, #44354, #100911, .T. ) ;
#63982=EDGE_CURVE ( 'NONE', #5935, #8490, #90134, .T. ) ;
#63983=DIRECTION ( 'NONE',  ( 1.000000000000000000, 1.224606353822377258E-16, 0.000000000000000000 ) ) ;
#63991=EDGE_CURVE ( 'NONE', #59552, #22614, #86806, .T. ) ;
#64000=EDGE_CURVE ( 'NONE', #42587, #60121, #99208, .T. ) ;
#64037=DIRECTION ( 'NONE',  ( 0.000000000000000000, -1.000000000000000000, 0.000000000000000000 ) ) ;
#64058=AXIS2_PLACEMENT_3D ( 'NONE', #30055, #54820, #87748 ) ;
#64081=EDGE_LOOP ( 'NONE', ( #411, #23110, #70648, #15353, #97344 ) ) ;
#64105=CARTESIAN_POINT ( 'NONE',  ( 0.000000000000000000, 0.000000000000000000, 0.000000000000000000 ) ) ;
#64120=ORIENTED_EDGE ( 'NONE', *, *, #59744, .F. ) ;
#64125=DIRECTION ( 'NONE',  ( -1.000000000000000000, -1.224606353822377258E-16, -0.000000000000000000 ) ) ;
#64129=EDGE_CURVE ( 'NONE', #55862, #44189, #92619, .T. ) ;
#64135=VECTOR ( 'NONE', #67460, 1000.000000000000000 ) ;
#64157=DIRECTION ( 'NONE',  ( 0.000000000000000000, 1.000000000000000000, -3.466879843239602429E-16 ) ) ;
#64169=FACE_OUTER_BOUND ( 'NONE', #79810, .T. ) ;
#64203=CIRCLE ( 'NONE', #48686, 4.000000000000001776 ) ;
#64220=CARTESIAN_POINT ( 'NONE',  ( 28.09999999999999787, 1.533819458162526451E-15, 0.000000000000000000 ) ) ;
#64221=ORIENTED_EDGE ( 'NONE', *, *, #98743, .T. ) ;
#64245=EDGE_CURVE ( 'NONE', #75882, #46481, #39897, .T. ) ;
#64250=AXIS2_PLACEMENT_3D ( 'NONE', #64341, #103720, #30931 ) ;
#64268=VERTEX_POINT ( 'NONE', #78037 ) ;
#64341=CARTESIAN_POINT ( 'NONE',  ( 9.833493305133801599, 1.593028355512270567E-15, 0.000000000000000000 ) ) ;
#64343=CARTESIAN_POINT ( 'NONE',  ( 0.000000000000000000, 2.253471898105741801E-15, 6.500000000000000000 ) ) ;
#64356=CARTESIAN_POINT ( 'NONE',  ( 0.000000000000000000, 0.000000000000000000, 0.000000000000000000 ) ) ;
#64375=ORIENTED_EDGE ( 'NONE', *, *, #80635, .T. ) ;
#64402=EDGE_CURVE ( 'NONE', #10553, #32012, #39034, .T. ) ;
#64410=VECTOR ( 'NONE', #99490, 1000.000000000000000 ) ;
#64415=DIRECTION ( 'NONE',  ( -0.5735764363510494901, -0.8191520442889894671, 0.000000000000000000 ) ) ;
#64454=EDGE_LOOP ( 'NONE', ( #14288, #19390, #42516, #43728, #90327 ) ) ;
#64467=LINE ( 'NONE', #98404, #8318 ) ;
#64483=PRESENTATION_STYLE_ASSIGNMENT (( #63433 ) ) ;
#64487=ORIENTED_EDGE ( 'NONE', *, *, #40478, .T. ) ;
#64490=DIRECTION ( 'NONE',  ( 0.000000000000000000, -1.000000000000000000, 0.000000000000000000 ) ) ;
#64495=CARTESIAN_POINT ( 'NONE',  ( 18.58349330513380337, 1.593028355512270567E-15, 0.000000000000000000 ) ) ;
#64502=EDGE_LOOP ( 'NONE', ( #26066, #93106, #98094, #50826, #8311 ) ) ;
#64517=EDGE_CURVE ( 'NONE', #35056, #27202, #19891, .T. ) ;
#64529=CIRCLE ( 'NONE', #40413, 4.000000000000000888 ) ;
#64538=CARTESIAN_POINT ( 'NONE',  ( 17.61650669486618881, -3.999999999999998224, 0.000000000000000000 ) ) ;
#64562=ORIENTED_EDGE ( 'NONE', *, *, #70472, .T. ) ;
#64563=EDGE_CURVE ( 'NONE', #39684, #77823, #80121, .T. ) ;
#64569=CARTESIAN_POINT ( 'NONE',  ( 8.099999999999999645, 3.752776749732565253, 6.499999999999997335 ) ) ;
#64573=ADVANCED_FACE ( 'NONE', ( #83867 ), #52552, .T. ) ;
#64582=CARTESIAN_POINT ( 'NONE',  ( 6.644028492724101120, -3.901260126079175716, 6.757180751914474648 ) ) ;
#64589=FACE_OUTER_BOUND ( 'NONE', #93808, .T. ) ;
#64596=CONICAL_SURFACE ( 'NONE', #18097, 4.000000000000001776, 0.9599310885968808105 ) ;
#64602=ORIENTED_EDGE ( 'NONE', *, *, #3920, .F. ) ;
#64605=LINE ( 'NONE', #80232, #56929 ) ;
#64608=AXIS2_PLACEMENT_3D ( 'NONE', #84830, #50840, #93465 ) ;
#64647=EDGE_CURVE ( 'NONE', #57692, #35426, #6271, .T. ) ;
#64653=DIRECTION ( 'NONE',  ( -1.000000000000000000, -1.224606353822377258E-16, -0.000000000000000000 ) ) ;
#64655=AXIS2_PLACEMENT_3D ( 'NONE', #9263, #81539, #17922 ) ;
#64658=CIRCLE ( 'NONE', #23343, 4.000000000000001776 ) ;
#64672=ORIENTED_EDGE ( 'NONE', *, *, #105765, .T. ) ;
#64692=EDGE_CURVE ( 'NONE', #60457, #105650, #75020, .T. ) ;
#64698=LINE ( 'NONE', #32355, #54660 ) ;
#64707=CARTESIAN_POINT ( 'NONE',  ( 22.33349330513380337, 4.000000000000002665, 0.000000000000000000 ) ) ;
#64733=VERTEX_POINT ( 'NONE', #78428 ) ;
#64746=CIRCLE ( 'NONE', #57791, 4.000000000000001776 ) ;
#64812=VECTOR ( 'NONE', #83535, 1000.000000000000114 ) ;
#64814=AXIS2_PLACEMENT_3D ( 'NONE', #36901, #102662, #103197 ) ;
#64827=DIRECTION ( 'NONE',  ( 0.000000000000000000, 0.000000000000000000, 1.000000000000000000 ) ) ;
#64859=VERTEX_POINT ( 'NONE', #21300 ) ;
#64914=EDGE_CURVE ( 'NONE', #76395, #35999, #15291, .T. ) ;
#64920=DIRECTION ( 'NONE',  ( -1.000000000000000000, -1.224606353822377258E-16, -0.000000000000000000 ) ) ;
#64924=EDGE_CURVE ( 'NONE', #78785, #55889, #55989, .T. ) ;
#64936=CARTESIAN_POINT ( 'NONE',  ( 6.289692432696784685, -1.240516797660047330E-13, -6.828989928337167115 ) ) ;
#64976=AXIS2_PLACEMENT_3D ( 'NONE', #13334, #12283, #78087 ) ;
#64980=VERTEX_POINT ( 'NONE', #100454 ) ;
#64988=EDGE_CURVE ( 'NONE', #34125, #84498, #82679, .T. ) ;
#64990=EDGE_LOOP ( 'NONE', ( #79124, #94276, #81694, #99393, #92866 ) ) ;
#65021=LINE ( 'NONE', #31620, #31851 ) ;
#65032=AXIS2_PLACEMENT_3D ( 'NONE', #76870, #18130, #99545 ) ;
#65074=ORIENTED_EDGE ( 'NONE', *, *, #46061, .T. ) ;
#65079=ORIENTED_EDGE ( 'NONE', *, *, #26095, .T. ) ;
#65080=ADVANCED_FACE ( 'NONE', ( #90244 ), #77785, .T. ) ;
#65093=EDGE_CURVE ( 'NONE', #19064, #2149, #20121, .T. ) ;
#65101=DIRECTION ( 'NONE',  ( -1.000000000000000000, -1.224606353822377258E-16, -0.000000000000000000 ) ) ;
#65111=DIRECTION ( 'NONE',  ( 0.000000000000000000, 1.000000000000000000, 0.000000000000000000 ) ) ;
#65113=EDGE_CURVE ( 'NONE', #97567, #25329, #45426, .T. ) ;
#65129=CONICAL_SURFACE ( 'NONE', #34136, 3.309500000000001663, 0.9599310885968770357 ) ;
#65171=CARTESIAN_POINT ( 'NONE',  ( 38.09999999999999432, 3.309500000000003439, 4.052968581778167743E-16 ) ) ;
#65172=EDGE_CURVE ( 'NONE', #4391, #58764, #92892, .T. ) ;
#65176=EDGE_CURVE ( 'NONE', #21079, #33104, #2657, .T. ) ;
#65200=ORIENTED_EDGE ( 'NONE', *, *, #30508, .T. ) ;
#65206=LINE ( 'NONE', #98101, #103001 ) ;
#65217=EDGE_CURVE ( 'NONE', #866, #35550, #100820, .T. ) ;
#65222=DIRECTION ( 'NONE',  ( 0.000000000000000000, -1.000000000000000000, 0.000000000000000000 ) ) ;
#65232=FACE_OUTER_BOUND ( 'NONE', #23049, .T. ) ;
#65246=EDGE_CURVE ( 'NONE', #100266, #77600, #55591, .T. ) ;
#65247=ORIENTED_EDGE ( 'NONE', *, *, #89999, .T. ) ;
#65257=CARTESIAN_POINT ( 'NONE',  ( 6.463344223170836678, 4.601472318010335627, -5.710032555828794543 ) ) ;
#65287=DIRECTION ( 'NONE',  ( -1.000000000000000000, -0.000000000000000000, -0.000000000000000000 ) ) ;
#65290=CIRCLE ( 'NONE', #30913, 4.000000000000001776 ) ;
#65307=EDGE_CURVE ( 'NONE', #51415, #13309, #92272, .T. ) ;
#65316=DIRECTION ( 'NONE',  ( 0.000000000000000000, -1.000000000000000000, 0.000000000000000000 ) ) ;
#65332=ORIENTED_EDGE ( 'NONE', *, *, #106495, .T. ) ;
#65336=DIRECTION ( 'NONE',  ( -1.000000000000000000, -1.224606353822377258E-16, -0.000000000000000000 ) ) ;
#65339=DIRECTION ( 'NONE',  ( 0.000000000000000000, -1.000000000000000000, 0.000000000000000000 ) ) ;
#65352=AXIS2_PLACEMENT_3D ( 'NONE', #24292, #98140, #49045 ) ;
#65355=ORIENTED_EDGE ( 'NONE', *, *, #55486, .F. ) ;
#65385=DIRECTION ( 'NONE',  ( -1.000000000000000000, -1.224606353822377258E-16, -0.000000000000000000 ) ) ;
#65392=EDGE_CURVE ( 'NONE', #5935, #49696, #92763, .T. ) ;
#65394=LINE ( 'NONE', #82636, #25278 ) ;
#65398=VECTOR ( 'NONE', #15809, 1000.000000000000114 ) ;
#65399=DIRECTION ( 'NONE',  ( -1.000000000000000000, -0.000000000000000000, -0.000000000000000000 ) ) ;
#65402=DIRECTION ( 'NONE',  ( 0.000000000000000000, -1.000000000000000000, 0.000000000000000000 ) ) ;
#65429=CARTESIAN_POINT ( 'NONE',  ( 23.58349330513380337, 1.593028355512270567E-15, 0.000000000000000000 ) ) ;
#65448=EDGE_LOOP ( 'NONE', ( #42440, #82956, #62656, #49380, #80231 ) ) ;
#65470=DIRECTION ( 'NONE',  ( -1.000000000000000000, -1.224606353822377258E-16, -0.000000000000000000 ) ) ;
#65487=CIRCLE ( 'NONE', #84431, 4.000000000000000888 ) ;
#65488=CARTESIAN_POINT ( 'NONE',  ( 9.349999999999997868, 1.533819458162526451E-15, 0.000000000000000000 ) ) ;
#65506=VERTEX_POINT ( 'NONE', #84579 ) ;
#65521=EDGE_CURVE ( 'NONE', #10553, #75882, #106537, .T. ) ;
#65538=VERTEX_POINT ( 'NONE', #68396 ) ;
#65550=CIRCLE ( 'NONE', #39765, 4.000000000000000888 ) ;
#65555=CARTESIAN_POINT ( 'NONE',  ( 45.11650669486618881, 4.000000000000003553, 4.898587196589414801E-16 ) ) ;
#65566=EDGE_CURVE ( 'NONE', #57881, #7789, #3118, .T. ) ;
#65570=ADVANCED_FACE ( 'NONE', ( #77002 ), #1007, .T. ) ;
#65575=DIRECTION ( 'NONE',  ( -1.000000000000000000, -1.224606353822377258E-16, -0.000000000000000000 ) ) ;
#65595=DIRECTION ( 'NONE',  ( -1.000000000000000000, -1.224606353822377258E-16, -0.000000000000000000 ) ) ;
#65642=ORIENTED_EDGE ( 'NONE', *, *, #87499, .F. ) ;
#65652=CIRCLE ( 'NONE', #19195, 4.000000000000001776 ) ;
#65657=VECTOR ( 'NONE', #32078, 1000.000000000000000 ) ;
#65658=CARTESIAN_POINT ( 'NONE',  ( 39.34999999999999432, 3.309500000000003439, 0.000000000000000000 ) ) ;
#65674=CARTESIAN_POINT ( 'NONE',  ( 6.162888688655347558, 7.505553499465140277, 0.000000000000000000 ) ) ;
#65700=AXIS2_PLACEMENT_3D ( 'NONE', #79138, #23055, #96405 ) ;
#65701=FACE_OUTER_BOUND ( 'NONE', #53592, .T. ) ;
#65704=CARTESIAN_POINT ( 'NONE',  ( 31.36650669486618881, -3.851859888774471706E-31, 4.000000000000000888 ) ) ;
#65715=CYLINDRICAL_SURFACE ( 'NONE', #29774, 4.000000000000000000 ) ;
#65718=DIRECTION ( 'NONE',  ( -0.5735764363510497121, 0.8191520442889892450, 1.003171929053521665E-16 ) ) ;
#65730=ORIENTED_EDGE ( 'NONE', *, *, #89598, .T. ) ;
#65742=ORIENTED_EDGE ( 'NONE', *, *, #35443, .F. ) ;
#65744=CARTESIAN_POINT ( 'NONE',  ( 8.099999999999999645, -3.752776749732561257, 6.500000000000000000 ) ) ;
#65764=DIRECTION ( 'NONE',  ( -1.000000000000000000, -1.224606353822377258E-16, -0.000000000000000000 ) ) ;
#65769=CONICAL_SURFACE ( 'NONE', #72610, 3.309500000000001663, 0.9599310885968770357 ) ;
#65781=VERTEX_POINT ( 'NONE', #98485 ) ;
#65807=DIRECTION ( 'NONE',  ( 0.5735764363510466035, -0.8191520442889914655, 1.003171929053524500E-16 ) ) ;
#65819=ADVANCED_FACE ( 'NONE', ( #58025 ), #90599, .T. ) ;
#65836=DIRECTION ( 'NONE',  ( -1.000000000000000000, -0.000000000000000000, -0.000000000000000000 ) ) ;
#65868=DIRECTION ( 'NONE',  ( -1.000000000000000000, -1.224606353822377258E-16, -0.000000000000000000 ) ) ;
#65882=VERTEX_POINT ( 'NONE', #96214 ) ;
#65885=DIRECTION ( 'NONE',  ( -1.000000000000000000, -0.000000000000000000, -0.000000000000000000 ) ) ;
#65917=CARTESIAN_POINT ( 'NONE',  ( 45.11650669486618881, 1.474610560812782335E-15, 0.000000000000000000 ) ) ;
#65921=DIRECTION ( 'NONE',  ( -0.5735764363510494901, -0.8191520442889894671, 0.000000000000000000 ) ) ;
#65925=ORIENTED_EDGE ( 'NONE', *, *, #55675, .F. ) ;
#65937=CARTESIAN_POINT ( 'NONE',  ( 39.83349330513380693, 1.593028355512270567E-15, 0.000000000000000000 ) ) ;
#65951=CARTESIAN_POINT ( 'NONE',  ( 16.36650669486618881, -3.999999999999998224, 0.000000000000000000 ) ) ;
#65952=LINE ( 'NONE', #73495, #39259 ) ;
#65968=ORIENTED_EDGE ( 'NONE', *, *, #81751, .T. ) ;
#65974=FACE_OUTER_BOUND ( 'NONE', #85256, .T. ) ;
#65994=DIRECTION ( 'NONE',  ( -1.000000000000000000, -1.224606353822377258E-16, -0.000000000000000000 ) ) ;
#66035=DIRECTION ( 'NONE',  ( 0.000000000000000000, -1.000000000000000000, 0.000000000000000000 ) ) ;
#66053=CARTESIAN_POINT ( 'NONE',  ( 29.83349330513380337, 4.000000000000002665, 0.000000000000000000 ) ) ;
#66078=ADVANCED_FACE ( 'NONE', ( #24700 ), #82376, .T. ) ;
#66092=VECTOR ( 'NONE', #102139, 1000.000000000000000 ) ;
#66096=AXIS2_PLACEMENT_3D ( 'NONE', #10339, #92854, #69138 ) ;
#66113=EDGE_CURVE ( 'NONE', #66259, #88304, #60786, .T. ) ;
#66117=CIRCLE ( 'NONE', #105688, 3.309500000000001663 ) ;
#66122=DIRECTION ( 'NONE',  ( -1.000000000000000000, -1.224606353822377258E-16, -0.000000000000000000 ) ) ;
#66128=DIRECTION ( 'NONE',  ( 0.000000000000000000, 0.000000000000000000, 1.000000000000000000 ) ) ;
#66134=DIRECTION ( 'NONE',  ( -1.000000000000000000, -1.224606353822377258E-16, -0.000000000000000000 ) ) ;
#66161=ORIENTED_EDGE ( 'NONE', *, *, #56000, .T. ) ;
#66166=VECTOR ( 'NONE', #27944, 1000.000000000000114 ) ;
#66178=VERTEX_POINT ( 'NONE', #10084 ) ;
#66194=CARTESIAN_POINT ( 'NONE',  ( 46.08349330513379982, -4.000000000000000888, 4.898587196589416773E-16 ) ) ;
#66243=ORIENTED_EDGE ( 'NONE', *, *, #24444, .T. ) ;
#66245=CARTESIAN_POINT ( 'NONE',  ( 26.36650669486618881, 1.474610560812782335E-15, 0.000000000000000000 ) ) ;
#66248=EDGE_CURVE ( 'NONE', #43166, #3450, #79613, .T. ) ;
#66254=CARTESIAN_POINT ( 'NONE',  ( 0.4037800551813712779, -4.058962678540093627, 5.969670414742685338 ) ) ;
#66259=VERTEX_POINT ( 'NONE', #79596 ) ;
#66266=AXIS2_PLACEMENT_3D ( 'NONE', #103455, #71606, #22576 ) ;
#66285=CARTESIAN_POINT ( 'NONE',  ( 10.11650669486618881, 4.000000000000003553, 4.898587196589414801E-16 ) ) ;
#66290=DIRECTION ( 'NONE',  ( 0.000000000000000000, -1.000000000000000000, 0.000000000000000000 ) ) ;
#66298=EDGE_CURVE ( 'NONE', #45473, #66178, #2888, .T. ) ;
#66306=ORIENTED_EDGE ( 'NONE', *, *, #32522, .T. ) ;
#66316=CARTESIAN_POINT ( 'NONE',  ( 6.289572920342626716, 6.243622107253691489, -2.843693100100564308 ) ) ;
#66320=ORIENTED_EDGE ( 'NONE', *, *, #37112, .F. ) ;
#66324=CARTESIAN_POINT ( 'NONE',  ( 13.09999999999999787, 1.533819458162526451E-15, 0.000000000000000000 ) ) ;
#66325=PRODUCT_DEFINITION_FORMATION_WITH_SPECIFIED_SOURCE ( 'ANY', '', #70009, .NOT_KNOWN. ) ;
#66378=CARTESIAN_POINT ( 'NONE',  ( 35.59999999999999432, 1.533819458162526451E-15, 0.000000000000000000 ) ) ;
#66387=ORIENTED_EDGE ( 'NONE', *, *, #45110, .T. ) ;
#66388=LINE ( 'NONE', #80967, #52661 ) ;
#66391=DIRECTION ( 'NONE',  ( 0.000000000000000000, -1.000000000000000000, 0.000000000000000000 ) ) ;
#66404=ORIENTED_EDGE ( 'NONE', *, *, #87071, .T. ) ;
#66409=CARTESIAN_POINT ( 'NONE',  ( 18.86650669486618881, 1.474610560812782335E-15, 0.000000000000000000 ) ) ;
#66423=AXIS2_PLACEMENT_3D ( 'NONE', #3185, #26963, #76001 ) ;
#66431=EDGE_LOOP ( 'NONE', ( #67745, #64375, #96565, #63283, #61427 ) ) ;
#66465=ORIENTED_EDGE ( 'NONE', *, *, #381, .F. ) ;
#66474=CARTESIAN_POINT ( 'NONE',  ( 10.59999999999999609, -3.309499999999999886, 0.000000000000000000 ) ) ;
#66484=DIRECTION ( 'NONE',  ( 0.5735764363510462704, 0.8191520442889915765, 0.000000000000000000 ) ) ;
#66486=CYLINDRICAL_SURFACE ( 'NONE', #49469, 4.000000000000000000 ) ;
#66504=EDGE_CURVE ( 'NONE', #77823, #33833, #100021, .T. ) ;
#66505=DIRECTION ( 'NONE',  ( 0.000000000000000000, -1.000000000000000000, 0.000000000000000000 ) ) ;
#66520=EDGE_CURVE ( 'NONE', #86885, #45510, #83840, .T. ) ;
#66546=DIRECTION ( 'NONE',  ( 1.000000000000000000, 1.224606353822377258E-16, 0.000000000000000000 ) ) ;
#66552=CARTESIAN_POINT ( 'NONE',  ( 33.09999999999999432, 3.309500000000003439, 0.000000000000000000 ) ) ;
#66560=EDGE_CURVE ( 'NONE', #100726, #88549, #60661, .T. ) ;
#66582=EDGE_CURVE ( 'NONE', #29335, #78409, #97649, .T. ) ;
#66609=VERTEX_POINT ( 'NONE', #62255 ) ;
#66610=CARTESIAN_POINT ( 'NONE',  ( 6.394337469123802187, -7.552703473009535706, 4.547976812830884136E-16 ) ) ;
#66624=DIRECTION ( 'NONE',  ( -1.000000000000000000, -0.000000000000000000, -0.000000000000000000 ) ) ;
#66634=EDGE_CURVE ( 'NONE', #75817, #63451, #94224, .T. ) ;
#66641=DIRECTION ( 'NONE',  ( -0.5735764363510494901, -0.8191520442889894671, 0.000000000000000000 ) ) ;
#66651=CARTESIAN_POINT ( 'NONE',  ( 42.33349330513380693, 1.593028355512270567E-15, 0.000000000000000000 ) ) ;
#66695=EDGE_LOOP ( 'NONE', ( #6685, #20961, #18181, #15501, #18062 ) ) ;
#66710=DIRECTION ( 'NONE',  ( 0.000000000000000000, -1.000000000000000000, 0.000000000000000000 ) ) ;
#66724=LINE ( 'NONE', #18741, #27702 ) ;
#66725=ORIENTED_EDGE ( 'NONE', *, *, #93426, .F. ) ;
#66730=CARTESIAN_POINT ( 'NONE',  ( 0.000000000000000000, 0.000000000000000000, 4.000000000000000000 ) ) ;
#66732=ADVANCED_FACE ( 'NONE', ( #30955 ), #28828, .T. ) ;
#66734=AXIS2_PLACEMENT_3D ( 'NONE', #86922, #21152, #20096 ) ;
#66760=DIRECTION ( 'NONE',  ( 0.000000000000000000, -1.000000000000000000, 0.000000000000000000 ) ) ;
#66768=CARTESIAN_POINT ( 'NONE',  ( 18.09999999999999787, -3.309499999999999886, 4.475777889183790779E-16 ) ) ;
#66776=AXIS2_PLACEMENT_3D ( 'NONE', #21766, #5545, #72915 ) ;
#66777=ORIENTED_EDGE ( 'NONE', *, *, #62328, .F. ) ;
#66779=DIRECTION ( 'NONE',  ( 1.000000000000000000, 1.224606353822377258E-16, 0.000000000000000000 ) ) ;
#66786=CARTESIAN_POINT ( 'NONE',  ( 0.000000000000000000, 4.898587196589412829E-16, -4.000000000000000000 ) ) ;
#66788=CARTESIAN_POINT ( 'NONE',  ( 5.821900211247815093, 1.420906337218632798, -6.499999999999999112 ) ) ;
#66809=DIRECTION ( 'NONE',  ( -1.000000000000000000, -1.224606353822377258E-16, -0.000000000000000000 ) ) ;
#66861=CARTESIAN_POINT ( 'NONE',  ( 41.08349330513380693, 4.000000000000003553, 0.000000000000000000 ) ) ;
#66878=AXIS2_PLACEMENT_3D ( 'NONE', #28110, #11331, #62574 ) ;
#66905=CARTESIAN_POINT ( 'NONE',  ( 26.08349330513380337, 4.000000000000002665, 0.000000000000000000 ) ) ;
#66921=VECTOR ( 'NONE', #32892, 1000.000000000000000 ) ;
#66997=DIRECTION ( 'NONE',  ( -1.000000000000000000, -1.224606353822377258E-16, -0.000000000000000000 ) ) ;
#66998=ORIENTED_EDGE ( 'NONE', *, *, #40335, .F. ) ;
#67009=ADVANCED_FACE ( 'NONE', ( #46446 ), #104589, .T. ) ;
#67010=CIRCLE ( 'NONE', #84164, 4.000000000000001776 ) ;
#67021=DIRECTION ( 'NONE',  ( 0.000000000000000000, -1.000000000000000000, 0.000000000000000000 ) ) ;
#67039=ORIENTED_EDGE ( 'NONE', *, *, #23124, .F. ) ;
#67043=DIRECTION ( 'NONE',  ( 0.000000000000000000, -1.000000000000000000, 0.000000000000000000 ) ) ;
#67061=ORIENTED_EDGE ( 'NONE', *, *, #62568, .T. ) ;
#67121=DIRECTION ( 'NONE',  ( 0.000000000000000000, -1.000000000000000000, 0.000000000000000000 ) ) ;
#67122=ORIENTED_EDGE ( 'NONE', *, *, #23603, .T. ) ;
#67149=CARTESIAN_POINT ( 'NONE',  ( 6.289692432696784685, 1.244805614057421469E-13, 6.828989928337167115 ) ) ;
#67172=ADVANCED_FACE ( 'NONE', ( #56507 ), #11580, .T. ) ;
#67208=FACE_OUTER_BOUND ( 'NONE', #88783, .T. ) ;
#67235=CARTESIAN_POINT ( 'NONE',  ( 0.000000000000000000, 0.000000000000000000, 0.000000000000000000 ) ) ;
#67236=CARTESIAN_POINT ( 'NONE',  ( 0.000000000000000000, 5.629165124598848102, 3.250000000000005329 ) ) ;
#67237=AXIS2_PLACEMENT_3D ( 'NONE', #35912, #60692, #4033 ) ;
#67271=AXIS2_PLACEMENT_3D ( 'NONE', #25848, #81349, #7461 ) ;
#67274=LINE ( 'NONE', #66730, #40341 ) ;
#67282=FACE_OUTER_BOUND ( 'NONE', #42965, .T. ) ;
#67288=CARTESIAN_POINT ( 'NONE',  ( 32.33349330513379982, 4.898587196589405926E-16, -4.000000000000001776 ) ) ;
#67325=LINE ( 'NONE', #66786, #99928 ) ;
#67331=AXIS2_PLACEMENT_3D ( 'NONE', #22728, #24322, #47488 ) ;
#67343=EDGE_LOOP ( 'NONE', ( #8210, #44339, #94257, #106342, #46850 ) ) ;
#67349=CARTESIAN_POINT ( 'NONE',  ( 26.08349330513380337, 1.593028355512270567E-15, 0.000000000000000000 ) ) ;
#67403=EDGE_CURVE ( 'NONE', #66609, #33845, #5207, .T. ) ;
#67408=EDGE_CURVE ( 'NONE', #35550, #88549, #75411, .T. ) ;
#67441=VERTEX_POINT ( 'NONE', #46195 ) ;
#67460=DIRECTION ( 'NONE',  ( 0.5735764363510466035, -0.8191520442889914655, 1.003171929053524500E-16 ) ) ;
#67471=ADVANCED_FACE ( 'NONE', ( #62389 ), #20914, .T. ) ;
#67475=DIRECTION ( 'NONE',  ( 1.000000000000000000, 0.000000000000000000, 0.000000000000000000 ) ) ;
#67477=CARTESIAN_POINT ( 'NONE',  ( 35.11650669486618170, 4.898587196589411843E-16, -4.000000000000000888 ) ) ;
#67507=AXIS2_PLACEMENT_3D ( 'NONE', #39367, #57107, #97562 ) ;
#67511=ORIENTED_EDGE ( 'NONE', *, *, #63103, .T. ) ;
#67513=VECTOR ( 'NONE', #35375, 1000.000000000000000 ) ;
#67527=ADVANCED_FACE ( 'NONE', ( #87192 ), #9972, .T. ) ;
#67561=DIRECTION ( 'NONE',  ( -1.000000000000000000, -1.224606353822377258E-16, -0.000000000000000000 ) ) ;
#67572=EDGE_LOOP ( 'NONE', ( #10998, #81441, #59352, #80297, #63402, #41451 ) ) ;
#67578=AXIS2_PLACEMENT_3D ( 'NONE', #80727, #56446, #105027 ) ;
#67600=FACE_OUTER_BOUND ( 'NONE', #4086, .T. ) ;
#67641=ORIENTED_EDGE ( 'NONE', *, *, #46788, .T. ) ;
#67660=CARTESIAN_POINT ( 'NONE',  ( 12.33349330513380337, 1.593028355512270567E-15, 0.000000000000000000 ) ) ;
#67691=CARTESIAN_POINT ( 'NONE',  ( 46.84999999999999432, 1.533819458162526451E-15, 0.000000000000000000 ) ) ;
#67704=ORIENTED_EDGE ( 'NONE', *, *, #83537, .F. ) ;
#67709=CARTESIAN_POINT ( 'NONE',  ( 44.83349330513380693, 1.593028355512270567E-15, 0.000000000000000000 ) ) ;
#67735=CYLINDRICAL_SURFACE ( 'NONE', #30989, 4.000000000000000000 ) ;
#67737=LINE ( 'NONE', #34339, #30057 ) ;
#67745=ORIENTED_EDGE ( 'NONE', *, *, #98167, .T. ) ;
#67746=CARTESIAN_POINT ( 'NONE',  ( 28.86650669486618881, 4.000000000000003553, 4.898587196589414801E-16 ) ) ;
#67756=DIRECTION ( 'NONE',  ( 0.000000000000000000, -1.000000000000000000, 0.000000000000000000 ) ) ;
#67765=CARTESIAN_POINT ( 'NONE',  ( 5.975663821521244756, 4.257391242883541871, 5.625982059626890575 ) ) ;
#67786=EDGE_CURVE ( 'NONE', #45306, #97178, #65952, .T. ) ;
#67793=CARTESIAN_POINT ( 'NONE',  ( 6.289692432696767810, 6.589071317540668993, -2.245373559998994129 ) ) ;
#67797=ORIENTED_EDGE ( 'NONE', *, *, #102858, .F. ) ;
#67800=CIRCLE ( 'NONE', #81538, 4.000000000000001776 ) ;
#67801=CARTESIAN_POINT ( 'NONE',  ( 16.36650669486618881, 4.000000000000003553, 4.898587196589414801E-16 ) ) ;
#67803=( GEOMETRIC_REPRESENTATION_CONTEXT ( 3 ) GLOBAL_UNCERTAINTY_ASSIGNED_CONTEXT ( ( #100642 ) ) GLOBAL_UNIT_ASSIGNED_CONTEXT ( ( #62140, #61604, #103628 ) ) REPRESENTATION_CONTEXT ( 'NONE', 'WORKASPACE' ) );
#67813=ADVANCED_FACE ( 'NONE', ( #34152 ), #76694, .T. ) ;
#67815=CARTESIAN_POINT ( 'NONE',  ( 13.58349330513380160, 4.000000000000002665, 0.000000000000000000 ) ) ;
#67833=CIRCLE ( 'NONE', #5843, 4.000000000000000888 ) ;
#67839=AXIS2_PLACEMENT_3D ( 'NONE', #73956, #37, #98755 ) ;
#67862=ORIENTED_EDGE ( 'NONE', *, *, #84338, .T. ) ;
#67920=DIRECTION ( 'NONE',  ( 0.000000000000000000, -1.000000000000000000, 0.000000000000000000 ) ) ;
#67922=EDGE_CURVE ( 'NONE', #82432, #85998, #32484, .T. ) ;
#67927=DIRECTION ( 'NONE',  ( 0.000000000000000000, -1.000000000000000000, 0.000000000000000000 ) ) ;
#67931=EDGE_CURVE ( 'NONE', #98370, #26898, #44484, .T. ) ;
#67940=CARTESIAN_POINT ( 'NONE',  ( 23.09999999999999432, 3.309500000000003439, 0.000000000000000000 ) ) ;
#67949=AXIS2_PLACEMENT_3D ( 'NONE', #36668, #22057, #62507 ) ;
#67958=CARTESIAN_POINT ( 'NONE',  ( 0.000000000000000000, 0.000000000000000000, 0.000000000000000000 ) ) ;
#67959=CARTESIAN_POINT ( 'NONE',  ( 28.09999999999999787, 3.309500000000003439, 0.000000000000000000 ) ) ;
#67960=ORIENTED_EDGE ( 'NONE', *, *, #99080, .T. ) ;
#67968=CIRCLE ( 'NONE', #59361, 4.000000000000001776 ) ;
#67972=ADVANCED_FACE ( 'NONE', ( #77772 ), #11725, .T. ) ;
#67976=CARTESIAN_POINT ( 'NONE',  ( 0.000000000000000000, 4.898587196589412829E-16, -4.000000000000000000 ) ) ;
#68010=CARTESIAN_POINT ( 'NONE',  ( 30.11650669486618881, -3.851859888774471706E-31, 4.000000000000000888 ) ) ;
#68011=DIRECTION ( 'NONE',  ( 0.000000000000000000, -1.000000000000000000, 0.000000000000000000 ) ) ;
#68067=AXIS2_PLACEMENT_3D ( 'NONE', #105161, #32360, #6982 ) ;
#68075=LINE ( 'NONE', #66474, #43971 ) ;
#68083=DIRECTION ( 'NONE',  ( -0.5735764363510497121, 0.8191520442889892450, 1.003171929053521665E-16 ) ) ;
#68090=DIRECTION ( 'NONE',  ( -0.5735764363510494901, -0.8191520442889894671, 0.000000000000000000 ) ) ;
#68111=EDGE_CURVE ( 'NONE', #74596, #29512, #25950, .T. ) ;
#68142=DIRECTION ( 'NONE',  ( -0.5735764363510497121, 0.8191520442889892450, 1.003171929053521665E-16 ) ) ;
#68167=FACE_OUTER_BOUND ( 'NONE', #78716, .T. ) ;
#68187=LINE ( 'NONE', #2379, #57354 ) ;
#68194=ORIENTED_EDGE ( 'NONE', *, *, #56637, .T. ) ;
#68226=ORIENTED_EDGE ( 'NONE', *, *, #94916, .F. ) ;
#68228=DIRECTION ( 'NONE',  ( 0.000000000000000000, 0.000000000000000000, 1.000000000000000000 ) ) ;
#68244=CIRCLE ( 'NONE', #6241, 4.000000000000001776 ) ;
#68270=DIRECTION ( 'NONE',  ( -1.000000000000000000, -1.224606353822377258E-16, -0.000000000000000000 ) ) ;
#68295=ADVANCED_FACE ( 'NONE', ( #65701 ), #60053, .T. ) ;
#68298=EDGE_LOOP ( 'NONE', ( #99666, #22713, #16806, #38856, #39340 ) ) ;
#68302=CIRCLE ( 'NONE', #18421, 4.000000000000000888 ) ;
#68303=CARTESIAN_POINT ( 'NONE',  ( 6.222742520105473574, 7.673830019007162662, -0.2914634815676393487 ) ) ;
#68328=ORIENTED_EDGE ( 'NONE', *, *, #64924, .T. ) ;
#68352=CARTESIAN_POINT ( 'NONE',  ( 0.000000000000000000, 0.000000000000000000, 0.000000000000000000 ) ) ;
#68363=DIRECTION ( 'NONE',  ( 0.000000000000000000, -1.000000000000000000, 0.000000000000000000 ) ) ;
#68383=DIRECTION ( 'NONE',  ( 0.000000000000000000, -1.000000000000000000, 0.000000000000000000 ) ) ;
#68393=ORIENTED_EDGE ( 'NONE', *, *, #37112, .T. ) ;
#68396=CARTESIAN_POINT ( 'NONE',  ( 21.36650669486618881, -3.851859888774471706E-31, 4.000000000000000888 ) ) ;
#68411=ORIENTED_EDGE ( 'NONE', *, *, #16740, .T. ) ;
#68412=EDGE_CURVE ( 'NONE', #54043, #93508, #75912, .T. ) ;
#68417=CARTESIAN_POINT ( 'NONE',  ( 23.86650669486618881, 4.000000000000003553, 4.898587196589414801E-16 ) ) ;
#68429=CARTESIAN_POINT ( 'NONE',  ( 6.692649838135032780, 4.003395468798079726, 6.852343244299697211 ) ) ;
#68449=VERTEX_POINT ( 'NONE', #26876 ) ;
#68459=AXIS2_PLACEMENT_3D ( 'NONE', #21586, #60970, #93856 ) ;
#68465=ADVANCED_FACE ( 'NONE', ( #51630 ), #68666, .T. ) ;
#68467=B_SPLINE_CURVE_WITH_KNOTS ( 'NONE', 3,
 ( #9752, #11890, #93359, #42667, #35140 ),
 .UNSPECIFIED., .F., .F.,
 ( 4, 1, 4 ),
 ( 0.000000000000000000, 0.003752776749732569632, 0.007505553499465139264 ),
 .UNSPECIFIED. ) ;
#68477=VECTOR ( 'NONE', #47600, 1000.000000000000114 ) ;
#68484=ORIENTED_EDGE ( 'NONE', *, *, #71879, .F. ) ;
#68492=EDGE_CURVE ( 'NONE', #35999, #69803, #63499, .T. ) ;
#68502=CARTESIAN_POINT ( 'NONE',  ( 0.000000000000000000, 4.898587196589412829E-16, -4.000000000000000000 ) ) ;
#68514=CARTESIAN_POINT ( 'NONE',  ( 43.58349330513380693, 1.593028355512270567E-15, 0.000000000000000000 ) ) ;
#68517=CIRCLE ( 'NONE', #28911, 4.000000000000000888 ) ;
#68564=ORIENTED_EDGE ( 'NONE', *, *, #94287, .T. ) ;
#68574=DIRECTION ( 'NONE',  ( 1.000000000000000000, 1.224606353822377258E-16, 0.000000000000000000 ) ) ;
#68584=CIRCLE ( 'NONE', #82337, 4.000000000000000888 ) ;
#68629=DIRECTION ( 'NONE',  ( -1.000000000000000000, -1.224606353822377258E-16, -0.000000000000000000 ) ) ;
#68639=DIRECTION ( 'NONE',  ( 0.000000000000000000, 0.000000000000000000, 1.000000000000000000 ) ) ;
#68666=CONICAL_SURFACE ( 'NONE', #53188, 4.000000000000001776, 0.9599310885968808105 ) ;
#68695=ORIENTED_EDGE ( 'NONE', *, *, #102647, .F. ) ;
#68709=CIRCLE ( 'NONE', #36018, 4.000000000000000888 ) ;
#68715=CONICAL_SURFACE ( 'NONE', #22215, 4.000000000000001776, 0.9599310885968808105 ) ;
#68726=LINE ( 'NONE', #101608, #8522 ) ;
#68744=EDGE_CURVE ( 'NONE', #9776, #103460, #49237, .T. ) ;
#68753=CIRCLE ( 'NONE', #22243, 4.000000000000001776 ) ;
#68770=CARTESIAN_POINT ( 'NONE',  ( 31.84999999999999787, -3.309499999999999886, 4.475777889183790779E-16 ) ) ;
#68792=ORIENTED_EDGE ( 'NONE', *, *, #91136, .F. ) ;
#68799=DIRECTION ( 'NONE',  ( -1.000000000000000000, -0.000000000000000000, -0.000000000000000000 ) ) ;
#68828=ADVANCED_FACE ( 'NONE', ( #99921 ), #39475, .T. ) ;
#68848=ORIENTED_EDGE ( 'NONE', *, *, #5247, .T. ) ;
#68861=ORIENTED_EDGE ( 'NONE', *, *, #77459, .F. ) ;
#68871=ORIENTED_EDGE ( 'NONE', *, *, #77719, .F. ) ;
#68873=ORIENTED_EDGE ( 'NONE', *, *, #17076, .F. ) ;
#68878=CIRCLE ( 'NONE', #60265, 4.000000000000000888 ) ;
#68925=EDGE_CURVE ( 'NONE', #82896, #19223, #10374, .T. ) ;
#68936=DIRECTION ( 'NONE',  ( -0.5735764363510497121, 0.8191520442889892450, 1.003171929053521665E-16 ) ) ;
#68940=ADVANCED_FACE ( 'NONE', ( #19057 ), #53254, .T. ) ;
#68944=VERTEX_POINT ( 'NONE', #77789 ) ;
#68951=CARTESIAN_POINT ( 'NONE',  ( 0.5805565836007602343, 3.752776749732561257, -6.499999999999999112 ) ) ;
#68957=CARTESIAN_POINT ( 'NONE',  ( 6.683837171061802529, 3.955946848495958346, -6.851900933636989599 ) ) ;
#68964=ORIENTED_EDGE ( 'NONE', *, *, #5996, .F. ) ;
#68968=CARTESIAN_POINT ( 'NONE',  ( 6.466227039643102081, 2.668354129823723664, 6.840182550749403845 ) ) ;
#68988=AXIS2_PLACEMENT_3D ( 'NONE', #59297, #58215, #9648 ) ;
#68997=CARTESIAN_POINT ( 'NONE',  ( 6.338278980374460581, -2.729992536301357742, 6.499999999999423572 ) ) ;
#69006=ORIENTED_EDGE ( 'NONE', *, *, #63103, .F. ) ;
#69010=CARTESIAN_POINT ( 'NONE',  ( 43.86650669486618881, 1.474610560812782335E-15, 0.000000000000000000 ) ) ;
#69018=DIRECTION ( 'NONE',  ( 1.000000000000000000, 1.224606353822377258E-16, 0.000000000000000000 ) ) ;
#69054=DIRECTION ( 'NONE',  ( -1.000000000000000000, -1.224606353822377258E-16, -0.000000000000000000 ) ) ;
#69056=CIRCLE ( 'NONE', #22581, 4.000000000000001776 ) ;
#69062=FACE_OUTER_BOUND ( 'NONE', #47293, .T. ) ;
#69073=EDGE_LOOP ( 'NONE', ( #98332, #61929, #35778, #93617, #7929 ) ) ;
#69123=DIRECTION ( 'NONE',  ( 0.000000000000000000, -1.000000000000000000, 0.000000000000000000 ) ) ;
#69127=CARTESIAN_POINT ( 'NONE',  ( 36.36650669486618881, 1.474610560812782335E-15, 0.000000000000000000 ) ) ;
#69138=DIRECTION ( 'NONE',  ( 0.000000000000000000, -1.000000000000000000, 0.000000000000000000 ) ) ;
#69152=EDGE_LOOP ( 'NONE', ( #52764, #68393, #91652, #28392, #33687 ) ) ;
#69171=DIRECTION ( 'NONE',  ( 1.000000000000000000, 1.224606353822377258E-16, 0.000000000000000000 ) ) ;
#69183=CIRCLE ( 'NONE', #65700, 4.000000000000000888 ) ;
#69250=DIRECTION ( 'NONE',  ( 0.000000000000000000, 0.000000000000000000, -1.000000000000000000 ) ) ;
#69262=EDGE_CURVE ( 'NONE', #66178, #444, #68753, .T. ) ;
#69275=ADVANCED_FACE ( 'NONE', ( #38236 ), #77357, .T. ) ;
#69300=CARTESIAN_POINT ( 'NONE',  ( 25.59999999999999787, 1.533819458162526451E-15, 0.000000000000000000 ) ) ;
#69303=ORIENTED_EDGE ( 'NONE', *, *, #97094, .F. ) ;
#69317=CARTESIAN_POINT ( 'NONE',  ( 18.58349330513380337, -4.000000000000000000, 4.898587196589415787E-16 ) ) ;
#69331=CARTESIAN_POINT ( 'NONE',  ( 16.84999999999999787, 1.533819458162526451E-15, 0.000000000000000000 ) ) ;
#69339=EDGE_CURVE ( 'NONE', #82432, #29715, #13909, .T. ) ;
#69342=ORIENTED_EDGE ( 'NONE', *, *, #47254, .T. ) ;
#69346=APPLICATION_CONTEXT ( 'automotive_design' ) ;
#69350=ORIENTED_EDGE ( 'NONE', *, *, #92131, .T. ) ;
#69355=ORIENTED_EDGE ( 'NONE', *, *, #27868, .T. ) ;
#69407=DIRECTION ( 'NONE',  ( 1.000000000000000000, 1.224606353822377258E-16, 0.000000000000000000 ) ) ;
#69409=DIRECTION ( 'NONE',  ( -1.000000000000000000, -0.000000000000000000, -0.000000000000000000 ) ) ;
#69425=ORIENTED_EDGE ( 'NONE', *, *, #68492, .F. ) ;
#69446=EDGE_LOOP ( 'NONE', ( #5758, #33313, #63835, #6016, #32216 ) ) ;
#69456=DIRECTION ( 'NONE',  ( 0.000000000000000000, 1.000000000000000000, 0.000000000000000000 ) ) ;
#69458=LINE ( 'NONE', #54838, #34297 ) ;
#69463=EDGE_LOOP ( 'NONE', ( #92664, #39398, #32655, #7650, #54837, #42520 ) ) ;
#69479=CARTESIAN_POINT ( 'NONE',  ( 16.08349330513380337, 1.593028355512270567E-15, 0.000000000000000000 ) ) ;
#69520=CARTESIAN_POINT ( 'NONE',  ( 6.288680569791107899, 0.6514782672946227704, 6.828922012435988620 ) ) ;
#69526=CARTESIAN_POINT ( 'NONE',  ( 5.947762761376472973, 4.378239541354660425, 5.416666666666664298 ) ) ;
#69533=LINE ( 'NONE', #60917, #30090 ) ;
#69615=CARTESIAN_POINT ( 'NONE',  ( 0.000000000000000000, 0.000000000000000000, 0.000000000000000000 ) ) ;
#69658=DIRECTION ( 'NONE',  ( 1.000000000000000000, 1.224606353822377258E-16, 0.000000000000000000 ) ) ;
#69683=CARTESIAN_POINT ( 'NONE',  ( 13.09999999999999787, 3.309500000000003439, 4.052968581778167743E-16 ) ) ;
#69686=CIRCLE ( 'NONE', #105853, 8.400000000000000355 ) ;
#69707=DIRECTION ( 'NONE',  ( -0.5735764363510497121, 0.8191520442889892450, 1.003171929053521665E-16 ) ) ;
#69748=DIRECTION ( 'NONE',  ( 0.000000000000000000, -1.000000000000000000, 0.000000000000000000 ) ) ;
#69753=ADVANCED_FACE ( 'NONE', ( #55873 ), #1632, .T. ) ;
#69766=CARTESIAN_POINT ( 'NONE',  ( 41.85000000000000142, 1.533819458162526451E-15, 0.000000000000000000 ) ) ;
#69770=AXIS2_PLACEMENT_3D ( 'NONE', #46229, #55354, #39732 ) ;
#69771=CARTESIAN_POINT ( 'NONE',  ( 30.59999999999999787, 1.533819458162526451E-15, 0.000000000000000000 ) ) ;
#69792=ORIENTED_EDGE ( 'NONE', *, *, #21610, .F. ) ;
#69797=ORIENTED_EDGE ( 'NONE', *, *, #68412, .F. ) ;
#69803=VERTEX_POINT ( 'NONE', #95848 ) ;
#69807=CARTESIAN_POINT ( 'NONE',  ( 14.83349330513380337, 1.593028355512270567E-15, 0.000000000000000000 ) ) ;
#69814=VECTOR ( 'NONE', #17432, 1000.000000000000000 ) ;
#69848=DIRECTION ( 'NONE',  ( 0.000000000000000000, -1.000000000000000000, 0.000000000000000000 ) ) ;
#69853=DIRECTION ( 'NONE',  ( -1.000000000000000000, -1.224606353822377258E-16, -0.000000000000000000 ) ) ;
#69867=CARTESIAN_POINT ( 'NONE',  ( 0.01372220897661700217, 5.948365447239582160, 2.697128823393880825 ) ) ;
#69934=EDGE_CURVE ( 'NONE', #45750, #30642, #3525, .T. ) ;
#69950=PLANE ( 'NONE',  #88337 ) ;
#69952=EDGE_CURVE ( 'NONE', #25223, #32332, #3442, .T. ) ;
#69974=ORIENTED_EDGE ( 'NONE', *, *, #78187, .T. ) ;
#69994=DIRECTION ( 'NONE',  ( 0.000000000000000000, -1.000000000000000000, 0.000000000000000000 ) ) ;
#70009=PRODUCT ( 'hex flange bolt_din_DIN 6921 - M8 x 40 x 40-S', 'hex flange bolt_din_DIN 6921 - M8 x 40 x 40-S', '', ( #80541 ) ) ;
#70011=LINE ( 'NONE', #94295, #1281 ) ;
#70014=CARTESIAN_POINT ( 'NONE',  ( 6.568242156162330758, 3.336471507263037761, 6.846117829660745890 ) ) ;
#70040=DIRECTION ( 'NONE',  ( -0.5735764363510494901, -0.8191520442889894671, 0.000000000000000000 ) ) ;
#70066=ORIENTED_EDGE ( 'NONE', *, *, #36422, .T. ) ;
#70087=AXIS2_PLACEMENT_3D ( 'NONE', #73553, #1241, #50342 ) ;
#70091=CARTESIAN_POINT ( 'NONE',  ( 36.08349330513379982, 1.593028355512270567E-15, 0.000000000000000000 ) ) ;
#70098=ADVANCED_FACE ( 'NONE', ( #38560 ), #88160, .T. ) ;
#70109=DIRECTION ( 'NONE',  ( 0.000000000000000000, -1.000000000000000000, 0.000000000000000000 ) ) ;
#70128=AXIS2_PLACEMENT_3D ( 'NONE', #97687, #7607, #23849 ) ;
#70140=VECTOR ( 'NONE', #80726, 1000.000000000000000 ) ;
#70167=DIRECTION ( 'NONE',  ( 1.000000000000000000, 1.224606353822377258E-16, 0.000000000000000000 ) ) ;
#70210=FACE_OUTER_BOUND ( 'NONE', #8124, .T. ) ;
#70223=AXIS2_PLACEMENT_3D ( 'NONE', #10574, #90982, #82878 ) ;
#70231=CARTESIAN_POINT ( 'NONE',  ( 22.61650669486618526, 4.898587196589411843E-16, -4.000000000000000888 ) ) ;
#70239=DIRECTION ( 'NONE',  ( 0.000000000000000000, 1.000000000000000000, 0.000000000000000000 ) ) ;
#70250=EDGE_CURVE ( 'NONE', #82202, #46114, #65487, .T. ) ;
#70259=VERTEX_POINT ( 'NONE', #55750 ) ;
#70279=DIRECTION ( 'NONE',  ( 0.000000000000000000, -1.000000000000000000, 0.000000000000000000 ) ) ;
#70292=VERTEX_POINT ( 'NONE', #102748 ) ;
#70293=EDGE_CURVE ( 'NONE', #86482, #64980, #44791, .T. ) ;
#70308=DIRECTION ( 'NONE',  ( 0.000000000000000000, -1.000000000000000000, 0.000000000000000000 ) ) ;
#70317=DIRECTION ( 'NONE',  ( -1.000000000000000000, -1.224606353822377258E-16, -0.000000000000000000 ) ) ;
#70375=EDGE_LOOP ( 'NONE', ( #84580, #70066, #75547, #16284, #71109, #64120 ) ) ;
#70386=ORIENTED_EDGE ( 'NONE', *, *, #48459, .T. ) ;
#70402=VECTOR ( 'NONE', #79586, 1000.000000000000000 ) ;
#70423=VERTEX_POINT ( 'NONE', #10275 ) ;
#70451=CARTESIAN_POINT ( 'NONE',  ( 38.86650669486618881, 1.474610560812782335E-15, 0.000000000000000000 ) ) ;
#70454=ORIENTED_EDGE ( 'NONE', *, *, #11747, .F. ) ;
#70460=DIRECTION ( 'NONE',  ( -1.000000000000000000, -1.224606353822377258E-16, -0.000000000000000000 ) ) ;
#70463=DIRECTION ( 'NONE',  ( 0.000000000000000000, -1.000000000000000000, 0.000000000000000000 ) ) ;
#70472=EDGE_CURVE ( 'NONE', #43441, #25659, #79257, .T. ) ;
#70473=EDGE_CURVE ( 'NONE', #73270, #958, #27477, .T. ) ;
#70489=DIRECTION ( 'NONE',  ( 0.000000000000000000, -1.000000000000000000, 0.000000000000000000 ) ) ;
#70494=EDGE_CURVE ( 'NONE', #98741, #54371, #34497, .T. ) ;
#70516=VERTEX_POINT ( 'NONE', #73005 ) ;
#70548=VERTEX_POINT ( 'NONE', #63634 ) ;
#70570=FACE_OUTER_BOUND ( 'NONE', #84103, .T. ) ;
#70583=AXIS2_PLACEMENT_3D ( 'NONE', #31140, #96904, #79120 ) ;
#70598=ORIENTED_EDGE ( 'NONE', *, *, #46491, .F. ) ;
#70607=EDGE_CURVE ( 'NONE', #673, #44445, #48294, .T. ) ;
#70620=CONICAL_SURFACE ( 'NONE', #44763, 3.309500000000001663, 0.9599310885968770357 ) ;
#70631=CARTESIAN_POINT ( 'NONE',  ( 33.86650669486618881, 4.898587196589411843E-16, -4.000000000000000888 ) ) ;
#70648=ORIENTED_EDGE ( 'NONE', *, *, #26457, .F. ) ;
#70650=DIRECTION ( 'NONE',  ( 0.000000000000000000, -1.000000000000000000, 0.000000000000000000 ) ) ;
#70674=CARTESIAN_POINT ( 'NONE',  ( 11.36650669486618881, -3.999999999999998224, 0.000000000000000000 ) ) ;
#70679=DIRECTION ( 'NONE',  ( 0.000000000000000000, 1.000000000000000000, 0.000000000000000000 ) ) ;
#70716=CARTESIAN_POINT ( 'NONE',  ( 0.000000000000000000, 0.000000000000000000, 0.000000000000000000 ) ) ;
#70772=CIRCLE ( 'NONE', #32918, 4.000000000000000888 ) ;
#70785=VECTOR ( 'NONE', #62639, 1000.000000000000000 ) ;
#70835=LINE ( 'NONE', #103727, #80127 ) ;
#70860=LINE ( 'NONE', #13129, #27295 ) ;
#70866=AXIS2_PLACEMENT_3D ( 'NONE', #99123, #89989, #17180 ) ;
#70867=CIRCLE ( 'NONE', #103582, 4.000000000000001776 ) ;
#70873=DIRECTION ( 'NONE',  ( -0.5735764363510494901, -0.8191520442889894671, 0.000000000000000000 ) ) ;
#70895=ADVANCED_FACE ( 'NONE', ( #99559 ), #1789, .T. ) ;
#70900=VERTEX_POINT ( 'NONE', #74222 ) ;
#70923=EDGE_LOOP ( 'NONE', ( #76577, #96836, #35164, #61704, #2461 ) ) ;
#70931=DIRECTION ( 'NONE',  ( -1.000000000000000000, -1.224606353822377258E-16, -0.000000000000000000 ) ) ;
#70932=FACE_OUTER_BOUND ( 'NONE', #104686, .T. ) ;
#70935=LINE ( 'NONE', #78487, #80060 ) ;
#70963=VERTEX_POINT ( 'NONE', #67746 ) ;
#70966=CARTESIAN_POINT ( 'NONE',  ( 6.683837171061802529, 3.955946848495962787, 6.851900933636986935 ) ) ;
#70969=DIRECTION ( 'NONE',  ( -1.000000000000000000, -0.000000000000000000, -0.000000000000000000 ) ) ;
#70979=CARTESIAN_POINT ( 'NONE',  ( 21.08349330513380337, 1.593028355512270567E-15, 0.000000000000000000 ) ) ;
#71026=ORIENTED_EDGE ( 'NONE', *, *, #83369, .F. ) ;
#71031=CIRCLE ( 'NONE', #55532, 4.000000000000001776 ) ;
#71043=ORIENTED_EDGE ( 'NONE', *, *, #55616, .F. ) ;
#71075=CIRCLE ( 'NONE', #79694, 4.000000000000001776 ) ;
#71097=CARTESIAN_POINT ( 'NONE',  ( 6.445370176742032164, -7.262437273739264398, 1.101027156348664215 ) ) ;
#71109=ORIENTED_EDGE ( 'NONE', *, *, #16114, .F. ) ;
#71121=DIRECTION ( 'NONE',  ( 0.000000000000000000, -1.000000000000000000, 0.000000000000000000 ) ) ;
#71134=EDGE_CURVE ( 'NONE', #74736, #21068, #81131, .T. ) ;
#71139=CIRCLE ( 'NONE', #60784, 4.000000000000000888 ) ;
#71161=FACE_OUTER_BOUND ( 'NONE', #73635, .T. ) ;
#71167=ORIENTED_EDGE ( 'NONE', *, *, #76380, .F. ) ;
#71178=VECTOR ( 'NONE', #2105, 1000.000000000000000 ) ;
#71195=CARTESIAN_POINT ( 'NONE',  ( 47.33349330513379982, 1.593028355512270567E-15, 0.000000000000000000 ) ) ;
#71233=CARTESIAN_POINT ( 'NONE',  ( 13.58349330513380160, -7.703719777548943412E-31, 4.000000000000001776 ) ) ;
#71250=AXIS2_PLACEMENT_3D ( 'NONE', #33181, #9935, #92440 ) ;
#71257=DIRECTION ( 'NONE',  ( -1.000000000000000000, -1.224606353822377258E-16, -0.000000000000000000 ) ) ;
#71268=EDGE_CURVE ( 'NONE', #19223, #74776, #77416, .T. ) ;
#71274=AXIS2_PLACEMENT_3D ( 'NONE', #69615, #92266, #102509 ) ;
#71277=CYLINDRICAL_SURFACE ( 'NONE', #77185, 4.000000000000000000 ) ;
#71286=FACE_OUTER_BOUND ( 'NONE', #76373, .T. ) ;
#71296=( BOUNDED_SURFACE ( )  B_SPLINE_SURFACE ( 3, 2, ( 
 ( #79189, #100408, #2227 ),
 ( #38233, #92845, #71097 ),
 ( #84764, #54351, #19008 ),
 ( #10329, #78640, #17919 ),
 ( #4243, #10848, #92306 ),
 ( #95379, #100939, #43765 ) ),
 .UNSPECIFIED., .F., .F., .F. ) 
 B_SPLINE_SURFACE_WITH_KNOTS ( ( 4, 2, 4 ),
 ( 3, 3 ),
 ( 0.003199762745115993304, 0.007302762474435750203, 0.01140576220375550710 ),
 ( 0.000000000000000000, 1.000000000000000000 ),
 .UNSPECIFIED. ) 
 GEOMETRIC_REPRESENTATION_ITEM ( )  RATIONAL_B_SPLINE_SURFACE ( (
 ( 1.000000000000000000, 0.8047731410850428313, 1.000000000000000000),
 ( 1.000000000000000000, 0.8125552299157410285, 1.000000000000000000),
 ( 1.000000000000000000, 0.8191520442888361453, 1.000000000000000000),
 ( 1.000000000000000000, 0.8191520442891434550, 1.000000000000000000),
 ( 1.000000000000000000, 0.8125552299155105462, 1.000000000000000000),
 ( 1.000000000000000000, 0.8047731410850427203, 1.000000000000000000) ) ) 
 REPRESENTATION_ITEM ( '' )  SURFACE ( )  );
#71302=DIRECTION ( 'NONE',  ( -1.000000000000000000, -1.224606353822377258E-16, -0.000000000000000000 ) ) ;
#71348=DIRECTION ( 'NONE',  ( 0.5735764363510462704, 0.8191520442889915765, 0.000000000000000000 ) ) ;
#71362=ORIENTED_EDGE ( 'NONE', *, *, #19474, .F. ) ;
#71395=VECTOR ( 'NONE', #102023, 1000.000000000000000 ) ;
#71398=EDGE_CURVE ( 'NONE', #97567, #34125, #82802, .T. ) ;
#71401=AXIS2_PLACEMENT_3D ( 'NONE', #30689, #49482, #23649 ) ;
#71417=VECTOR ( 'NONE', #15091, 1000.000000000000000 ) ;
#71422=DIRECTION ( 'NONE',  ( -1.000000000000000000, -0.000000000000000000, -0.000000000000000000 ) ) ;
#71425=CYLINDRICAL_SURFACE ( 'NONE', #42781, 4.000000000000000000 ) ;
#71435=CIRCLE ( 'NONE', #9442, 0.5999999999999980904 ) ;
#71474=DIRECTION ( 'NONE',  ( 1.000000000000000000, 0.000000000000000000, -0.000000000000000000 ) ) ;
#71479=EDGE_CURVE ( 'NONE', #76326, #59773, #81325, .T. ) ;
#71509=DIRECTION ( 'NONE',  ( 0.000000000000000000, 0.000000000000000000, 1.000000000000000000 ) ) ;
#71514=CIRCLE ( 'NONE', #883, 4.000000000000001776 ) ;
#71593=CARTESIAN_POINT ( 'NONE',  ( 20.59999999999999787, -3.309499999999999886, 4.475777889183790779E-16 ) ) ;
#71601=CARTESIAN_POINT ( 'NONE',  ( 38.58349330513380693, 1.593028355512270567E-15, 0.000000000000000000 ) ) ;
#71605=DIRECTION ( 'NONE',  ( -1.000000000000000000, -1.224606353822377258E-16, -0.000000000000000000 ) ) ;
#71606=DIRECTION ( 'NONE',  ( -1.000000000000000000, -1.224606353822377258E-16, -0.000000000000000000 ) ) ;
#71607=FACE_OUTER_BOUND ( 'NONE', #64454, .T. ) ;
#71621=CIRCLE ( 'NONE', #57834, 3.309500000000001663 ) ;
#71638=CARTESIAN_POINT ( 'NONE',  ( 36.08349330513379982, 1.593028355512270567E-15, 0.000000000000000000 ) ) ;
#71701=LINE ( 'NONE', #104613, #76451 ) ;
#71720=EDGE_CURVE ( 'NONE', #100006, #65882, #94765, .T. ) ;
#71737=LINE ( 'NONE', #35849, #37614 ) ;
#71745=ORIENTED_EDGE ( 'NONE', *, *, #19382, .T. ) ;
#71785=B_SPLINE_CURVE_WITH_KNOTS ( 'NONE', 3,
 ( #95124, #6084, #104246, #63814, #62240, #64343 ),
 .UNSPECIFIED., .F., .F.,
 ( 4, 2, 4 ),
 ( 0.006874058789394425426, 0.008773169699889938472, 0.01067228061038544978 ),
 .UNSPECIFIED. ) ;
#71808=AXIS2_PLACEMENT_3D ( 'NONE', #99662, #27423, #19342 ) ;
#71819=AXIS2_PLACEMENT_3D ( 'NONE', #71980, #104889, #7230 ) ;
#71840=CIRCLE ( 'NONE', #15019, 4.000000000000000888 ) ;
#71874=EDGE_CURVE ( 'NONE', #21594, #84503, #9260, .T. ) ;
#71879=EDGE_CURVE ( 'NONE', #29099, #74232, #42706, .T. ) ;
#71882=FACE_OUTER_BOUND ( 'NONE', #21243, .T. ) ;
#71886=ORIENTED_EDGE ( 'NONE', *, *, #79500, .T. ) ;
#71888=ORIENTED_EDGE ( 'NONE', *, *, #58675, .T. ) ;
#71895=CIRCLE ( 'NONE', #61527, 3.309500000000001663 ) ;
#71931=DIRECTION ( 'NONE',  ( -1.000000000000000000, -0.000000000000000000, -0.000000000000000000 ) ) ;
#71938=VECTOR ( 'NONE', #47083, 1000.000000000000000 ) ;
#71962=LINE ( 'NONE', #31534, #21587 ) ;
#71966=DIRECTION ( 'NONE',  ( 0.000000000000000000, -1.000000000000000000, 0.000000000000000000 ) ) ;
#71967=AXIS2_PLACEMENT_3D ( 'NONE', #53284, #2588, #60855 ) ;
#71980=CARTESIAN_POINT ( 'NONE',  ( 27.61650669486618881, 1.474610560812782335E-15, 0.000000000000000000 ) ) ;
#71984=DIRECTION ( 'NONE',  ( 1.000000000000000000, 1.224606353822377258E-16, 0.000000000000000000 ) ) ;
#71985=DIRECTION ( 'NONE',  ( 0.000000000000000000, -1.000000000000000000, 0.000000000000000000 ) ) ;
#72001=VERTEX_POINT ( 'NONE', #27888 ) ;
#72003=AXIS2_PLACEMENT_3D ( 'NONE', #53564, #4481, #44415 ) ;
#72006=CARTESIAN_POINT ( 'NONE',  ( 41.08349330513380693, -4.000000000000000888, 4.898587196589416773E-16 ) ) ;
#72026=FACE_OUTER_BOUND ( 'NONE', #87449, .T. ) ;
#72038=CARTESIAN_POINT ( 'NONE',  ( 43.10000000000000142, 1.533819458162526451E-15, 0.000000000000000000 ) ) ;
#72043=AXIS2_PLACEMENT_3D ( 'NONE', #54521, #71257, #102033 ) ;
#72045=DIRECTION ( 'NONE',  ( 1.000000000000000000, 1.224606353822377258E-16, 0.000000000000000000 ) ) ;
#72083=EDGE_CURVE ( 'NONE', #81954, #30642, #58558, .T. ) ;
#72146=DIRECTION ( 'NONE',  ( 0.000000000000000000, 1.000000000000000000, 0.000000000000000000 ) ) ;
#72148=CARTESIAN_POINT ( 'NONE',  ( 31.36650669486618881, 4.898587196589411843E-16, -4.000000000000000888 ) ) ;
#72155=EDGE_LOOP ( 'NONE', ( #89818, #19718, #99294, #16496, #33618, #64602 ) ) ;
#72165=DIRECTION ( 'NONE',  ( 0.000000000000000000, -1.000000000000000000, 0.000000000000000000 ) ) ;
#72217=ORIENTED_EDGE ( 'NONE', *, *, #34724, .T. ) ;
#72242=CIRCLE ( 'NONE', #73918, 4.000000000000001776 ) ;
#72255=VECTOR ( 'NONE', #19228, 1000.000000000000000 ) ;
#72260=CYLINDRICAL_SURFACE ( 'NONE', #68067, 4.000000000000000000 ) ;
#72267=DIRECTION ( 'NONE',  ( 0.000000000000000000, 0.000000000000000000, 1.000000000000000000 ) ) ;
#72269=ORIENTED_EDGE ( 'NONE', *, *, #65566, .F. ) ;
#72279=DIRECTION ( 'NONE',  ( -1.000000000000000000, -1.224606353822377258E-16, -0.000000000000000000 ) ) ;
#72283=CIRCLE ( 'NONE', #99606, 3.309500000000001663 ) ;
#72304=AXIS2_PLACEMENT_3D ( 'NONE', #6449, #48499, #39385 ) ;
#72314=DIRECTION ( 'NONE',  ( -1.000000000000000000, -1.224606353822377258E-16, -0.000000000000000000 ) ) ;
#72342=CARTESIAN_POINT ( 'NONE',  ( 0.5805565836007605673, 3.752776749732565253, 6.499999999999997335 ) ) ;
#72364=CARTESIAN_POINT ( 'NONE',  ( 38.86650669486618881, 4.000000000000003553, 4.898587196589414801E-16 ) ) ;
#72372=ORIENTED_EDGE ( 'NONE', *, *, #26870, .T. ) ;
#72379=DIRECTION ( 'NONE',  ( 0.000000000000000000, 1.000000000000000000, 0.000000000000000000 ) ) ;
#72391=DIRECTION ( 'NONE',  ( -0.000000000000000000, 0.000000000000000000, -1.000000000000000000 ) ) ;
#72392=ADVANCED_FACE ( 'NONE', ( #12569 ), #39700, .T. ) ;
#72409=CARTESIAN_POINT ( 'NONE',  ( 6.162888688655346670, -3.752776749732575468, -6.499999999999999112 ) ) ;
#72411=CARTESIAN_POINT ( 'NONE',  ( 36.36650669486618881, 1.474610560812782335E-15, 0.000000000000000000 ) ) ;
#72418=CARTESIAN_POINT ( 'NONE',  ( 12.61650669486618881, -3.999999999999998224, 0.000000000000000000 ) ) ;
#72431=DIRECTION ( 'NONE',  ( -1.000000000000000000, -0.000000000000000000, -0.000000000000000000 ) ) ;
#72439=VERTEX_POINT ( 'NONE', #14684 ) ;
#72447=CIRCLE ( 'NONE', #8685, 3.309500000000001663 ) ;
#72493=CONICAL_SURFACE ( 'NONE', #19200, 4.000000000000001776, 0.9599310885968808105 ) ;
#72499=AXIS2_PLACEMENT_3D ( 'NONE', #62898, #79593, #23512 ) ;
#72515=CARTESIAN_POINT ( 'NONE',  ( 6.289692432696789126, -0.6629690750393453236, -6.828989928337168003 ) ) ;
#72518=FACE_OUTER_BOUND ( 'NONE', #57742, .T. ) ;
#72534=LINE ( 'NONE', #81148, #36642 ) ;
#72545=ORIENTED_EDGE ( 'NONE', *, *, #36422, .F. ) ;
#72554=DIRECTION ( 'NONE',  ( -1.000000000000000000, -1.224606353822377258E-16, -0.000000000000000000 ) ) ;
#72556=EDGE_CURVE ( 'NONE', #3450, #8490, #16916, .T. ) ;
#72560=DIRECTION ( 'NONE',  ( -1.000000000000000000, -1.224606353822377258E-16, -0.000000000000000000 ) ) ;
#72609=CARTESIAN_POINT ( 'NONE',  ( 16.08349330513380337, 4.000000000000002665, 0.000000000000000000 ) ) ;
#72610=AXIS2_PLACEMENT_3D ( 'NONE', #91039, #17144, #82924 ) ;
#72611=CARTESIAN_POINT ( 'NONE',  ( 15.59999999999999787, 1.533819458162526451E-15, 0.000000000000000000 ) ) ;
#72722=CARTESIAN_POINT ( 'NONE',  ( 45.59999999999999432, 3.309500000000003439, 4.052968581778167743E-16 ) ) ;
#72725=ORIENTED_EDGE ( 'NONE', *, *, #78306, .T. ) ;
#72759=DIRECTION ( 'NONE',  ( 0.5735764363510466035, -0.8191520442889914655, 1.003171929053524500E-16 ) ) ;
#72776=CARTESIAN_POINT ( 'NONE',  ( 10.11650669486618881, 1.474610560812782335E-15, 0.000000000000000000 ) ) ;
#72780=EDGE_CURVE ( 'NONE', #98423, #24472, #19025, .T. ) ;
#72800=CARTESIAN_POINT ( 'NONE',  ( 6.326592304916277776, 5.253140224433045624, -4.564380808752273033 ) ) ;
#72846=AXIS2_PLACEMENT_3D ( 'NONE', #104935, #89281, #41245 ) ;
#72869=ORIENTED_EDGE ( 'NONE', *, *, #91651, .T. ) ;
#72915=DIRECTION ( 'NONE',  ( 1.000000000000000000, 0.000000000000000000, 0.000000000000000000 ) ) ;
#72928=CIRCLE ( 'NONE', #90198, 4.000000000000001776 ) ;
#72936=LINE ( 'NONE', #15778, #40095 ) ;
#72954=EDGE_CURVE ( 'NONE', #44189, #55983, #24321, .T. ) ;
#72966=ORIENTED_EDGE ( 'NONE', *, *, #106484, .F. ) ;
#73005=CARTESIAN_POINT ( 'NONE',  ( 13.86650669486618881, 4.000000000000003553, 4.898587196589414801E-16 ) ) ;
#73023=CARTESIAN_POINT ( 'NONE',  ( 32.33349330513379982, 1.593028355512270567E-15, 0.000000000000000000 ) ) ;
#73053=EDGE_CURVE ( 'NONE', #16354, #103853, #86289, .T. ) ;
#73055=EDGE_LOOP ( 'NONE', ( #12290, #4665, #102019, #34355, #15508 ) ) ;
#73074=EDGE_CURVE ( 'NONE', #9279, #50002, #44866, .T. ) ;
#73094=EDGE_CURVE ( 'NONE', #100024, #88304, #84578, .T. ) ;
#73111=DIRECTION ( 'NONE',  ( -1.000000000000000000, -0.000000000000000000, -0.000000000000000000 ) ) ;
#73122=DIRECTION ( 'NONE',  ( 0.000000000000000000, -1.000000000000000000, 0.000000000000000000 ) ) ;
#73124=ADVANCED_FACE ( 'NONE', ( #95016 ), #98344, .T. ) ;
#73166=CARTESIAN_POINT ( 'NONE',  ( 0.2573354458087839247, 6.889406814520512512, -1.067197363239225760 ) ) ;
#73181=CIRCLE ( 'NONE', #88765, 4.000000000000000888 ) ;
#73183=ORIENTED_EDGE ( 'NONE', *, *, #44294, .T. ) ;
#73207=ADVANCED_FACE ( 'NONE', ( #106784 ), #98270, .T. ) ;
#73254=ORIENTED_EDGE ( 'NONE', *, *, #48383, .T. ) ;
#73270=VERTEX_POINT ( 'NONE', #8092 ) ;
#73285=DIRECTION ( 'NONE',  ( 0.5735764363510466035, -0.8191520442889914655, 1.003171929053524500E-16 ) ) ;
#73314=EDGE_CURVE ( 'NONE', #31200, #66609, #22553, .T. ) ;
#73346=EDGE_CURVE ( 'NONE', #15372, #16354, #60421, .T. ) ;
#73370=ORIENTED_EDGE ( 'NONE', *, *, #33450, .F. ) ;
#73382=VERTEX_POINT ( 'NONE', #60399 ) ;
#73389=CARTESIAN_POINT ( 'NONE',  ( 23.09999999999999432, 1.533819458162526451E-15, 0.000000000000000000 ) ) ;
#73418=AXIS2_PLACEMENT_3D ( 'NONE', #32827, #9043, #9571 ) ;
#73458=FACE_OUTER_BOUND ( 'NONE', #7819, .T. ) ;
#73481=AXIS2_PLACEMENT_3D ( 'NONE', #28853, #96200, #20233 ) ;
#73492=ORIENTED_EDGE ( 'NONE', *, *, #476, .T. ) ;
#73493=VECTOR ( 'NONE', #2156, 1000.000000000000000 ) ;
#73495=CARTESIAN_POINT ( 'NONE',  ( 29.83349330513380337, 4.000000000000003553, 0.000000000000000000 ) ) ;
#73514=DIRECTION ( 'NONE',  ( -1.000000000000000000, -0.000000000000000000, -0.000000000000000000 ) ) ;
#73533=EDGE_CURVE ( 'NONE', #57508, #91175, #29556, .T. ) ;
#73553=CARTESIAN_POINT ( 'NONE',  ( 45.11650669486618881, 1.474610560812782335E-15, 0.000000000000000000 ) ) ;
#73554=ORIENTED_EDGE ( 'NONE', *, *, #55616, .T. ) ;
#73573=ORIENTED_EDGE ( 'NONE', *, *, #38615, .F. ) ;
#73574=AXIS2_PLACEMENT_3D ( 'NONE', #45387, #36791, #78268 ) ;
#73584=ORIENTED_EDGE ( 'NONE', *, *, #28804, .F. ) ;
#73628=DIRECTION ( 'NONE',  ( -1.000000000000000000, -0.000000000000000000, -0.000000000000000000 ) ) ;
#73633=DIRECTION ( 'NONE',  ( -1.000000000000000000, -1.224606353822377258E-16, -0.000000000000000000 ) ) ;
#73635=EDGE_LOOP ( 'NONE', ( #81745, #59289, #59081, #33637, #39477, #42310 ) ) ;
#73672=CARTESIAN_POINT ( 'NONE',  ( 18.09999999999999787, 1.533819458162526451E-15, 0.000000000000000000 ) ) ;
#73711=CIRCLE ( 'NONE', #29050, 4.000000000000001776 ) ;
#73713=CARTESIAN_POINT ( 'NONE',  ( 19.34999999999999787, 3.309500000000003439, 4.052968581778167743E-16 ) ) ;
#73717=ORIENTED_EDGE ( 'NONE', *, *, #66560, .F. ) ;
#73762=CONICAL_SURFACE ( 'NONE', #56508, 4.000000000000001776, 0.9599310885968808105 ) ;
#73773=AXIS2_PLACEMENT_3D ( 'NONE', #94925, #43691, #44236 ) ;
#73799=ORIENTED_EDGE ( 'NONE', *, *, #16880, .F. ) ;
#73801=CONICAL_SURFACE ( 'NONE', #48010, 3.309500000000001663, 0.9599310885968770357 ) ;
#73814=ADVANCED_FACE ( 'NONE', ( #100695 ), #92076, .T. ) ;
#73834=AXIS2_PLACEMENT_3D ( 'NONE', #58904, #18453, #69123 ) ;
#73860=ADVANCED_FACE ( 'NONE', ( #9024 ), #50022, .T. ) ;
#73871=CARTESIAN_POINT ( 'NONE',  ( 6.683837171061802529, 3.955946848495958346, -6.851900933636989599 ) ) ;
#73918=AXIS2_PLACEMENT_3D ( 'NONE', #75220, #75767, #9414 ) ;
#73931=DIRECTION ( 'NONE',  ( 0.000000000000000000, -1.000000000000000000, 0.000000000000000000 ) ) ;
#73936=ORIENTED_EDGE ( 'NONE', *, *, #63991, .F. ) ;
#73940=VERTEX_POINT ( 'NONE', #43010 ) ;
#73956=CARTESIAN_POINT ( 'NONE',  ( 28.09999999999999787, 1.533819458162526451E-15, 0.000000000000000000 ) ) ;
#73965=VERTEX_POINT ( 'NONE', #67815 ) ;
#73992=DIRECTION ( 'NONE',  ( 0.000000000000000000, -1.000000000000000000, 0.000000000000000000 ) ) ;
#73995=CARTESIAN_POINT ( 'NONE',  ( 43.58349330513380693, 4.000000000000003553, 0.000000000000000000 ) ) ;
#74038=FACE_OUTER_BOUND ( 'NONE', #78780, .T. ) ;
#74064=VECTOR ( 'NONE', #81412, 1000.000000000000114 ) ;
#74066=AXIS2_PLACEMENT_3D ( 'NONE', #19134, #43888, #2883 ) ;
#74067=VERTEX_POINT ( 'NONE', #85064 ) ;
#74127=ADVANCED_FACE ( 'NONE', ( #87194 ), #31323, .T. ) ;
#74128=AXIS2_PLACEMENT_3D ( 'NONE', #43485, #19265, #67756 ) ;
#74129=DIRECTION ( 'NONE',  ( -1.000000000000000000, -1.224606353822377258E-16, -0.000000000000000000 ) ) ;
#74142=CARTESIAN_POINT ( 'NONE',  ( 11.84999999999999787, -3.309499999999999886, 4.475777889183790779E-16 ) ) ;
#74147=ORIENTED_EDGE ( 'NONE', *, *, #31336, .F. ) ;
#74173=CARTESIAN_POINT ( 'NONE',  ( 42.33349330513380693, 1.593028355512270567E-15, 0.000000000000000000 ) ) ;
#74203=EDGE_CURVE ( 'NONE', #106458, #58764, #89874, .T. ) ;
#74222=CARTESIAN_POINT ( 'NONE',  ( 0.000000000000000000, 0.000000000000000000, -6.499999999999999112 ) ) ;
#74232=VERTEX_POINT ( 'NONE', #83324 ) ;
#74285=LINE ( 'NONE', #40332, #95150 ) ;
#74297=DIRECTION ( 'NONE',  ( -1.000000000000000000, -0.000000000000000000, -0.000000000000000000 ) ) ;
#74312=AXIS2_PLACEMENT_3D ( 'NONE', #45149, #12749, #28451 ) ;
#74321=CARTESIAN_POINT ( 'NONE',  ( 47.33349330513379982, -4.000000000000000000, 4.898587196589415787E-16 ) ) ;
#74325=CARTESIAN_POINT ( 'NONE',  ( 42.61650669486618881, 4.000000000000003553, 4.898587196589414801E-16 ) ) ;
#74342=VERTEX_POINT ( 'NONE', #65555 ) ;
#74381=CARTESIAN_POINT ( 'NONE',  ( 24.83349330513380337, 1.593028355512270567E-15, 0.000000000000000000 ) ) ;
#74412=CIRCLE ( 'NONE', #100211, 3.309500000000001663 ) ;
#74414=EDGE_CURVE ( 'NONE', #57113, #67441, #98444, .T. ) ;
#74420=DIRECTION ( 'NONE',  ( -1.000000000000000000, -1.224606353822377258E-16, -0.000000000000000000 ) ) ;
#74465=VERTEX_POINT ( 'NONE', #55196 ) ;
#74530=CIRCLE ( 'NONE', #90088, 4.000000000000000888 ) ;
#74546=EDGE_CURVE ( 'NONE', #59135, #64268, #58863, .T. ) ;
#74552=VERTEX_POINT ( 'NONE', #85750 ) ;
#74578=CARTESIAN_POINT ( 'NONE',  ( 0.000000000000000000, 4.898587196589412829E-16, -4.000000000000000000 ) ) ;
#74588=DIRECTION ( 'NONE',  ( 1.000000000000000000, 1.224606353822377258E-16, 0.000000000000000000 ) ) ;
#74591=CONICAL_SURFACE ( 'NONE', #47108, 3.309500000000001663, 0.9599310885968770357 ) ;
#74592=DIRECTION ( 'NONE',  ( 0.000000000000000000, -1.000000000000000000, 0.000000000000000000 ) ) ;
#74596=VERTEX_POINT ( 'NONE', #50550 ) ;
#74651=DIRECTION ( 'NONE',  ( 0.000000000000000000, -1.000000000000000000, 0.000000000000000000 ) ) ;
#74656=ORIENTED_EDGE ( 'NONE', *, *, #25695, .F. ) ;
#74659=CARTESIAN_POINT ( 'NONE',  ( 0.06682554136337834350, 4.993536075455418555, -4.350941807883112133 ) ) ;
#74660=DIRECTION ( 'NONE',  ( -1.000000000000000000, -1.224606353822377258E-16, -0.000000000000000000 ) ) ;
#74664=ORIENTED_EDGE ( 'NONE', *, *, #86255, .T. ) ;
#74718=ORIENTED_EDGE ( 'NONE', *, *, #59344, .T. ) ;
#74736=VERTEX_POINT ( 'NONE', #36565 ) ;
#74737=CARTESIAN_POINT ( 'NONE',  ( 35.11650669486618170, 4.000000000000003553, 4.898587196589414801E-16 ) ) ;
#74752=ADVANCED_FACE ( 'NONE', ( #53242 ), #17595, .T. ) ;
#74776=VERTEX_POINT ( 'NONE', #103382 ) ;
#74799=CARTESIAN_POINT ( 'NONE',  ( 5.819846122303830249, 4.937269551422627245, -4.448398286273205215 ) ) ;
#74806=CYLINDRICAL_SURFACE ( 'NONE', #51397, 4.000000000000000000 ) ;
#74811=DIRECTION ( 'NONE',  ( 0.000000000000000000, -1.000000000000000000, 0.000000000000000000 ) ) ;
#74816=AXIS2_PLACEMENT_3D ( 'NONE', #81176, #14848, #64490 ) ;
#74822=ORIENTED_EDGE ( 'NONE', *, *, #13536, .F. ) ;
#74847=CIRCLE ( 'NONE', #28412, 4.000000000000001776 ) ;
#74848=CARTESIAN_POINT ( 'NONE',  ( 39.34999999999999432, 1.533819458162526451E-15, 0.000000000000000000 ) ) ;
#74863=VERTEX_POINT ( 'NONE', #4693 ) ;
#74866=ADVANCED_FACE ( 'NONE', ( #101783 ), #44629, .T. ) ;
#74872=CARTESIAN_POINT ( 'NONE',  ( 6.326445470157509909, 5.253846677262518305, 4.563138989068574958 ) ) ;
#74905=VERTEX_POINT ( 'NONE', #87208 ) ;
#74930=CARTESIAN_POINT ( 'NONE',  ( 16.08349330513380337, -4.000000000000000000, 4.898587196589415787E-16 ) ) ;
#74955=CONICAL_SURFACE ( 'NONE', #11200, 3.309500000000001663, 0.9599310885968770357 ) ;
#74988=CARTESIAN_POINT ( 'NONE',  ( 19.83349330513379982, -4.000000000000000888, 4.898587196589416773E-16 ) ) ;
#75018=ORIENTED_EDGE ( 'NONE', *, *, #45041, .T. ) ;
#75020=CIRCLE ( 'NONE', #88822, 4.000000000000001776 ) ;
#75040=VERTEX_POINT ( 'NONE', #106547 ) ;
#75055=CIRCLE ( 'NONE', #35466, 4.000000000000001776 ) ;
#75072=ORIENTED_EDGE ( 'NONE', *, *, #32257, .T. ) ;
#75075=ORIENTED_EDGE ( 'NONE', *, *, #27122, .T. ) ;
#75078=DIRECTION ( 'NONE',  ( 0.000000000000000000, 0.000000000000000000, 1.000000000000000000 ) ) ;
#75080=CARTESIAN_POINT ( 'NONE',  ( 35.11650669486618170, -3.999999999999998224, 0.000000000000000000 ) ) ;
#75094=CARTESIAN_POINT ( 'NONE',  ( 27.33349330513380337, 4.000000000000002665, 0.000000000000000000 ) ) ;
#75118=DIRECTION ( 'NONE',  ( -1.000000000000000000, -0.000000000000000000, -0.000000000000000000 ) ) ;
#75157=CONICAL_SURFACE ( 'NONE', #7948, 4.000000000000001776, 0.9599310885968808105 ) ;
#75205=AXIS2_PLACEMENT_3D ( 'NONE', #45764, #86778, #37717 ) ;
#75220=CARTESIAN_POINT ( 'NONE',  ( 34.83349330513379982, 1.593028355512270567E-15, 0.000000000000000000 ) ) ;
#75225=VECTOR ( 'NONE', #14259, 1000.000000000000000 ) ;
#75260=DIRECTION ( 'NONE',  ( 0.000000000000000000, -1.000000000000000000, 0.000000000000000000 ) ) ;
#75279=DIRECTION ( 'NONE',  ( 0.000000000000000000, -1.000000000000000000, 0.000000000000000000 ) ) ;
#75284=CONICAL_SURFACE ( 'NONE', #99373, 4.000000000000001776, 0.9599310885968808105 ) ;
#75295=ORIENTED_EDGE ( 'NONE', *, *, #84834, .F. ) ;
#75322=EDGE_LOOP ( 'NONE', ( #69974, #76801, #82813, #31625, #85719 ) ) ;
#75336=CARTESIAN_POINT ( 'NONE',  ( 5.947762761376473861, -2.501851166488373579, 6.500000000000000000 ) ) ;
#75362=EDGE_LOOP ( 'NONE', ( #14898, #73254, #61498, #16210, #5676, #18807 ) ) ;
#75368=ADVANCED_FACE ( 'NONE', ( #45565 ), #46166, .T. ) ;
#75407=VECTOR ( 'NONE', #17868, 1000.000000000000114 ) ;
#75411=CIRCLE ( 'NONE', #89209, 4.000000000000000888 ) ;
#75427=CARTESIAN_POINT ( 'NONE',  ( 6.683837171061806082, 7.911893696991934455, 7.436622852660996417E-19 ) ) ;
#75440=VERTEX_POINT ( 'NONE', #38537 ) ;
#75468=AXIS2_PLACEMENT_3D ( 'NONE', #63133, #13494, #98659 ) ;
#75476=LINE ( 'NONE', #76005, #71178 ) ;
#75488=CARTESIAN_POINT ( 'NONE',  ( 21.08349330513380337, 1.593028355512270567E-15, 0.000000000000000000 ) ) ;
#75531=CARTESIAN_POINT ( 'NONE',  ( 37.33349330513379982, -7.703719777548943412E-31, 4.000000000000001776 ) ) ;
#75547=ORIENTED_EDGE ( 'NONE', *, *, #48976, .T. ) ;
#75599=DIRECTION ( 'NONE',  ( 1.000000000000000000, 1.224606353822377258E-16, 0.000000000000000000 ) ) ;
#75614=AXIS2_PLACEMENT_3D ( 'NONE', #72411, #23358, #105315 ) ;
#75640=AXIS2_PLACEMENT_3D ( 'NONE', #51900, #43816, #12496 ) ;
#75641=DIRECTION ( 'NONE',  ( -1.000000000000000000, -1.224606353822377258E-16, -0.000000000000000000 ) ) ;
#75662=EDGE_LOOP ( 'NONE', ( #55571, #51041, #12892, #88044, #35121 ) ) ;
#75669=VECTOR ( 'NONE', #48864, 1000.000000000000000 ) ;
#75688=DIRECTION ( 'NONE',  ( -1.000000000000000000, -1.224606353822377258E-16, -0.000000000000000000 ) ) ;
#75691=DIRECTION ( 'NONE',  ( -1.000000000000000000, -1.224606353822377258E-16, -0.000000000000000000 ) ) ;
#75716=EDGE_LOOP ( 'NONE', ( #11760, #44666, #39288, #6327, #102484 ) ) ;
#75738=CARTESIAN_POINT ( 'NONE',  ( 9.349999999999997868, 3.309500000000003439, 0.000000000000000000 ) ) ;
#75748=CARTESIAN_POINT ( 'NONE',  ( 13.09999999999999787, 3.309500000000003439, 0.000000000000000000 ) ) ;
#75758=ORIENTED_EDGE ( 'NONE', *, *, #15786, .T. ) ;
#75767=DIRECTION ( 'NONE',  ( -1.000000000000000000, -1.224606353822377258E-16, -0.000000000000000000 ) ) ;
#75770=CARTESIAN_POINT ( 'NONE',  ( 42.33349330513380693, -4.000000000000000000, 4.898587196589415787E-16 ) ) ;
#75812=EDGE_CURVE ( 'NONE', #35969, #54043, #101285, .T. ) ;
#75817=VERTEX_POINT ( 'NONE', #7064 ) ;
#75819=CARTESIAN_POINT ( 'NONE',  ( 20.59999999999999787, 1.533819458162526451E-15, 0.000000000000000000 ) ) ;
#75828=CARTESIAN_POINT ( 'NONE',  ( 12.33349330513380337, -4.000000000000000888, 4.898587196589416773E-16 ) ) ;
#75841=DIRECTION ( 'NONE',  ( 0.000000000000000000, 0.000000000000000000, -1.000000000000000000 ) ) ;
#75843=ADVANCED_FACE ( 'NONE', ( #79893 ), #71277, .T. ) ;
#75857=VERTEX_POINT ( 'NONE', #56672 ) ;
#75881=DIRECTION ( 'NONE',  ( 0.000000000000000000, 0.000000000000000000, 1.000000000000000000 ) ) ;
#75882=VERTEX_POINT ( 'NONE', #72342 ) ;
#75912=LINE ( 'NONE', #2011, #30804 ) ;
#75925=EDGE_LOOP ( 'NONE', ( #84786, #85760, #60742, #81484, #92451 ) ) ;
#76000=CIRCLE ( 'NONE', #79469, 3.309500000000001663 ) ;
#76001=DIRECTION ( 'NONE',  ( 0.000000000000000000, 0.000000000000000000, 1.000000000000000000 ) ) ;
#76005=CARTESIAN_POINT ( 'NONE',  ( 15.59999999999999787, -3.309499999999999886, 0.000000000000000000 ) ) ;
#76006=ORIENTED_EDGE ( 'NONE', *, *, #736, .F. ) ;
#76025=ADVANCED_FACE ( 'NONE', ( #97140 ), #30784, .T. ) ;
#76029=CIRCLE ( 'NONE', #62360, 4.000000000000001776 ) ;
#76040=EDGE_LOOP ( 'NONE', ( #45136, #46996, #69350, #63932, #102963, #90821 ) ) ;
#76045=CARTESIAN_POINT ( 'NONE',  ( 43.86650669486618881, 4.000000000000003553, 4.898587196589414801E-16 ) ) ;
#76086=VERTEX_POINT ( 'NONE', #24357 ) ;
#76090=CARTESIAN_POINT ( 'NONE',  ( 22.61650669486618526, 4.000000000000003553, 4.898587196589414801E-16 ) ) ;
#76099=DIRECTION ( 'NONE',  ( -1.000000000000000000, -1.224606353822377258E-16, -0.000000000000000000 ) ) ;
#76138=CARTESIAN_POINT ( 'NONE',  ( 33.09999999999999432, 3.309500000000003439, 4.052968581778167743E-16 ) ) ;
#76157=ORIENTED_EDGE ( 'NONE', *, *, #4440, .T. ) ;
#76169=ORIENTED_EDGE ( 'NONE', *, *, #63155, .T. ) ;
#76170=DIRECTION ( 'NONE',  ( -1.000000000000000000, -1.224606353822377258E-16, -0.000000000000000000 ) ) ;
#76182=EDGE_CURVE ( 'NONE', #50002, #29335, #18695, .T. ) ;
#76194=CARTESIAN_POINT ( 'NONE',  ( 23.86650669486618881, 4.898587196589411843E-16, -4.000000000000000888 ) ) ;
#76213=VERTEX_POINT ( 'NONE', #76579 ) ;
#76221=LINE ( 'NONE', #35270, #13105 ) ;
#76237=AXIS2_PLACEMENT_3D ( 'NONE', #89669, #81534, #7659 ) ;
#76250=EDGE_CURVE ( 'NONE', #43396, #34171, #77255, .T. ) ;
#76253=ORIENTED_EDGE ( 'NONE', *, *, #56998, .F. ) ;
#76262=ORIENTED_EDGE ( 'NONE', *, *, #93644, .T. ) ;
#76296=DIRECTION ( 'NONE',  ( 0.000000000000000000, -1.000000000000000000, 0.000000000000000000 ) ) ;
#76319=VERTEX_POINT ( 'NONE', #90398 ) ;
#76326=VERTEX_POINT ( 'NONE', #72609 ) ;
#76348=ORIENTED_EDGE ( 'NONE', *, *, #64402, .F. ) ;
#76371=CARTESIAN_POINT ( 'NONE',  ( 6.585468679846623985, 7.640532685286893333, -0.2337908078075575935 ) ) ;
#76373=EDGE_LOOP ( 'NONE', ( #60768, #48156, #49588, #76157, #18053 ) ) ;
#76380=EDGE_CURVE ( 'NONE', #74905, #76835, #59218, .T. ) ;
#76395=VERTEX_POINT ( 'NONE', #70631 ) ;
#76418=ADVANCED_FACE ( 'NONE', ( #6812 ), #91053, .T. ) ;
#76436=EDGE_CURVE ( 'NONE', #78081, #15372, #23563, .T. ) ;
#76451=VECTOR ( 'NONE', #5403, 1000.000000000000000 ) ;
#76461=CARTESIAN_POINT ( 'NONE',  ( 0.000000000000000000, 2.253471898105741801E-15, 6.500000000000000000 ) ) ;
#76476=ADVANCED_FACE ( 'NONE', ( #59636 ), #92510, .T. ) ;
#76486=DIRECTION ( 'NONE',  ( -1.000000000000000000, -1.224606353822377258E-16, -0.000000000000000000 ) ) ;
#76490=ADVANCED_FACE ( 'NONE', ( #18120 ), #10527, .T. ) ;
#76496=CARTESIAN_POINT ( 'NONE',  ( 12.61650669486618881, 1.474610560812782335E-15, 0.000000000000000000 ) ) ;
#76525=VECTOR ( 'NONE', #80697, 1000.000000000000000 ) ;
#76526=FACE_OUTER_BOUND ( 'NONE', #93387, .T. ) ;
#76530=ORIENTED_EDGE ( 'NONE', *, *, #45458, .F. ) ;
#76537=CARTESIAN_POINT ( 'NONE',  ( 0.000000000000000000, 4.898587196589412829E-16, -4.000000000000000000 ) ) ;
#76555=CIRCLE ( 'NONE', #67949, 4.000000000000001776 ) ;
#76567=EDGE_LOOP ( 'NONE', ( #41220, #21273, #44764, #80867, #68871 ) ) ;
#76577=ORIENTED_EDGE ( 'NONE', *, *, #26697, .T. ) ;
#76579=CARTESIAN_POINT ( 'NONE',  ( 0.5805565836007605673, -3.752776749732561257, 6.500000000000000000 ) ) ;
#76605=DIRECTION ( 'NONE',  ( 1.000000000000000000, 1.224606353822377258E-16, 0.000000000000000000 ) ) ;
#76673=AXIS2_PLACEMENT_3D ( 'NONE', #62764, #95657, #54630 ) ;
#76688=CARTESIAN_POINT ( 'NONE',  ( 24.34999999999999787, 3.309500000000003439, 4.052968581778167743E-16 ) ) ;
#76694=CYLINDRICAL_SURFACE ( 'NONE', #18550, 4.000000000000000000 ) ;
#76696=DIRECTION ( 'NONE',  ( 0.000000000000000000, -1.000000000000000000, 0.000000000000000000 ) ) ;
#76701=DIRECTION ( 'NONE',  ( 0.000000000000000000, 1.000000000000000000, 0.000000000000000000 ) ) ;
#76704=CARTESIAN_POINT ( 'NONE',  ( 34.35000000000000142, 3.309500000000003439, 4.052968581778167743E-16 ) ) ;
#76712=ORIENTED_EDGE ( 'NONE', *, *, #95248, .T. ) ;
#76726=CIRCLE ( 'NONE', #54306, 4.000000000000000888 ) ;
#76747=CARTESIAN_POINT ( 'NONE',  ( 23.09999999999999432, 1.533819458162526451E-15, 0.000000000000000000 ) ) ;
#76793=CARTESIAN_POINT ( 'NONE',  ( 6.445370176742030388, -7.262437273739259957, -1.101027156348882041 ) ) ;
#76801=ORIENTED_EDGE ( 'NONE', *, *, #58055, .T. ) ;
#76823=FACE_OUTER_BOUND ( 'NONE', #28290, .T. ) ;
#76835=VERTEX_POINT ( 'NONE', #10867 ) ;
#76867=CARTESIAN_POINT ( 'NONE',  ( 37.33349330513379982, -4.000000000000000000, 4.898587196589415787E-16 ) ) ;
#76870=CARTESIAN_POINT ( 'NONE',  ( 15.59999999999999787, 1.533819458162526451E-15, 0.000000000000000000 ) ) ;
#76875=CARTESIAN_POINT ( 'NONE',  ( 36.84999999999999432, -3.309499999999999886, 4.475777889183790779E-16 ) ) ;
#76898=AXIS2_PLACEMENT_3D ( 'NONE', #56002, #87886, #54415 ) ;
#76903=EDGE_CURVE ( 'NONE', #76395, #70292, #87665, .T. ) ;
#76906=( GEOMETRIC_REPRESENTATION_CONTEXT ( 3 ) GLOBAL_UNCERTAINTY_ASSIGNED_CONTEXT ( ( #24797 ) ) GLOBAL_UNIT_ASSIGNED_CONTEXT ( ( #40714, #87698, #88225 ) ) REPRESENTATION_CONTEXT ( 'NONE', 'WORKASPACE' ) );
#76929=VERTEX_POINT ( 'NONE', #55569 ) ;
#76948=FACE_OUTER_BOUND ( 'NONE', #65448, .T. ) ;
#76968=( BOUNDED_SURFACE ( )  B_SPLINE_SURFACE ( 3, 2, ( 
 ( #90870, #34789, #60123 ),
 ( #35317, #49862, #10988 ),
 ( #43905, #1832, #83823 ),
 ( #51985, #83296, #50913 ),
 ( #99466, #92987, #76793 ),
 ( #92439, #51457, #26178 ) ),
 .UNSPECIFIED., .F., .F., .F. ) 
 B_SPLINE_SURFACE_WITH_KNOTS ( ( 4, 2, 4 ),
 ( 3, 3 ),
 ( 0.003199762745116010217, 0.007302762474435760612, 0.01140576220375551057 ),
 ( 0.000000000000000000, 1.000000000000000000 ),
 .UNSPECIFIED. ) 
 GEOMETRIC_REPRESENTATION_ITEM ( )  RATIONAL_B_SPLINE_SURFACE ( (
 ( 1.000000000000000000, 0.8047731410850426093, 1.000000000000000000),
 ( 1.000000000000000000, 0.8125552299153950830, 1.000000000000000000),
 ( 1.000000000000000000, 0.8191520442892971099, 1.000000000000000000),
 ( 1.000000000000000000, 0.8191520442886824904, 1.000000000000000000),
 ( 1.000000000000000000, 0.8125552299158561587, 1.000000000000000000),
 ( 1.000000000000000000, 0.8047731410850428313, 1.000000000000000000) ) ) 
 REPRESENTATION_ITEM ( '' )  SURFACE ( )  );
#76999=ORIENTED_EDGE ( 'NONE', *, *, #97368, .F. ) ;
#77002=FACE_OUTER_BOUND ( 'NONE', #69073, .T. ) ;
#77004=LINE ( 'NONE', #3121, #575 ) ;
#77009=ORIENTED_EDGE ( 'NONE', *, *, #64563, .T. ) ;
#77033=ORIENTED_EDGE ( 'NONE', *, *, #57378, .T. ) ;
#77069=CIRCLE ( 'NONE', #30593, 4.000000000000001776 ) ;
#77070=CARTESIAN_POINT ( 'NONE',  ( 26.08349330513380337, -7.703719777548943412E-31, 4.000000000000001776 ) ) ;
#77096=VECTOR ( 'NONE', #28929, 1000.000000000000000 ) ;
#77104=ADVANCED_FACE ( 'NONE', ( #28051 ), #37796, .T. ) ;
#77135=DIRECTION ( 'NONE',  ( -1.000000000000000000, -1.224606353822377258E-16, -0.000000000000000000 ) ) ;
#77149=VERTEX_POINT ( 'NONE', #10742 ) ;
#77156=CARTESIAN_POINT ( 'NONE',  ( 20.11650669486618881, 1.474610560812782335E-15, 0.000000000000000000 ) ) ;
#77172=ORIENTED_EDGE ( 'NONE', *, *, #2980, .F. ) ;
#77185=AXIS2_PLACEMENT_3D ( 'NONE', #31390, #22232, #29799 ) ;
#77187=FACE_OUTER_BOUND ( 'NONE', #31025, .T. ) ;
#77224=CARTESIAN_POINT ( 'NONE',  ( 46.08349330513379982, 4.000000000000003553, 0.000000000000000000 ) ) ;
#77242=AXIS2_PLACEMENT_3D ( 'NONE', #6454, #39390, #80879 ) ;
#77255=CIRCLE ( 'NONE', #37649, 3.309500000000001663 ) ;
#77294=VERTEX_POINT ( 'NONE', #5846 ) ;
#77299=VERTEX_POINT ( 'NONE', #53869 ) ;
#77321=DIRECTION ( 'NONE',  ( 0.000000000000000000, -1.000000000000000000, 0.000000000000000000 ) ) ;
#77337=VERTEX_POINT ( 'NONE', #98442 ) ;
#77343=CARTESIAN_POINT ( 'NONE',  ( 46.84999999999999432, 1.533819458162526451E-15, 0.000000000000000000 ) ) ;
#77357=CONICAL_SURFACE ( 'NONE', #30871, 3.309500000000001663, 0.9599310885968770357 ) ;
#77380=EDGE_CURVE ( 'NONE', #53956, #56662, #72242, .T. ) ;
#77394=DIRECTION ( 'NONE',  ( -0.5735764363510494901, -0.8191520442889894671, 0.000000000000000000 ) ) ;
#77416=CIRCLE ( 'NONE', #30954, 4.000000000000001776 ) ;
#77440=ORIENTED_EDGE ( 'NONE', *, *, #1983, .F. ) ;
#77457=ORIENTED_EDGE ( 'NONE', *, *, #19197, .T. ) ;
#77459=EDGE_CURVE ( 'NONE', #18, #48447, #104975, .T. ) ;
#77480=ORIENTED_EDGE ( 'NONE', *, *, #11571, .T. ) ;
#77494=AXIS2_PLACEMENT_3D ( 'NONE', #35431, #77983, #92564 ) ;
#77495=DIRECTION ( 'NONE',  ( -1.000000000000000000, -0.000000000000000000, -0.000000000000000000 ) ) ;
#77536=CARTESIAN_POINT ( 'NONE',  ( 6.692649149972418776, -4.003391779698783459, -6.852343209863736462 ) ) ;
#77539=AXIS2_PLACEMENT_3D ( 'NONE', #101130, #27290, #60173 ) ;
#77542=CARTESIAN_POINT ( 'NONE',  ( 0.05613245601036488674, 1.278525034529254034, 6.499999999999999112 ) ) ;
#77544=DIRECTION ( 'NONE',  ( -1.000000000000000000, -0.000000000000000000, -0.000000000000000000 ) ) ;
#77579=DIRECTION ( 'NONE',  ( 0.000000000000000000, -1.000000000000000000, 0.000000000000000000 ) ) ;
#77591=VERTEX_POINT ( 'NONE', #50940 ) ;
#77597=ADVANCED_FACE ( 'NONE', ( #76823 ), #98106, .T. ) ;
#77600=VERTEX_POINT ( 'NONE', #86551 ) ;
#77607=CARTESIAN_POINT ( 'NONE',  ( 5.818834259648034468, 0.6677920147391552819, 6.499999999999999112 ) ) ;
#77613=CARTESIAN_POINT ( 'NONE',  ( 6.162888688655344005, 3.752776749732565253, 6.499999999999997335 ) ) ;
#77634=CARTESIAN_POINT ( 'NONE',  ( 6.162888688655344005, 3.752776749732561257, -6.499999999999999112 ) ) ;
#77668=VERTEX_POINT ( 'NONE', #45020 ) ;
#77669=VECTOR ( 'NONE', #21349, 1000.000000000000114 ) ;
#77674=ORIENTED_EDGE ( 'NONE', *, *, #37496, .T. ) ;
#77684=VERTEX_POINT ( 'NONE', #43935 ) ;
#77685=VERTEX_POINT ( 'NONE', #84930 ) ;
#77689=VECTOR ( 'NONE', #25898, 1000.000000000000000 ) ;
#77705=LINE ( 'NONE', #3283, #61569 ) ;
#77713=DIRECTION ( 'NONE',  ( -1.000000000000000000, -1.224606353822377258E-16, -0.000000000000000000 ) ) ;
#77719=EDGE_CURVE ( 'NONE', #7464, #56846, #63723, .T. ) ;
#77720=CARTESIAN_POINT ( 'NONE',  ( 8.099999999999999645, 7.505553499465140277, 0.000000000000000000 ) ) ;
#77735=CARTESIAN_POINT ( 'NONE',  ( 23.58349330513380337, 1.593028355512270567E-15, 0.000000000000000000 ) ) ;
#77743=CARTESIAN_POINT ( 'NONE',  ( 43.10000000000000142, 1.533819458162526451E-15, 0.000000000000000000 ) ) ;
#77768=EDGE_CURVE ( 'NONE', #29102, #21068, #58553, .T. ) ;
#77772=FACE_OUTER_BOUND ( 'NONE', #85585, .T. ) ;
#77776=CARTESIAN_POINT ( 'NONE',  ( 45.59999999999999432, 1.533819458162526451E-15, 0.000000000000000000 ) ) ;
#77785=CYLINDRICAL_SURFACE ( 'NONE', #99116, 4.000000000000000000 ) ;
#77786=CARTESIAN_POINT ( 'NONE',  ( 40.11650669486618881, 1.474610560812782335E-15, 0.000000000000000000 ) ) ;
#77789=CARTESIAN_POINT ( 'NONE',  ( 38.58349330513380693, 4.000000000000002665, 0.000000000000000000 ) ) ;
#77799=CARTESIAN_POINT ( 'NONE',  ( 28.09999999999999787, 1.533819458162526451E-15, 0.000000000000000000 ) ) ;
#77823=VERTEX_POINT ( 'NONE', #47103 ) ;
#77858=FACE_OUTER_BOUND ( 'NONE', #29197, .T. ) ;
#77864=CARTESIAN_POINT ( 'NONE',  ( 5.691929483231185749, -5.629165124598853431, 3.250000000000002220 ) ) ;
#77870=DIRECTION ( 'NONE',  ( -0.5735764363510497121, 0.8191520442889892450, 1.003171929053521665E-16 ) ) ;
#77885=ORIENTED_EDGE ( 'NONE', *, *, #96973, .T. ) ;
#77913=EDGE_LOOP ( 'NONE', ( #48045, #47411, #26156, #72545, #71043 ) ) ;
#77956=CARTESIAN_POINT ( 'NONE',  ( 28.58349330513380337, 1.593028355512270567E-15, 0.000000000000000000 ) ) ;
#77976=ADVANCED_FACE ( 'NONE', ( #74038 ), #101588, .T. ) ;
#77983=DIRECTION ( 'NONE',  ( -1.000000000000000000, -0.000000000000000000, -0.000000000000000000 ) ) ;
#77990=EDGE_CURVE ( 'NONE', #19064, #53956, #50296, .T. ) ;
#78005=B_SPLINE_CURVE_WITH_KNOTS ( 'NONE', 3,
 ( #80631, #1288, #10464, #74659, #744, #1833, #25090, #49863 ),
 .UNSPECIFIED., .F., .F.,
 ( 4, 2, 2, 4 ),
 ( 0.003797433802554452380, 0.004743183970586248299, 0.005688934138618042917, 0.007580434474681632152 ),
 .UNSPECIFIED. ) ;
#78037=CARTESIAN_POINT ( 'NONE',  ( 36.08349330513379982, -4.000000000000000888, 4.898587196589416773E-16 ) ) ;
#78051=DIRECTION ( 'NONE',  ( -1.000000000000000000, -0.000000000000000000, -0.000000000000000000 ) ) ;
#78066=VERTEX_POINT ( 'NONE', #78291 ) ;
#78081=VERTEX_POINT ( 'NONE', #60545 ) ;
#78087=DIRECTION ( 'NONE',  ( 0.000000000000000000, -1.000000000000000000, 0.000000000000000000 ) ) ;
#78151=AXIS2_PLACEMENT_3D ( 'NONE', #60841, #29561, #85649 ) ;
#78173=EDGE_LOOP ( 'NONE', ( #49567, #61380, #66161, #54076, #41185 ) ) ;
#78178=ADVANCED_FACE ( 'NONE', ( #2263 ), #61610, .T. ) ;
#78187=EDGE_CURVE ( 'NONE', #35426, #57692, #1771, .T. ) ;
#78201=EDGE_CURVE ( 'NONE', #87130, #11128, #43278, .T. ) ;
#78261=ADVANCED_FACE ( 'NONE', ( #70210 ), #103112, .T. ) ;
#78268=DIRECTION ( 'NONE',  ( 0.000000000000000000, -1.000000000000000000, 0.000000000000000000 ) ) ;
#78286=EDGE_LOOP ( 'NONE', ( #104183, #65730, #89249, #104390, #102649 ) ) ;
#78287=AXIS2_PLACEMENT_3D ( 'NONE', #45499, #20732, #85963 ) ;
#78291=CARTESIAN_POINT ( 'NONE',  ( 9.833493305133801599, -4.000000000000000888, 4.898587196589416773E-16 ) ) ;
#78300=DIRECTION ( 'NONE',  ( 0.000000000000000000, 0.000000000000000000, 1.000000000000000000 ) ) ;
#78306=EDGE_CURVE ( 'NONE', #34171, #35056, #92883, .T. ) ;
#78345=ORIENTED_EDGE ( 'NONE', *, *, #103254, .T. ) ;
#78356=CARTESIAN_POINT ( 'NONE',  ( 36.08349330513379982, 1.593028355512270567E-15, 0.000000000000000000 ) ) ;
#78394=CARTESIAN_POINT ( 'NONE',  ( 0.000000000000000000, 4.898587196589412829E-16, -4.000000000000000000 ) ) ;
#78409=VERTEX_POINT ( 'NONE', #30300 ) ;
#78424=VECTOR ( 'NONE', #2815, 1000.000000000000000 ) ;
#78428=CARTESIAN_POINT ( 'NONE',  ( 46.08349330513379982, 4.000000000000002665, 0.000000000000000000 ) ) ;
#78432=DIRECTION ( 'NONE',  ( 0.000000000000000000, 1.000000000000000000, 0.000000000000000000 ) ) ;
#78445=CARTESIAN_POINT ( 'NONE',  ( 39.34999999999999432, 3.309500000000003439, 4.052968581778167743E-16 ) ) ;
#78464=DIRECTION ( 'NONE',  ( -1.000000000000000000, -1.224606353822377258E-16, -0.000000000000000000 ) ) ;
#78483=CIRCLE ( 'NONE', #50906, 4.000000000000001776 ) ;
#78487=CARTESIAN_POINT ( 'NONE',  ( 12.33349330513380337, -4.000000000000000000, 4.898587196589415787E-16 ) ) ;
#78514=ORIENTED_EDGE ( 'NONE', *, *, #43222, .F. ) ;
#78516=DIRECTION ( 'NONE',  ( -1.000000000000000000, -1.224606353822377258E-16, -0.000000000000000000 ) ) ;
#78535=CIRCLE ( 'NONE', #13151, 3.309500000000001663 ) ;
#78536=EDGE_LOOP ( 'NONE', ( #31920, #19580, #61305, #8063 ) ) ;
#78571=ORIENTED_EDGE ( 'NONE', *, *, #58100, .T. ) ;
#78572=CARTESIAN_POINT ( 'NONE',  ( 36.84999999999999432, 3.309500000000003439, 0.000000000000000000 ) ) ;
#78595=AXIS2_PLACEMENT_3D ( 'NONE', #90518, #16631, #58696 ) ;
#78596=ORIENTED_EDGE ( 'NONE', *, *, #56998, .T. ) ;
#78628=ORIENTED_EDGE ( 'NONE', *, *, #89999, .F. ) ;
#78640=CARTESIAN_POINT ( 'NONE',  ( 6.169949891408688991, -4.949864754179184700, 4.426582755167964400 ) ) ;
#78645=VECTOR ( 'NONE', #18610, 1000.000000000000000 ) ;
#78673=DIRECTION ( 'NONE',  ( 1.000000000000000000, 1.224606353822377258E-16, 0.000000000000000000 ) ) ;
#78694=DIRECTION ( 'NONE',  ( 0.000000000000000000, -1.000000000000000000, 0.000000000000000000 ) ) ;
#78716=EDGE_LOOP ( 'NONE', ( #22802, #60886, #16416, #936, #89695 ) ) ;
#78766=CIRCLE ( 'NONE', #59861, 4.000000000000000888 ) ;
#78767=VERTEX_POINT ( 'NONE', #81856 ) ;
#78780=EDGE_LOOP ( 'NONE', ( #49714, #59324, #92118, #22068, #83834 ) ) ;
#78785=VERTEX_POINT ( 'NONE', #65704 ) ;
#78835=LINE ( 'NONE', #38409, #51566 ) ;
#78868=ORIENTED_EDGE ( 'NONE', *, *, #97090, .F. ) ;
#78906=CIRCLE ( 'NONE', #23816, 3.309500000000001663 ) ;
#78914=DIRECTION ( 'NONE',  ( 0.000000000000000000, 0.000000000000000000, 1.000000000000000000 ) ) ;
#78963=DIRECTION ( 'NONE',  ( -1.000000000000000000, -1.224606353822377258E-16, -0.000000000000000000 ) ) ;
#78974=VECTOR ( 'NONE', #77495, 1000.000000000000000 ) ;
#79030=DIRECTION ( 'NONE',  ( 0.000000000000000000, -1.000000000000000000, 0.000000000000000000 ) ) ;
#79064=ORIENTED_EDGE ( 'NONE', *, *, #26899, .T. ) ;
#79083=VECTOR ( 'NONE', #49725, 1000.000000000000114 ) ;
#79101=DIRECTION ( 'NONE',  ( 1.000000000000000000, 0.000000000000000000, -0.000000000000000000 ) ) ;
#79117=CARTESIAN_POINT ( 'NONE',  ( 46.84999999999999432, 1.533819458162526451E-15, 0.000000000000000000 ) ) ;
#79120=DIRECTION ( 'NONE',  ( 0.000000000000000000, -1.000000000000000000, 0.000000000000000000 ) ) ;
#79124=ORIENTED_EDGE ( 'NONE', *, *, #93806, .T. ) ;
#79133=ORIENTED_EDGE ( 'NONE', *, *, #9345, .F. ) ;
#79138=CARTESIAN_POINT ( 'NONE',  ( 37.61650669486618881, 1.474610560812782335E-15, 0.000000000000000000 ) ) ;
#79163=CARTESIAN_POINT ( 'NONE',  ( 41.36650669486618881, 1.474610560812782335E-15, 0.000000000000000000 ) ) ;
#79189=CARTESIAN_POINT ( 'NONE',  ( 6.222742520105477126, -7.673830019007173320, -0.2914634815676439561 ) ) ;
#79191=LINE ( 'NONE', #38235, #31617 ) ;
#79192=VECTOR ( 'NONE', #70040, 1000.000000000000000 ) ;
#79217=DIRECTION ( 'NONE',  ( 0.000000000000000000, 1.000000000000000000, 0.000000000000000000 ) ) ;
#79244=CARTESIAN_POINT ( 'NONE',  ( 0.4033376246892507733, -4.059728990630811829, -5.968343123267133343 ) ) ;
#79256=EDGE_CURVE ( 'NONE', #85984, #80639, #47131, .T. ) ;
#79257=CIRCLE ( 'NONE', #20744, 4.000000000000001776 ) ;
#79278=EDGE_CURVE ( 'NONE', #34518, #866, #65550, .T. ) ;
#79280=ORIENTED_EDGE ( 'NONE', *, *, #28581, .F. ) ;
#79288=FACE_OUTER_BOUND ( 'NONE', #38918, .T. ) ;
#79294=CARTESIAN_POINT ( 'NONE',  ( 25.11650669486618881, 4.000000000000003553, 4.898587196589414801E-16 ) ) ;
#79309=LINE ( 'NONE', #62613, #74064 ) ;
#79347=ORIENTED_EDGE ( 'NONE', *, *, #70607, .T. ) ;
#79365=CARTESIAN_POINT ( 'NONE',  ( 23.86650669486618881, 1.474610560812782335E-15, 0.000000000000000000 ) ) ;
#79399=AXIS2_PLACEMENT_3D ( 'NONE', #19962, #29126, #85734 ) ;
#79413=EDGE_LOOP ( 'NONE', ( #63633, #12187, #43785, #92943, #23249, #34912 ) ) ;
#79431=VERTEX_POINT ( 'NONE', #2565 ) ;
#79432=DIRECTION ( 'NONE',  ( -0.000000000000000000, 0.8660254037844382635, 0.5000000000000006661 ) ) ;
#79469=AXIS2_PLACEMENT_3D ( 'NONE', #61864, #12213, #34938 ) ;
#79471=CARTESIAN_POINT ( 'NONE',  ( 8.099999999999999645, -7.505553499465148271, 0.000000000000000000 ) ) ;
#79483=AXIS2_PLACEMENT_3D ( 'NONE', #104021, #30163, #63049 ) ;
#79485=EDGE_CURVE ( 'NONE', #52531, #81845, #57726, .T. ) ;
#79500=EDGE_CURVE ( 'NONE', #65882, #100006, #51902, .T. ) ;
#79507=DIRECTION ( 'NONE',  ( -0.000000000000000000, 1.000000000000000000, 1.224646799147353207E-16 ) ) ;
#79524=EDGE_LOOP ( 'NONE', ( #12780, #101182, #74664, #27791, #83305 ) ) ;
#79555=CARTESIAN_POINT ( 'NONE',  ( 31.08349330513380337, 1.593028355512270567E-15, 0.000000000000000000 ) ) ;
#79586=DIRECTION ( 'NONE',  ( -0.5735764363510494901, -0.8191520442889894671, 0.000000000000000000 ) ) ;
#79593=DIRECTION ( 'NONE',  ( -1.000000000000000000, -1.224606353822377258E-16, -0.000000000000000000 ) ) ;
#79596=CARTESIAN_POINT ( 'NONE',  ( 19.34999999999999787, 3.309500000000003439, 0.000000000000000000 ) ) ;
#79598=VERTEX_POINT ( 'NONE', #76045 ) ;
#79606=CARTESIAN_POINT ( 'NONE',  ( 23.09999999999999432, -3.309499999999999886, 0.000000000000000000 ) ) ;
#79613=B_SPLINE_CURVE_WITH_KNOTS ( 'NONE', 3,
 ( #45654, #28987, #38632, #39160, #63442, #103866, #86132, #4128, #30016, #61314 ),
 .UNSPECIFIED., .F., .F.,
 ( 4, 2, 2, 2, 4 ),
 ( 0.000000000000000000, 0.001993803085173303895, 0.003987606170346607790, 0.005981409255519911684, 0.007975212340693215579 ),
 .UNSPECIFIED. ) ;
#79641=DIRECTION ( 'NONE',  ( -1.000000000000000000, -1.224606353822377258E-16, -0.000000000000000000 ) ) ;
#79646=EDGE_CURVE ( 'NONE', #63451, #92028, #7089, .T. ) ;
#79657=EDGE_CURVE ( 'NONE', #55862, #7464, #3654, .T. ) ;
#79660=DIRECTION ( 'NONE',  ( -1.000000000000000000, -1.224606353822377258E-16, -0.000000000000000000 ) ) ;
#79673=FACE_OUTER_BOUND ( 'NONE', #22533, .T. ) ;
#79681=DIRECTION ( 'NONE',  ( -1.000000000000000000, -1.224606353822377258E-16, -0.000000000000000000 ) ) ;
#79690=ORIENTED_EDGE ( 'NONE', *, *, #46202, .F. ) ;
#79694=AXIS2_PLACEMENT_3D ( 'NONE', #62397, #35485, #19328 ) ;
#79705=CARTESIAN_POINT ( 'NONE',  ( 40.11650669486618881, 1.474610560812782335E-15, 0.000000000000000000 ) ) ;
#79707=CARTESIAN_POINT ( 'NONE',  ( 38.58349330513380693, 1.593028355512270567E-15, 0.000000000000000000 ) ) ;
#79712=ORIENTED_EDGE ( 'NONE', *, *, #44488, .T. ) ;
#79719=DIRECTION ( 'NONE',  ( 0.5735764363510466035, -0.8191520442889914655, 1.003171929053524500E-16 ) ) ;
#79772=EDGE_LOOP ( 'NONE', ( #26051, #57447, #4335, #34613, #65925, #104915 ) ) ;
#79773=ADVANCED_FACE ( 'NONE', ( #40370 ), #32308, .T. ) ;
#79792=CARTESIAN_POINT ( 'NONE',  ( 28.58349330513380337, 1.593028355512270567E-15, 0.000000000000000000 ) ) ;
#79794=CIRCLE ( 'NONE', #53917, 4.000000000000000888 ) ;
#79802=AXIS2_PLACEMENT_3D ( 'NONE', #11795, #1570, #85172 ) ;
#79810=EDGE_LOOP ( 'NONE', ( #16835, #20299, #37538, #38969, #6544 ) ) ;
#79823=ORIENTED_EDGE ( 'NONE', *, *, #47254, .F. ) ;
#79826=LINE ( 'NONE', #22695, #71417 ) ;
#79828=EDGE_CURVE ( 'NONE', #92046, #21079, #106691, .T. ) ;
#79838=AXIS2_PLACEMENT_3D ( 'NONE', #44769, #33624, #45822 ) ;
#79845=VERTEX_POINT ( 'NONE', #15562 ) ;
#79852=DIRECTION ( 'NONE',  ( 0.5735764363510466035, -0.8191520442889914655, 1.003171929053524500E-16 ) ) ;
#79860=EDGE_CURVE ( 'NONE', #80889, #30981, #10561, .T. ) ;
#79869=VECTOR ( 'NONE', #28293, 999.9999999999998863 ) ;
#79890=VERTEX_POINT ( 'NONE', #106152 ) ;
#79893=FACE_OUTER_BOUND ( 'NONE', #32740, .T. ) ;
#79902=DIRECTION ( 'NONE',  ( -1.000000000000000000, -1.224606353822377258E-16, -0.000000000000000000 ) ) ;
#79906=VERTEX_POINT ( 'NONE', #74325 ) ;
#79933=ORIENTED_EDGE ( 'NONE', *, *, #35901, .F. ) ;
#79948=ORIENTED_EDGE ( 'NONE', *, *, #73314, .T. ) ;
#79953=DIRECTION ( 'NONE',  ( 0.000000000000000000, -0.5000000000000006661, 0.8660254037844382635 ) ) ;
#79983=ORIENTED_EDGE ( 'NONE', *, *, #43711, .F. ) ;
#79998=ADVANCED_FACE ( 'NONE', ( #51647 ), #93028, .T. ) ;
#80015=ORIENTED_EDGE ( 'NONE', *, *, #5983, .T. ) ;
#80045=LINE ( 'NONE', #6694, #85472 ) ;
#80046=EDGE_CURVE ( 'NONE', #56846, #87110, #93266, .T. ) ;
#80060=VECTOR ( 'NONE', #37547, 1000.000000000000000 ) ;
#80064=AXIS2_PLACEMENT_3D ( 'NONE', #95894, #54875, #5292 ) ;
#80067=LINE ( 'NONE', #88180, #77669 ) ;
#80081=ORIENTED_EDGE ( 'NONE', *, *, #99080, .F. ) ;
#80107=CARTESIAN_POINT ( 'NONE',  ( 41.08349330513380693, 1.593028355512270567E-15, 0.000000000000000000 ) ) ;
#80115=ORIENTED_EDGE ( 'NONE', *, *, #73346, .F. ) ;
#80121=CIRCLE ( 'NONE', #100990, 3.309500000000001663 ) ;
#80127=VECTOR ( 'NONE', #95647, 1000.000000000000000 ) ;
#80136=VECTOR ( 'NONE', #106301, 1000.000000000000114 ) ;
#80148=AXIS2_PLACEMENT_3D ( 'NONE', #98697, #15665, #81448 ) ;
#80192=EDGE_CURVE ( 'NONE', #77294, #77299, #8633, .T. ) ;
#80206=VERTEX_POINT ( 'NONE', #105512 ) ;
#80226=CARTESIAN_POINT ( 'NONE',  ( 41.08349330513380693, 1.593028355512270567E-15, 0.000000000000000000 ) ) ;
#80229=ORIENTED_EDGE ( 'NONE', *, *, #97831, .T. ) ;
#80231=ORIENTED_EDGE ( 'NONE', *, *, #67786, .F. ) ;
#80232=CARTESIAN_POINT ( 'NONE',  ( 19.83349330513379982, -4.000000000000000000, 4.898587196589415787E-16 ) ) ;
#80297=ORIENTED_EDGE ( 'NONE', *, *, #61492, .T. ) ;
#80311=EDGE_CURVE ( 'NONE', #85998, #92028, #79309, .T. ) ;
#80317=CARTESIAN_POINT ( 'NONE',  ( 11.08349330513380160, -4.000000000000000888, 4.898587196589416773E-16 ) ) ;
#80333=DIRECTION ( 'NONE',  ( 0.000000000000000000, -1.000000000000000000, 0.000000000000000000 ) ) ;
#80361=AXIS2_PLACEMENT_3D ( 'NONE', #31414, #32469, #65339 ) ;
#80394=CARTESIAN_POINT ( 'NONE',  ( 36.08349330513379982, 4.000000000000002665, 0.000000000000000000 ) ) ;
#80413=DIRECTION ( 'NONE',  ( -1.000000000000000000, -1.224606353822377258E-16, -0.000000000000000000 ) ) ;
#80461=CARTESIAN_POINT ( 'NONE',  ( 18.58349330513380337, 1.593028355512270567E-15, 0.000000000000000000 ) ) ;
#80462=CARTESIAN_POINT ( 'NONE',  ( 36.84999999999999432, 1.533819458162526451E-15, 0.000000000000000000 ) ) ;
#80484=DIRECTION ( 'NONE',  ( 0.000000000000000000, -1.000000000000000000, 0.000000000000000000 ) ) ;
#80498=VERTEX_POINT ( 'NONE', #27906 ) ;
#80529=CONICAL_SURFACE ( 'NONE', #34067, 4.000000000000001776, 0.9599310885968808105 ) ;
#80533=ORIENTED_EDGE ( 'NONE', *, *, #31946, .T. ) ;
#80541=PRODUCT_CONTEXT ( 'NONE', #69346, 'mechanical' ) ;
#80553=AXIS2_PLACEMENT_3D ( 'NONE', #71195, #45870, #104091 ) ;
#80574=CIRCLE ( 'NONE', #37522, 6.500000000000000888 ) ;
#80590=CARTESIAN_POINT ( 'NONE',  ( 26.84999999999999787, 3.309500000000003439, 4.052968581778167743E-16 ) ) ;
#80631=CARTESIAN_POINT ( 'NONE',  ( 0.000000000000000000, 5.629165124598847214, -3.250000000000007550 ) ) ;
#80635=EDGE_CURVE ( 'NONE', #12958, #596, #13775, .T. ) ;
#80639=VERTEX_POINT ( 'NONE', #70966 ) ;
#80648=ORIENTED_EDGE ( 'NONE', *, *, #79256, .F. ) ;
#80657=VECTOR ( 'NONE', #22942, 1000.000000000000114 ) ;
#80662=CIRCLE ( 'NONE', #84145, 3.309500000000001663 ) ;
#80677=DIRECTION ( 'NONE',  ( 0.5735764363510466035, -0.8191520442889914655, 1.003171929053524500E-16 ) ) ;
#80694=EDGE_CURVE ( 'NONE', #18717, #10704, #8710, .T. ) ;
#80697=DIRECTION ( 'NONE',  ( -1.000000000000000000, -0.000000000000000000, -0.000000000000000000 ) ) ;
#80720=DIRECTION ( 'NONE',  ( 0.5735764363510462704, 0.8191520442889915765, 0.000000000000000000 ) ) ;
#80726=DIRECTION ( 'NONE',  ( -1.000000000000000000, -0.000000000000000000, -0.000000000000000000 ) ) ;
#80727=CARTESIAN_POINT ( 'NONE',  ( 41.08349330513380693, 1.593028355512270567E-15, 0.000000000000000000 ) ) ;
#80746=ORIENTED_EDGE ( 'NONE', *, *, #37711, .T. ) ;
#80774=VECTOR ( 'NONE', #84334, 1000.000000000000000 ) ;
#80789=DIRECTION ( 'NONE',  ( 0.000000000000000000, 0.000000000000000000, 1.000000000000000000 ) ) ;
#80806=DIRECTION ( 'NONE',  ( -1.000000000000000000, -1.224606353822377258E-16, -0.000000000000000000 ) ) ;
#80816=FACE_OUTER_BOUND ( 'NONE', #75322, .T. ) ;
#80834=CARTESIAN_POINT ( 'NONE',  ( -2.414679174385195903E-15, -5.469921996229795802, 3.525817189091422055 ) ) ;
#80839=AXIS2_PLACEMENT_3D ( 'NONE', #94974, #3825, #70679 ) ;
#80867=ORIENTED_EDGE ( 'NONE', *, *, #80046, .F. ) ;
#80871=DIRECTION ( 'NONE',  ( -1.000000000000000000, -1.224606353822377258E-16, -0.000000000000000000 ) ) ;
#80879=DIRECTION ( 'NONE',  ( 0.000000000000000000, -1.000000000000000000, 0.000000000000000000 ) ) ;
#80889=VERTEX_POINT ( 'NONE', #59039 ) ;
#80916=AXIS2_PLACEMENT_3D ( 'NONE', #41278, #73633, #89840 ) ;
#80967=CARTESIAN_POINT ( 'NONE',  ( 11.08349330513380160, -4.000000000000000000, 4.898587196589415787E-16 ) ) ;
#80970=CARTESIAN_POINT ( 'NONE',  ( 25.11650669486618881, 4.898587196589411843E-16, -4.000000000000000888 ) ) ;
#80978=EDGE_CURVE ( 'NONE', #10704, #70423, #20793, .T. ) ;
#81021=DIRECTION ( 'NONE',  ( 0.000000000000000000, 0.000000000000000000, 1.000000000000000000 ) ) ;
#81034=DIRECTION ( 'NONE',  ( -1.000000000000000000, -0.000000000000000000, -0.000000000000000000 ) ) ;
#81041=EDGE_CURVE ( 'NONE', #95250, #99083, #96577, .T. ) ;
#81048=VERTEX_POINT ( 'NONE', #75738 ) ;
#81072=CARTESIAN_POINT ( 'NONE',  ( 0.000000000000000000, 0.000000000000000000, 0.000000000000000000 ) ) ;
#81073=SHAPE_DEFINITION_REPRESENTATION ( #27828, #88164 ) ;
#81075=ORIENTED_EDGE ( 'NONE', *, *, #78201, .F. ) ;
#81123=ADVANCED_FACE ( 'NONE', ( #48137 ), #105330, .T. ) ;
#81131=LINE ( 'NONE', #48749, #22327 ) ;
#81132=CARTESIAN_POINT ( 'NONE',  ( 6.326416241096634252, -1.324101276589547238, -6.831531844319973956 ) ) ;
#81148=CARTESIAN_POINT ( 'NONE',  ( 0.000000000000000000, 4.898587196589412829E-16, -4.000000000000000000 ) ) ;
#81169=ORIENTED_EDGE ( 'NONE', *, *, #93001, .T. ) ;
#81176=CARTESIAN_POINT ( 'NONE',  ( 18.58349330513380337, 1.593028355512270567E-15, 0.000000000000000000 ) ) ;
#81239=EDGE_LOOP ( 'NONE', ( #27582, #33204, #19509, #36264, #103732, #16656, #56876 ) ) ;
#81263=CARTESIAN_POINT ( 'NONE',  ( 38.58349330513380693, 4.898587196589405926E-16, -4.000000000000001776 ) ) ;
#81267=CARTESIAN_POINT ( 'NONE',  ( 6.394343112843831278, -3.776352960569627104, 6.540835195019758075 ) ) ;
#81279=B_SPLINE_CURVE_WITH_KNOTS ( 'NONE', 3,
 ( #13778, #62894, #14306, #87168, #22976, #47210, #104387, #14841, #54765, #5698 ),
 .UNSPECIFIED., .F., .F.,
 ( 4, 2, 2, 2, 4 ),
 ( 0.000000000000000000, 0.001993803085173306063, 0.003987606170346612126, 0.005981409255519918623, 0.007975212340693225987 ),
 .UNSPECIFIED. ) ;
#81298=CIRCLE ( 'NONE', #19399, 4.000000000000000888 ) ;
#81322=FACE_OUTER_BOUND ( 'NONE', #37163, .T. ) ;
#81325=CIRCLE ( 'NONE', #40002, 4.000000000000001776 ) ;
#81341=FACE_OUTER_BOUND ( 'NONE', #4438, .T. ) ;
#81343=( BOUNDED_SURFACE ( )  B_SPLINE_SURFACE ( 3, 2, ( 
 ( #21709, #5497, #55086 ),
 ( #88014, #14094, #47000 ),
 ( #66788, #3112, #99674 ),
 ( #2568, #91603, #84030 ),
 ( #44652, #3655, #44108 ),
 ( #92649, #27968, #77536 ) ),
 .UNSPECIFIED., .F., .F., .F. ) 
 B_SPLINE_SURFACE_WITH_KNOTS ( ( 4, 2, 4 ),
 ( 3, 3 ),
 ( 0.03206831234578212675, 0.03607477026923534835, 0.04008122819268857689 ),
 ( 0.000000000000000000, 1.000000000000000000 ),
 .UNSPECIFIED. ) 
 GEOMETRIC_REPRESENTATION_ITEM ( )  RATIONAL_B_SPLINE_SURFACE ( (
 ( 1.000000000000000000, 0.8047780936700352772, 1.000000000000000000),
 ( 1.000000000000000000, 0.8123790890099109596, 1.000000000000000000),
 ( 1.000000000000000000, 0.8190678900508677751, 1.000000000000000000),
 ( 1.000000000000000000, 0.8192345188317070592, 1.000000000000000000),
 ( 1.000000000000000000, 0.8126126219723366351, 1.000000000000000000),
 ( 1.000000000000000000, 0.8047712657247791945, 1.000000000000000000) ) ) 
 REPRESENTATION_ITEM ( '' )  SURFACE ( )  );
#81348=EDGE_LOOP ( 'NONE', ( #57794, #84321, #80746, #24574, #77172 ) ) ;
#81349=DIRECTION ( 'NONE',  ( -1.000000000000000000, -1.224606353822377258E-16, -0.000000000000000000 ) ) ;
#81363=ORIENTED_EDGE ( 'NONE', *, *, #28946, .T. ) ;
#81365=VERTEX_POINT ( 'NONE', #11933 ) ;
#81378=LINE ( 'NONE', #6968, #7194 ) ;
#81412=DIRECTION ( 'NONE',  ( 0.5735764363510462704, 0.8191520442889915765, 0.000000000000000000 ) ) ;
#81436=CONICAL_SURFACE ( 'NONE', #55566, 4.000000000000001776, 0.9599310885968808105 ) ;
#81441=ORIENTED_EDGE ( 'NONE', *, *, #94957, .T. ) ;
#81448=DIRECTION ( 'NONE',  ( 0.000000000000000000, 0.000000000000000000, 1.000000000000000000 ) ) ;
#81484=ORIENTED_EDGE ( 'NONE', *, *, #32522, .F. ) ;
#81487=LINE ( 'NONE', #97158, #80136 ) ;
#81499=ORIENTED_EDGE ( 'NONE', *, *, #8255, .F. ) ;
#81512=AXIS2_PLACEMENT_3D ( 'NONE', #75819, #2988, #10546 ) ;
#81534=DIRECTION ( 'NONE',  ( -1.000000000000000000, -1.224606353822377258E-16, -0.000000000000000000 ) ) ;
#81538=AXIS2_PLACEMENT_3D ( 'NONE', #80107, #6754, #47732 ) ;
#81539=DIRECTION ( 'NONE',  ( -1.000000000000000000, -1.224606353822377258E-16, -0.000000000000000000 ) ) ;
#81541=EDGE_LOOP ( 'NONE', ( #13771, #37458, #95978, #69303, #68484 ) ) ;
#81550=VECTOR ( 'NONE', #46450, 1000.000000000000114 ) ;
#81585=VECTOR ( 'NONE', #52189, 1000.000000000000000 ) ;
#81597=ORIENTED_EDGE ( 'NONE', *, *, #5476, .T. ) ;
#81602=DIRECTION ( 'NONE',  ( -1.000000000000000000, -1.224606353822377258E-16, -0.000000000000000000 ) ) ;
#81613=ORIENTED_EDGE ( 'NONE', *, *, #68744, .T. ) ;
#81614=DIRECTION ( 'NONE',  ( 0.000000000000000000, -1.000000000000000000, 0.000000000000000000 ) ) ;
#81615=EDGE_CURVE ( 'NONE', #8430, #79845, #55282, .T. ) ;
#81617=AXIS2_PLACEMENT_3D ( 'NONE', #20091, #19557, #52393 ) ;
#81624=ADVANCED_FACE ( 'NONE', ( #50647 ), #56968, .T. ) ;
#81637=DIRECTION ( 'NONE',  ( 0.000000000000000000, -1.000000000000000000, 0.000000000000000000 ) ) ;
#81694=ORIENTED_EDGE ( 'NONE', *, *, #21354, .F. ) ;
#81697=CONICAL_SURFACE ( 'NONE', #105812, 3.309500000000001663, 0.9599310885968770357 ) ;
#81702=ORIENTED_EDGE ( 'NONE', *, *, #80311, .T. ) ;
#81711=EDGE_CURVE ( 'NONE', #20373, #21459, #32916, .T. ) ;
#81728=AXIS2_PLACEMENT_3D ( 'NONE', #28984, #61850, #52657 ) ;
#81733=CARTESIAN_POINT ( 'NONE',  ( 26.84999999999999787, -3.309499999999999886, 0.000000000000000000 ) ) ;
#81735=VECTOR ( 'NONE', #90177, 1000.000000000000000 ) ;
#81737=ORIENTED_EDGE ( 'NONE', *, *, #93339, .F. ) ;
#81745=ORIENTED_EDGE ( 'NONE', *, *, #26221, .F. ) ;
#81751=EDGE_CURVE ( 'NONE', #57113, #2149, #60487, .T. ) ;
#81792=LINE ( 'NONE', #73713, #44771 ) ;
#81802=ORIENTED_EDGE ( 'NONE', *, *, #69934, .T. ) ;
#81822=CIRCLE ( 'NONE', #35374, 4.000000000000000888 ) ;
#81845=VERTEX_POINT ( 'NONE', #53343 ) ;
#81851=EDGE_CURVE ( 'NONE', #60121, #73382, #51732, .T. ) ;
#81856=CARTESIAN_POINT ( 'NONE',  ( 17.33349330513380337, -7.703719777548943412E-31, 4.000000000000001776 ) ) ;
#81941=ORIENTED_EDGE ( 'NONE', *, *, #61958, .F. ) ;
#81949=CARTESIAN_POINT ( 'NONE',  ( 6.326445470157510798, 6.578717624163890498, -2.268395195563515099 ) ) ;
#81951=AXIS2_PLACEMENT_3D ( 'NONE', #85647, #101292, #69456 ) ;
#81954=VERTEX_POINT ( 'NONE', #56502 ) ;
#81969=VECTOR ( 'NONE', #102635, 1000.000000000000000 ) ;
#81977=CARTESIAN_POINT ( 'NONE',  ( 6.683837171061802529, -3.955946848495957457, 6.851900933636990487 ) ) ;
#81996=AXIS2_PLACEMENT_3D ( 'NONE', #77956, #52600, #37001 ) ;
#81997=EDGE_LOOP ( 'NONE', ( #96601, #68194, #63006, #93513, #102474, #104186 ) ) ;
#82023=ORIENTED_EDGE ( 'NONE', *, *, #7059, .F. ) ;
#82044=CIRCLE ( 'NONE', #94084, 4.000000000000000888 ) ;
#82046=VERTEX_POINT ( 'NONE', #54365 ) ;
#82049=AXIS2_PLACEMENT_3D ( 'NONE', #84715, #43195, #1099 ) ;
#82066=ADVANCED_FACE ( 'NONE', ( #13392 ), #26168, .T. ) ;
#82122=CARTESIAN_POINT ( 'NONE',  ( 11.84999999999999787, -3.309499999999999886, 0.000000000000000000 ) ) ;
#82123=ADVANCED_FACE ( 'NONE', ( #364 ), #101873, .T. ) ;
#82129=VECTOR ( 'NONE', #39326, 1000.000000000000000 ) ;
#82139=VECTOR ( 'NONE', #75118, 1000.000000000000000 ) ;
#82183=CARTESIAN_POINT ( 'NONE',  ( 0.5805565836007654523, 7.505553499465140277, 2.211437577243512467E-16 ) ) ;
#82200=ORIENTED_EDGE ( 'NONE', *, *, #19424, .T. ) ;
#82202=VERTEX_POINT ( 'NONE', #9018 ) ;
#82206=VECTOR ( 'NONE', #29412, 1000.000000000000000 ) ;
#82254=EDGE_CURVE ( 'NONE', #74863, #100726, #76000, .T. ) ;
#82260=DIRECTION ( 'NONE',  ( -0.5735764363510494901, -0.8191520442889894671, 0.000000000000000000 ) ) ;
#82262=AXIS2_PLACEMENT_3D ( 'NONE', #4677, #6236, #71509 ) ;
#82266=ORIENTED_EDGE ( 'NONE', *, *, #71268, .T. ) ;
#82278=ADVANCED_FACE ( 'NONE', ( #51610 ), #101763, .T. ) ;
#82288=EDGE_LOOP ( 'NONE', ( #41192, #51040, #58362, #59897, #17222 ) ) ;
#82297=ORIENTED_EDGE ( 'NONE', *, *, #60113, .T. ) ;
#82305=DIRECTION ( 'NONE',  ( -1.000000000000000000, -1.224606353822377258E-16, -0.000000000000000000 ) ) ;
#82309=EDGE_LOOP ( 'NONE', ( #2049, #62077, #6459, #101856, #51554, #22383 ) ) ;
#82329=ORIENTED_EDGE ( 'NONE', *, *, #59656, .T. ) ;
#82337=AXIS2_PLACEMENT_3D ( 'NONE', #19801, #94728, #93653 ) ;
#82345=DIRECTION ( 'NONE',  ( 0.000000000000000000, -1.000000000000000000, 0.000000000000000000 ) ) ;
#82351=ORIENTED_EDGE ( 'NONE', *, *, #24161, .F. ) ;
#82376=CYLINDRICAL_SURFACE ( 'NONE', #49307, 4.000000000000000000 ) ;
#82384=VECTOR ( 'NONE', #925, 1000.000000000000000 ) ;
#82391=EDGE_CURVE ( 'NONE', #99054, #74596, #8925, .T. ) ;
#82397=CIRCLE ( 'NONE', #4875, 4.000000000000001776 ) ;
#82429=CYLINDRICAL_SURFACE ( 'NONE', #78595, 4.000000000000000000 ) ;
#82432=VERTEX_POINT ( 'NONE', #40078 ) ;
#82453=DIRECTION ( 'NONE',  ( -1.000000000000000000, -1.224606353822377258E-16, -0.000000000000000000 ) ) ;
#82462=DIRECTION ( 'NONE',  ( 0.000000000000000000, -1.000000000000000000, 0.000000000000000000 ) ) ;
#82469=CARTESIAN_POINT ( 'NONE',  ( 23.09999999999999432, 1.533819458162526451E-15, 0.000000000000000000 ) ) ;
#82470=ORIENTED_EDGE ( 'NONE', *, *, #3949, .F. ) ;
#82473=CIRCLE ( 'NONE', #41136, 4.000000000000001776 ) ;
#82479=CARTESIAN_POINT ( 'NONE',  ( 37.33349330513379982, 4.000000000000002665, 0.000000000000000000 ) ) ;
#82480=CARTESIAN_POINT ( 'NONE',  ( 29.34999999999999787, -3.309499999999999886, 4.475777889183790779E-16 ) ) ;
#82504=CARTESIAN_POINT ( 'NONE',  ( 6.683837171061806082, 7.911893696991934455, 7.436622852660996417E-19 ) ) ;
#82530=DIRECTION ( 'NONE',  ( -1.000000000000000000, -1.224606353822377258E-16, -0.000000000000000000 ) ) ;
#82531=DIRECTION ( 'NONE',  ( -1.000000000000000000, -1.224606353822377258E-16, -0.000000000000000000 ) ) ;
#82541=CIRCLE ( 'NONE', #22296, 3.309500000000001663 ) ;
#82555=ORIENTED_EDGE ( 'NONE', *, *, #54946, .F. ) ;
#82566=CARTESIAN_POINT ( 'NONE',  ( 6.463178677061750754, 2.643201791673480905, 6.839998497243177766 ) ) ;
#82626=CARTESIAN_POINT ( 'NONE',  ( 47.33349330513379982, 4.000000000000002665, 0.000000000000000000 ) ) ;
#82636=CARTESIAN_POINT ( 'NONE',  ( 39.34999999999999432, -3.309499999999999886, 0.000000000000000000 ) ) ;
#82645=CYLINDRICAL_SURFACE ( 'NONE', #28756, 4.000000000000000000 ) ;
#82653=AXIS2_PLACEMENT_3D ( 'NONE', #19519, #76099, #1122 ) ;
#82665=EDGE_CURVE ( 'NONE', #23893, #101293, #2798, .T. ) ;
#82674=EDGE_CURVE ( 'NONE', #57765, #26186, #27942, .T. ) ;
#82679=LINE ( 'NONE', #99372, #69814 ) ;
#82692=CARTESIAN_POINT ( 'NONE',  ( 27.61650669486618881, -3.999999999999998224, 0.000000000000000000 ) ) ;
#82704=ORIENTED_EDGE ( 'NONE', *, *, #3949, .T. ) ;
#82729=FACE_OUTER_BOUND ( 'NONE', #85254, .T. ) ;
#82734=CARTESIAN_POINT ( 'NONE',  ( 13.86650669486618881, 4.898587196589411843E-16, -4.000000000000000888 ) ) ;
#82736=LINE ( 'NONE', #8838, #80657 ) ;
#82741=VECTOR ( 'NONE', #60425, 1000.000000000000000 ) ;
#82775=ORIENTED_EDGE ( 'NONE', *, *, #62908, .T. ) ;
#82802=CIRCLE ( 'NONE', #54984, 3.309500000000001663 ) ;
#82807=ORIENTED_EDGE ( 'NONE', *, *, #49034, .F. ) ;
#82813=ORIENTED_EDGE ( 'NONE', *, *, #10434, .F. ) ;
#82816=CONICAL_SURFACE ( 'NONE', #58733, 4.000000000000001776, 0.9599310885968808105 ) ;
#82819=EDGE_CURVE ( 'NONE', #30981, #20310, #85324, .T. ) ;
#82836=CIRCLE ( 'NONE', #36395, 4.000000000000000888 ) ;
#82840=DIRECTION ( 'NONE',  ( -1.000000000000000000, -1.224606353822377258E-16, -0.000000000000000000 ) ) ;
#82851=CARTESIAN_POINT ( 'NONE',  ( 25.59999999999999787, 1.533819458162526451E-15, 0.000000000000000000 ) ) ;
#82858=AXIS2_PLACEMENT_3D ( 'NONE', #5570, #23376, #89152 ) ;
#82878=DIRECTION ( 'NONE',  ( 0.000000000000000000, 0.000000000000000000, 1.000000000000000000 ) ) ;
#82896=VERTEX_POINT ( 'NONE', #105220 ) ;
#82901=AXIS2_PLACEMENT_3D ( 'NONE', #46400, #30773, #14532 ) ;
#82910=FACE_OUTER_BOUND ( 'NONE', #66695, .T. ) ;
#82924=DIRECTION ( 'NONE',  ( 0.000000000000000000, -1.000000000000000000, 0.000000000000000000 ) ) ;
#82925=CARTESIAN_POINT ( 'NONE',  ( 41.08349330513380693, 1.593028355512270567E-15, 0.000000000000000000 ) ) ;
#82934=DIRECTION ( 'NONE',  ( 0.000000000000000000, -1.000000000000000000, 0.000000000000000000 ) ) ;
#82952=CARTESIAN_POINT ( 'NONE',  ( 21.84999999999999787, 1.533819458162526451E-15, 0.000000000000000000 ) ) ;
#82956=ORIENTED_EDGE ( 'NONE', *, *, #17362, .T. ) ;
#82957=CARTESIAN_POINT ( 'NONE',  ( 29.83349330513380337, 1.593028355512270567E-15, 0.000000000000000000 ) ) ;
#82981=VERTEX_POINT ( 'NONE', #31367 ) ;
#82983=CARTESIAN_POINT ( 'NONE',  ( 14.83349330513380337, 4.000000000000003553, 0.000000000000000000 ) ) ;
#83024=AXIS2_PLACEMENT_3D ( 'NONE', #54726, #38076, #55260 ) ;
#83044=CIRCLE ( 'NONE', #67578, 4.000000000000001776 ) ;
#83054=CIRCLE ( 'NONE', #58727, 4.000000000000000888 ) ;
#83073=ADVANCED_FACE ( 'NONE', ( #52276 ), #95188, .T. ) ;
#83090=ORIENTED_EDGE ( 'NONE', *, *, #79500, .F. ) ;
#83104=ORIENTED_EDGE ( 'NONE', *, *, #49995, .T. ) ;
#83172=DIRECTION ( 'NONE',  ( 0.000000000000000000, 0.000000000000000000, 1.000000000000000000 ) ) ;
#83179=CARTESIAN_POINT ( 'NONE',  ( 32.33349330513379982, 1.593028355512270567E-15, 0.000000000000000000 ) ) ;
#83186=DIRECTION ( 'NONE',  ( -1.000000000000000000, -0.000000000000000000, -0.000000000000000000 ) ) ;
#83212=ORIENTED_EDGE ( 'NONE', *, *, #75812, .T. ) ;
#83253=VERTEX_POINT ( 'NONE', #98577 ) ;
#83257=DIRECTION ( 'NONE',  ( 0.000000000000000000, 1.000000000000000000, 0.000000000000000000 ) ) ;
#83277=DIRECTION ( 'NONE',  ( 0.000000000000000000, -1.000000000000000000, 0.000000000000000000 ) ) ;
#83296=CARTESIAN_POINT ( 'NONE',  ( 6.169949891408691656, -6.308465495018314328, -2.073417244831073258 ) ) ;
#83305=ORIENTED_EDGE ( 'NONE', *, *, #56204, .F. ) ;
#83322=DIRECTION ( 'NONE',  ( 0.000000000000000000, -1.000000000000000000, 0.000000000000000000 ) ) ;
#83324=CARTESIAN_POINT ( 'NONE',  ( 0.000000000000000000, 5.629165124598847214, -3.250000000000007550 ) ) ;
#83331=VERTEX_POINT ( 'NONE', #58120 ) ;
#83333=DIRECTION ( 'NONE',  ( 0.000000000000000000, -1.000000000000000000, 0.000000000000000000 ) ) ;
#83339=VECTOR ( 'NONE', #52935, 1000.000000000000000 ) ;
#83353=ORIENTED_EDGE ( 'NONE', *, *, #58055, .F. ) ;
#83369=EDGE_CURVE ( 'NONE', #54043, #70963, #7388, .T. ) ;
#83406=DIRECTION ( 'NONE',  ( -0.5735764363510497121, 0.8191520442889892450, 1.003171929053521665E-16 ) ) ;
#83432=ORIENTED_EDGE ( 'NONE', *, *, #94216, .T. ) ;
#83435=CARTESIAN_POINT ( 'NONE',  ( 6.169949891408687215, 4.949864754179436943, -4.426582755167822292 ) ) ;
#83463=CARTESIAN_POINT ( 'NONE',  ( 0.05533025579362068486, 4.993776679985853839, 4.350525068611871049 ) ) ;
#83486=EDGE_CURVE ( 'NONE', #61806, #99054, #74530, .T. ) ;
#83488=ORIENTED_EDGE ( 'NONE', *, *, #34418, .F. ) ;
#83489=DIRECTION ( 'NONE',  ( 0.000000000000000000, -1.000000000000000000, 0.000000000000000000 ) ) ;
#83514=DIRECTION ( 'NONE',  ( -1.000000000000000000, -1.224606353822377258E-16, -0.000000000000000000 ) ) ;
#83530=DIRECTION ( 'NONE',  ( 0.000000000000000000, -1.000000000000000000, 0.000000000000000000 ) ) ;
#83535=DIRECTION ( 'NONE',  ( 0.5735764363510462704, 0.8191520442889915765, 0.000000000000000000 ) ) ;
#83537=EDGE_CURVE ( 'NONE', #78767, #79890, #71075, .T. ) ;
#83540=ORIENTED_EDGE ( 'NONE', *, *, #63991, .T. ) ;
#83544=EDGE_CURVE ( 'NONE', #80206, #6993, #102310, .T. ) ;
#83556=EDGE_CURVE ( 'NONE', #101661, #49207, #52130, .T. ) ;
#83558=AXIS2_PLACEMENT_3D ( 'NONE', #67958, #91709, #99238 ) ;
#83565=CARTESIAN_POINT ( 'NONE',  ( 18.86650669486618881, 1.474610560812782335E-15, 0.000000000000000000 ) ) ;
#83569=ORIENTED_EDGE ( 'NONE', *, *, #77768, .T. ) ;
#83575=CARTESIAN_POINT ( 'NONE',  ( 10.59999999999999609, -3.309499999999999886, 4.475777889183790779E-16 ) ) ;
#83586=ADVANCED_FACE ( 'NONE', ( #27943 ), #69950, .F. ) ;
#83624=ORIENTED_EDGE ( 'NONE', *, *, #35490, .F. ) ;
#83632=CARTESIAN_POINT ( 'NONE',  ( 12.61650669486618881, 4.898587196589411843E-16, -4.000000000000000888 ) ) ;
#83645=EDGE_LOOP ( 'NONE', ( #45081, #71886, #99352, #57498, #98318 ) ) ;
#83648=LINE ( 'NONE', #9760, #45039 ) ;
#83674=DIRECTION ( 'NONE',  ( 0.000000000000000000, -1.000000000000000000, 0.000000000000000000 ) ) ;
#83682=DIRECTION ( 'NONE',  ( -1.000000000000000000, -1.224606353822377258E-16, -0.000000000000000000 ) ) ;
#83688=ORIENTED_EDGE ( 'NONE', *, *, #39815, .T. ) ;
#83695=LINE ( 'NONE', #76138, #83339 ) ;
#83724=CARTESIAN_POINT ( 'NONE',  ( 19.83349330513379982, 1.593028355512270567E-15, 0.000000000000000000 ) ) ;
#83743=AXIS2_PLACEMENT_3D ( 'NONE', #45640, #78516, #4649 ) ;
#83745=AXIS2_PLACEMENT_3D ( 'NONE', #50331, #1227, #57355 ) ;
#83755=DIRECTION ( 'NONE',  ( 0.000000000000000000, -1.000000000000000000, 0.000000000000000000 ) ) ;
#83823=CARTESIAN_POINT ( 'NONE',  ( 6.289692432696806890, -5.239086202715462548, -4.583616368338172542 ) ) ;
#83828=AXIS2_PLACEMENT_3D ( 'NONE', #91990, #2442, #75260 ) ;
#83833=CARTESIAN_POINT ( 'NONE',  ( 30.59999999999999787, 3.309500000000003439, 0.000000000000000000 ) ) ;
#83834=ORIENTED_EDGE ( 'NONE', *, *, #9827, .T. ) ;
#83837=AXIS2_PLACEMENT_3D ( 'NONE', #70716, #86391, #4921 ) ;
#83840=LINE ( 'NONE', #101632, #78645 ) ;
#83862=FACE_OUTER_BOUND ( 'NONE', #101146, .T. ) ;
#83867=FACE_OUTER_BOUND ( 'NONE', #94852, .T. ) ;
#83888=DIRECTION ( 'NONE',  ( 0.000000000000000000, 0.000000000000000000, 1.000000000000000000 ) ) ;
#83896=DIRECTION ( 'NONE',  ( -1.000000000000000000, -0.000000000000000000, 0.000000000000000000 ) ) ;
#83897=VECTOR ( 'NONE', #36060, 1000.000000000000000 ) ;
#83907=AXIS2_PLACEMENT_3D ( 'NONE', #105203, #24315, #46438 ) ;
#83914=ORIENTED_EDGE ( 'NONE', *, *, #76182, .F. ) ;
#83917=AXIS2_PLACEMENT_3D ( 'NONE', #41048, #90662, #73931 ) ;
#83998=ORIENTED_EDGE ( 'NONE', *, *, #79278, .T. ) ;
#84028=DIRECTION ( 'NONE',  ( -1.000000000000000000, -0.000000000000000000, -0.000000000000000000 ) ) ;
#84030=CARTESIAN_POINT ( 'NONE',  ( 6.287679341995262128, -1.331405739688502399, -6.828854810278215837 ) ) ;
#84052=CARTESIAN_POINT ( 'NONE',  ( 6.683837171061806082, 7.911893696991934455, 7.436622852660996417E-19 ) ) ;
#84066=FACE_OUTER_BOUND ( 'NONE', #81997, .T. ) ;
#84074=DIRECTION ( 'NONE',  ( -1.000000000000000000, -1.224606353822377258E-16, -0.000000000000000000 ) ) ;
#84079=CYLINDRICAL_SURFACE ( 'NONE', #100076, 4.000000000000000000 ) ;
#84080=AXIS2_PLACEMENT_3D ( 'NONE', #77799, #28758, #49381 ) ;
#84103=EDGE_LOOP ( 'NONE', ( #62886, #92984, #83104, #69006, #28484 ) ) ;
#84113=CARTESIAN_POINT ( 'NONE',  ( 0.000000000000000000, 4.898587196589412829E-16, -4.000000000000000000 ) ) ;
#84137=CARTESIAN_POINT ( 'NONE',  ( 0.000000000000000000, 0.000000000000000000, 4.000000000000000000 ) ) ;
#84144=CYLINDRICAL_SURFACE ( 'NONE', #83558, 4.000000000000000000 ) ;
#84145=AXIS2_PLACEMENT_3D ( 'NONE', #99345, #91299, #7690 ) ;
#84146=LINE ( 'NONE', #91710, #5303 ) ;
#84164=AXIS2_PLACEMENT_3D ( 'NONE', #104843, #78963, #14747 ) ;
#84168=CARTESIAN_POINT ( 'NONE',  ( 6.289692432696784685, 1.244805614057421469E-13, 6.828989928337167115 ) ) ;
#84182=DIRECTION ( 'NONE',  ( 1.000000000000000000, 0.000000000000000000, -0.000000000000000000 ) ) ;
#84199=VECTOR ( 'NONE', #73514, 1000.000000000000000 ) ;
#84268=DIRECTION ( 'NONE',  ( -1.000000000000000000, -0.000000000000000000, -0.000000000000000000 ) ) ;
#84280=EDGE_CURVE ( 'NONE', #80639, #17581, #15687, .T. ) ;
#84293=ADVANCED_FACE ( 'NONE', ( #34588 ), #17850, .T. ) ;
#84300=ORIENTED_EDGE ( 'NONE', *, *, #41675, .T. ) ;
#84306=DIRECTION ( 'NONE',  ( 1.000000000000000000, 1.224606353822377258E-16, 0.000000000000000000 ) ) ;
#84321=ORIENTED_EDGE ( 'NONE', *, *, #86794, .T. ) ;
#84328=ORIENTED_EDGE ( 'NONE', *, *, #59971, .F. ) ;
#84334=DIRECTION ( 'NONE',  ( -0.5735764363510497121, 0.8191520442889892450, 1.003171929053521665E-16 ) ) ;
#84338=EDGE_CURVE ( 'NONE', #73270, #87270, #18388, .T. ) ;
#84357=CARTESIAN_POINT ( 'NONE',  ( 43.10000000000000142, 3.309500000000003439, 0.000000000000000000 ) ) ;
#84388=ORIENTED_EDGE ( 'NONE', *, *, #2403, .T. ) ;
#84418=AXIS2_PLACEMENT_3D ( 'NONE', #59479, #92344, #100976 ) ;
#84422=CARTESIAN_POINT ( 'NONE',  ( 42.61650669486618881, 1.474610560812782335E-15, 0.000000000000000000 ) ) ;
#84431=AXIS2_PLACEMENT_3D ( 'NONE', #29430, #69853, #71966 ) ;
#84441=ORIENTED_EDGE ( 'NONE', *, *, #8892, .F. ) ;
#84498=VERTEX_POINT ( 'NONE', #101418 ) ;
#84503=VERTEX_POINT ( 'NONE', #11856 ) ;
#84515=CARTESIAN_POINT ( 'NONE',  ( 35.59999999999999432, 3.309500000000003439, 0.000000000000000000 ) ) ;
#84517=EDGE_CURVE ( 'NONE', #81365, #9776, #14378, .T. ) ;
#84571=CARTESIAN_POINT ( 'NONE',  ( 9.833493305133801599, 1.593028355512270567E-15, 0.000000000000000000 ) ) ;
#84578=CIRCLE ( 'NONE', #38117, 4.000000000000001776 ) ;
#84579=CARTESIAN_POINT ( 'NONE',  ( 24.83349330513380337, 4.000000000000002665, 0.000000000000000000 ) ) ;
#84580=ORIENTED_EDGE ( 'NONE', *, *, #36564, .F. ) ;
#84591=ORIENTED_EDGE ( 'NONE', *, *, #61037, .T. ) ;
#84597=LINE ( 'NONE', #3139, #49459 ) ;
#84636=AXIS2_PLACEMENT_3D ( 'NONE', #105083, #40334, #39821 ) ;
#84653=CIRCLE ( 'NONE', #41597, 4.000000000000000888 ) ;
#84659=ORIENTED_EDGE ( 'NONE', *, *, #86522, .F. ) ;
#84673=CIRCLE ( 'NONE', #31265, 4.000000000000000888 ) ;
#84692=DIRECTION ( 'NONE',  ( 0.000000000000000000, -1.000000000000000000, 0.000000000000000000 ) ) ;
#84713=LINE ( 'NONE', #41062, #75407 ) ;
#84715=CARTESIAN_POINT ( 'NONE',  ( 44.35000000000000142, 1.533819458162526451E-15, 0.000000000000000000 ) ) ;
#84757=DIRECTION ( 'NONE',  ( -1.000000000000000000, -1.224606353822377258E-16, -0.000000000000000000 ) ) ;
#84764=CARTESIAN_POINT ( 'NONE',  ( 5.819846122303831137, -6.321060697774819381, 2.051601713727242426 ) ) ;
#84786=ORIENTED_EDGE ( 'NONE', *, *, #40352, .F. ) ;
#84797=VERTEX_POINT ( 'NONE', #58711 ) ;
#84830=CARTESIAN_POINT ( 'NONE',  ( 0.000000000000000000, 0.000000000000000000, 0.000000000000000000 ) ) ;
#84834=EDGE_CURVE ( 'NONE', #74736, #16354, #98611, .T. ) ;
#84835=DIRECTION ( 'NONE',  ( -1.000000000000000000, -1.224606353822377258E-16, -0.000000000000000000 ) ) ;
#84837=DIRECTION ( 'NONE',  ( 0.000000000000000000, -1.000000000000000000, 0.000000000000000000 ) ) ;
#84859=AXIS2_PLACEMENT_3D ( 'NONE', #906, #92617, #82934 ) ;
#84920=EDGE_CURVE ( 'NONE', #74067, #81365, #77004, .T. ) ;
#84930=CARTESIAN_POINT ( 'NONE',  ( 41.36650669486618881, -3.999999999999998224, 0.000000000000000000 ) ) ;
#84951=ADVANCED_FACE ( 'NONE', ( #101811 ), #27975, .T. ) ;
#84971=DIRECTION ( 'NONE',  ( -0.5735764363510494901, -0.8191520442889894671, 0.000000000000000000 ) ) ;
#85064=CARTESIAN_POINT ( 'NONE',  ( 11.84999999999999787, 3.309500000000003439, 0.000000000000000000 ) ) ;
#85070=CARTESIAN_POINT ( 'NONE',  ( 30.59999999999999787, 1.533819458162526451E-15, 0.000000000000000000 ) ) ;
#85082=LINE ( 'NONE', #19864, #60156 ) ;
#85093=ORIENTED_EDGE ( 'NONE', *, *, #48383, .F. ) ;
#85107=AXIS2_PLACEMENT_3D ( 'NONE', #101777, #36030, #68363 ) ;
#85127=EDGE_LOOP ( 'NONE', ( #54206, #2167, #30059, #54329 ) ) ;
#85143=EDGE_CURVE ( 'NONE', #87161, #32332, #67737, .T. ) ;
#85161=CIRCLE ( 'NONE', #38669, 4.000000000000000888 ) ;
#85169=ORIENTED_EDGE ( 'NONE', *, *, #20511, .T. ) ;
#85172=DIRECTION ( 'NONE',  ( 0.000000000000000000, -1.000000000000000000, 0.000000000000000000 ) ) ;
#85177=DIRECTION ( 'NONE',  ( -1.000000000000000000, -0.000000000000000000, -0.000000000000000000 ) ) ;
#85185=EDGE_LOOP ( 'NONE', ( #56771, #52122, #33427, #98754, #43209 ) ) ;
#85216=DIRECTION ( 'NONE',  ( 0.000000000000000000, -1.000000000000000000, 0.000000000000000000 ) ) ;
#85249=FACE_OUTER_BOUND ( 'NONE', #60146, .T. ) ;
#85254=EDGE_LOOP ( 'NONE', ( #1294, #27351, #61603, #18072, #1495 ) ) ;
#85256=EDGE_LOOP ( 'NONE', ( #52721, #8761, #17186, #17886, #6822 ) ) ;
#85297=EDGE_CURVE ( 'NONE', #32332, #25223, #31750, .T. ) ;
#85324=LINE ( 'NONE', #86930, #38305 ) ;
#85329=SURFACE_SIDE_STYLE ('',( #36292 ) ) ;
#85338=CARTESIAN_POINT ( 'NONE',  ( 30.59999999999999787, 3.309500000000003439, 4.052968581778167743E-16 ) ) ;
#85357=CARTESIAN_POINT ( 'NONE',  ( 16.36650669486618881, 1.474610560812782335E-15, 0.000000000000000000 ) ) ;
#85360=EDGE_CURVE ( 'NONE', #9600, #40876, #55798, .T. ) ;
#85389=ORIENTED_EDGE ( 'NONE', *, *, #58533, .T. ) ;
#85472=VECTOR ( 'NONE', #71422, 1000.000000000000000 ) ;
#85518=DIRECTION ( 'NONE',  ( -1.000000000000000000, -1.224606353822377258E-16, -0.000000000000000000 ) ) ;
#85576=ORIENTED_EDGE ( 'NONE', *, *, #95625, .F. ) ;
#85582=CYLINDRICAL_SURFACE ( 'NONE', #40721, 4.000000000000000000 ) ;
#85584=EDGE_CURVE ( 'NONE', #10582, #105650, #57256, .T. ) ;
#85585=EDGE_LOOP ( 'NONE', ( #74822, #102933, #14370, #92462, #18134 ) ) ;
#85613=DIRECTION ( 'NONE',  ( 0.000000000000000000, -0.8660254037844381525, -0.5000000000000008882 ) ) ;
#85632=CIRCLE ( 'NONE', #71819, 4.000000000000000888 ) ;
#85647=CARTESIAN_POINT ( 'NONE',  ( 19.83349330513379982, 1.593028355512270567E-15, 0.000000000000000000 ) ) ;
#85649=DIRECTION ( 'NONE',  ( 0.000000000000000000, 0.000000000000000000, 1.000000000000000000 ) ) ;
#85662=ORIENTED_EDGE ( 'NONE', *, *, #56204, .T. ) ;
#85663=CARTESIAN_POINT ( 'NONE',  ( 0.4053525175235886957, 3.145852061455926219, -6.500000000000000000 ) ) ;
#85680=CARTESIAN_POINT ( 'NONE',  ( 6.326195795702134639, 1.326139502404688697, 6.831522767507085980 ) ) ;
#85683=AXIS2_PLACEMENT_3D ( 'NONE', #82925, #898, #16597 ) ;
#85703=ORIENTED_EDGE ( 'NONE', *, *, #39167, .T. ) ;
#85719=ORIENTED_EDGE ( 'NONE', *, *, #14219, .F. ) ;
#85734=DIRECTION ( 'NONE',  ( 0.000000000000000000, -1.000000000000000000, 0.000000000000000000 ) ) ;
#85743=DIRECTION ( 'NONE',  ( -1.000000000000000000, -1.224606353822377258E-16, -0.000000000000000000 ) ) ;
#85750=CARTESIAN_POINT ( 'NONE',  ( 20.11650669486618881, 4.000000000000003553, 4.898587196589414801E-16 ) ) ;
#85760=ORIENTED_EDGE ( 'NONE', *, *, #26631, .T. ) ;
#85779=CARTESIAN_POINT ( 'NONE',  ( 0.000000000000000000, 0.000000000000000000, 4.000000000000000000 ) ) ;
#85783=DIRECTION ( 'NONE',  ( 0.000000000000000000, -1.000000000000000000, 0.000000000000000000 ) ) ;
#85827=CARTESIAN_POINT ( 'NONE',  ( 37.61650669486618881, -3.999999999999998224, 0.000000000000000000 ) ) ;
#85888=CYLINDRICAL_SURFACE ( 'NONE', #8474, 4.000000000000000000 ) ;
#85893=CARTESIAN_POINT ( 'NONE',  ( 43.58349330513380693, 1.593028355512270567E-15, 0.000000000000000000 ) ) ;
#85901=VECTOR ( 'NONE', #48322, 1000.000000000000000 ) ;
#85963=DIRECTION ( 'NONE',  ( 0.000000000000000000, -1.000000000000000000, 0.000000000000000000 ) ) ;
#85984=VERTEX_POINT ( 'NONE', #96530 ) ;
#85997=LINE ( 'NONE', #14179, #71938 ) ;
#85998=VERTEX_POINT ( 'NONE', #6965 ) ;
#86006=ORIENTED_EDGE ( 'NONE', *, *, #21015, .F. ) ;
#86033=AXIS2_PLACEMENT_3D ( 'NONE', #62042, #5881, #53907 ) ;
#86050=CYLINDRICAL_SURFACE ( 'NONE', #62922, 4.000000000000000000 ) ;
#86056=CARTESIAN_POINT ( 'NONE',  ( 10.11650669486618881, -3.999999999999998224, 0.000000000000000000 ) ) ;
#86101=CARTESIAN_POINT ( 'NONE',  ( 6.445370176741822554, 4.584736124523701939, 5.738941594274445279 ) ) ;
#86122=DIRECTION ( 'NONE',  ( -1.000000000000000000, -1.224606353822377258E-16, -0.000000000000000000 ) ) ;
#86132=CARTESIAN_POINT ( 'NONE',  ( 6.326445470157513462, -5.253846677262528075, -4.563138989068575846 ) ) ;
#86143=AXIS2_PLACEMENT_3D ( 'NONE', #69807, #52018, #102703 ) ;
#86152=AXIS2_PLACEMENT_3D ( 'NONE', #42917, #83896, #27845 ) ;
#86182=AXIS2_PLACEMENT_3D ( 'NONE', #4741, #102367, #95346 ) ;
#86184=ORIENTED_EDGE ( 'NONE', *, *, #11571, .F. ) ;
#86194=DIRECTION ( 'NONE',  ( 0.000000000000000000, -1.000000000000000000, 0.000000000000000000 ) ) ;
#86202=DIRECTION ( 'NONE',  ( -1.000000000000000000, -1.224606353822377258E-16, -0.000000000000000000 ) ) ;
#86203=ORIENTED_EDGE ( 'NONE', *, *, #36770, .T. ) ;
#86204=ADVANCED_FACE ( 'NONE', ( #65232 ), #72260, .T. ) ;
#86244=EDGE_LOOP ( 'NONE', ( #6499, #75075, #15791 ) ) ;
#86255=EDGE_CURVE ( 'NONE', #47728, #78767, #30200, .T. ) ;
#86259=VERTEX_POINT ( 'NONE', #82479 ) ;
#86266=EDGE_CURVE ( 'NONE', #35660, #8756, #26759, .T. ) ;
#86273=ORIENTED_EDGE ( 'NONE', *, *, #19513, .T. ) ;
#86289=CIRCLE ( 'NONE', #10495, 4.000000000000001776 ) ;
#86294=LINE ( 'NONE', #68502, #82741 ) ;
#86301=DIRECTION ( 'NONE',  ( 0.000000000000000000, -1.000000000000000000, 0.000000000000000000 ) ) ;
#86315=LINE ( 'NONE', #85779, #106207 ) ;
#86344=EDGE_LOOP ( 'NONE', ( #26006, #106173, #13530, #37445, #16854, #18966 ) ) ;
#86349=EDGE_CURVE ( 'NONE', #19064, #77149, #7765, .T. ) ;
#86368=DIRECTION ( 'NONE',  ( 1.000000000000000000, 1.224606353822377258E-16, 0.000000000000000000 ) ) ;
#86391=DIRECTION ( 'NONE',  ( 1.000000000000000000, 0.000000000000000000, -0.000000000000000000 ) ) ;
#86410=ADVANCED_FACE ( 'NONE', ( #64589 ), #50796, .T. ) ;
#86417=( LENGTH_UNIT ( ) NAMED_UNIT ( * ) SI_UNIT ( .MILLI., .METRE. ) );
#86419=DIRECTION ( 'NONE',  ( 0.000000000000000000, -1.000000000000000000, 0.000000000000000000 ) ) ;
#86422=DIRECTION ( 'NONE',  ( -1.000000000000000000, -0.000000000000000000, -0.000000000000000000 ) ) ;
#86427=ORIENTED_EDGE ( 'NONE', *, *, #5996, .T. ) ;
#86438=CONICAL_SURFACE ( 'NONE', #39914, 4.000000000000001776, 0.9599310885968808105 ) ;
#86461=CARTESIAN_POINT ( 'NONE',  ( 27.33349330513380337, 1.593028355512270567E-15, 0.000000000000000000 ) ) ;
#86473=ORIENTED_EDGE ( 'NONE', *, *, #87004, .T. ) ;
#86482=VERTEX_POINT ( 'NONE', #71593 ) ;
#86491=CARTESIAN_POINT ( 'NONE',  ( 21.08349330513380337, 1.593028355512270567E-15, 0.000000000000000000 ) ) ;
#86497=CARTESIAN_POINT ( 'NONE',  ( 0.000000000000000000, 0.000000000000000000, 0.000000000000000000 ) ) ;
#86522=EDGE_CURVE ( 'NONE', #87130, #44939, #88780, .T. ) ;
#86536=ORIENTED_EDGE ( 'NONE', *, *, #103541, .T. ) ;
#86541=ADVANCED_FACE ( 'NONE', ( #62466 ), #21674, .T. ) ;
#86545=ORIENTED_EDGE ( 'NONE', *, *, #97090, .T. ) ;
#86551=CARTESIAN_POINT ( 'NONE',  ( 24.83349330513380337, -7.703719777548943412E-31, 4.000000000000001776 ) ) ;
#86573=CARTESIAN_POINT ( 'NONE',  ( 11.08349330513380160, -7.703719777548943412E-31, 4.000000000000001776 ) ) ;
#86592=ORIENTED_EDGE ( 'NONE', *, *, #65113, .F. ) ;
#86593=AXIS2_PLACEMENT_3D ( 'NONE', #65917, #83682, #98796 ) ;
#86604=DIRECTION ( 'NONE',  ( -1.000000000000000000, -0.000000000000000000, -0.000000000000000000 ) ) ;
#86615=CARTESIAN_POINT ( 'NONE',  ( 15.11650669486618881, 4.898587196589411843E-16, -4.000000000000000888 ) ) ;
#86619=CARTESIAN_POINT ( 'NONE',  ( 19.34999999999999787, 1.533819458162526451E-15, 0.000000000000000000 ) ) ;
#86643=CARTESIAN_POINT ( 'NONE',  ( 43.58349330513380693, 1.593028355512270567E-15, 0.000000000000000000 ) ) ;
#86683=DIRECTION ( 'NONE',  ( -1.000000000000000000, -1.224606353822377258E-16, -0.000000000000000000 ) ) ;
#86707=FACE_OUTER_BOUND ( 'NONE', #17345, .T. ) ;
#86708=ADVANCED_FACE ( 'NONE', ( #54894 ), #4394, .T. ) ;
#86709=VERTEX_POINT ( 'NONE', #23632 ) ;
#86713=DIRECTION ( 'NONE',  ( -1.000000000000000000, -0.000000000000000000, -0.000000000000000000 ) ) ;
#86715=ORIENTED_EDGE ( 'NONE', *, *, #14040, .F. ) ;
#86730=LINE ( 'NONE', #12804, #87612 ) ;
#86733=CARTESIAN_POINT ( 'NONE',  ( 6.683837171061802529, 3.955946848495958346, -6.851900933636989599 ) ) ;
#86745=ORIENTED_EDGE ( 'NONE', *, *, #24505, .T. ) ;
#86749=CARTESIAN_POINT ( 'NONE',  ( 6.585531397294614564, 4.023063057964794353, 6.499999999999997335 ) ) ;
#86756=ADVANCED_FACE ( 'NONE', ( #41913 ), #45768, .F. ) ;
#86765=EDGE_LOOP ( 'NONE', ( #91220, #30785, #5184, #93863, #44378 ) ) ;
#86778=DIRECTION ( 'NONE',  ( 1.000000000000000000, 0.000000000000000000, 0.000000000000000000 ) ) ;
#86784=EDGE_CURVE ( 'NONE', #61668, #76086, #67274, .T. ) ;
#86785=CARTESIAN_POINT ( 'NONE',  ( 5.947762761376478302, 6.880090707843046438, 1.083333333333333481 ) ) ;
#86794=EDGE_CURVE ( 'NONE', #21594, #85984, #41096, .T. ) ;
#86806=LINE ( 'NONE', #60931, #56142 ) ;
#86820=ADVANCED_FACE ( 'NONE', ( #82910 ), #7590, .T. ) ;
#86847=EDGE_LOOP ( 'NONE', ( #38562, #73554, #101640, #22445, #58828, #23713 ) ) ;
#86885=VERTEX_POINT ( 'NONE', #84515 ) ;
#86904=DIRECTION ( 'NONE',  ( -1.000000000000000000, -1.224606353822377258E-16, -0.000000000000000000 ) ) ;
#86922=CARTESIAN_POINT ( 'NONE',  ( 19.34999999999999787, 1.533819458162526451E-15, 0.000000000000000000 ) ) ;
#86927=VERTEX_POINT ( 'NONE', #4660 ) ;
#86930=CARTESIAN_POINT ( 'NONE',  ( 39.83349330513380693, 4.000000000000003553, 0.000000000000000000 ) ) ;
#87004=EDGE_CURVE ( 'NONE', #99083, #95250, #26849, .T. ) ;
#87013=ORIENTED_EDGE ( 'NONE', *, *, #74203, .T. ) ;
#87016=AXIS2_PLACEMENT_3D ( 'NONE', #54885, #71605, #44298 ) ;
#87029=CARTESIAN_POINT ( 'NONE',  ( 0.5805565836007602343, 3.752776749732561257, -6.499999999999999112 ) ) ;
#87035=CYLINDRICAL_SURFACE ( 'NONE', #58309, 4.000000000000000000 ) ;
#87050=EDGE_CURVE ( 'NONE', #1155, #84498, #14522, .T. ) ;
#87071=EDGE_CURVE ( 'NONE', #74465, #55990, #69686, .T. ) ;
#87073=AXIS2_PLACEMENT_3D ( 'NONE', #28737, #76170, #28209 ) ;
#87085=DIRECTION ( 'NONE',  ( -1.000000000000000000, -0.000000000000000000, -0.000000000000000000 ) ) ;
#87105=EDGE_CURVE ( 'NONE', #49899, #6924, #24879, .T. ) ;
#87110=VERTEX_POINT ( 'NONE', #13786 ) ;
#87113=DIRECTION ( 'NONE',  ( 0.000000000000000000, 0.000000000000000000, 1.000000000000000000 ) ) ;
#87130=VERTEX_POINT ( 'NONE', #75748 ) ;
#87161=VERTEX_POINT ( 'NONE', #99478 ) ;
#87168=CARTESIAN_POINT ( 'NONE',  ( 6.326592304916277776, -5.253140224433049177, 4.564380808752273921 ) ) ;
#87188=ORIENTED_EDGE ( 'NONE', *, *, #100533, .F. ) ;
#87191=AXIS2_PLACEMENT_3D ( 'NONE', #64105, #46831, #13920 ) ;
#87192=FACE_OUTER_BOUND ( 'NONE', #97548, .T. ) ;
#87194=FACE_OUTER_BOUND ( 'NONE', #106569, .T. ) ;
#87208=CARTESIAN_POINT ( 'NONE',  ( 0.5805565836007643421, -3.752776749732575468, -6.499999999999999112 ) ) ;
#87217=AXIS2_PLACEMENT_3D ( 'NONE', #90410, #84306, #17060 ) ;
#87247=EDGE_LOOP ( 'NONE', ( #41491, #106295, #38618, #29603, #49327, #105463 ) ) ;
#87269=AXIS2_PLACEMENT_3D ( 'NONE', #82851, #66134, #33794 ) ;
#87270=VERTEX_POINT ( 'NONE', #2384 ) ;
#87274=DIRECTION ( 'NONE',  ( 1.000000000000000000, 1.224606353822377258E-16, 0.000000000000000000 ) ) ;
#87285=DIRECTION ( 'NONE',  ( 0.000000000000000000, 1.000000000000000000, 0.000000000000000000 ) ) ;
#87344=AXIS2_PLACEMENT_3D ( 'NONE', #65488, #75691, #7763 ) ;
#87355=CARTESIAN_POINT ( 'NONE',  ( 0.05533025579362559065, -4.993776679985863609, -4.350525068611871049 ) ) ;
#87364=AXIS2_PLACEMENT_3D ( 'NONE', #83724, #69171, #76701 ) ;
#87366=DIRECTION ( 'NONE',  ( -1.000000000000000000, -0.000000000000000000, -0.000000000000000000 ) ) ;
#87383=CARTESIAN_POINT ( 'NONE',  ( 47.33349330513379982, 4.898587196589405926E-16, -4.000000000000001776 ) ) ;
#87387=AXIS2_PLACEMENT_3D ( 'NONE', #94542, #62184, #12520 ) ;
#87408=AXIS2_PLACEMENT_3D ( 'NONE', #5796, #95887, #53301 ) ;
#87415=VERTEX_POINT ( 'NONE', #83632 ) ;
#87435=ADVANCED_FACE ( 'NONE', ( #41592 ), #57637, .T. ) ;
#87449=EDGE_LOOP ( 'NONE', ( #37383, #5257, #92602, #1762, #657, #41492 ) ) ;
#87451=CARTESIAN_POINT ( 'NONE',  ( 33.86650669486618881, 1.474610560812782335E-15, 0.000000000000000000 ) ) ;
#87458=DIRECTION ( 'NONE',  ( 0.5735764363510462704, 0.8191520442889915765, 0.000000000000000000 ) ) ;
#87486=CARTESIAN_POINT ( 'NONE',  ( 13.58349330513380160, -4.000000000000000000, 4.898587196589415787E-16 ) ) ;
#87499=EDGE_CURVE ( 'NONE', #29512, #20310, #45666, .T. ) ;
#87512=ORIENTED_EDGE ( 'NONE', *, *, #86255, .F. ) ;
#87521=ORIENTED_EDGE ( 'NONE', *, *, #64988, .F. ) ;
#87538=AXIS2_PLACEMENT_3D ( 'NONE', #60336, #19375, #71985 ) ;
#87547=FACE_OUTER_BOUND ( 'NONE', #82288, .T. ) ;
#87548=CARTESIAN_POINT ( 'NONE',  ( 6.683837171061805194, -3.955946848495972556, -6.851900933636989599 ) ) ;
#87557=DIRECTION ( 'NONE',  ( -1.000000000000000000, -0.000000000000000000, -0.000000000000000000 ) ) ;
#87564=DIRECTION ( 'NONE',  ( 0.5735764363510462704, 0.8191520442889915765, 0.000000000000000000 ) ) ;
#87573=DIRECTION ( 'NONE',  ( -1.000000000000000000, -1.224606353822377258E-16, -0.000000000000000000 ) ) ;
#87606=CARTESIAN_POINT ( 'NONE',  ( 31.36650669486618881, 1.474610560812782335E-15, 0.000000000000000000 ) ) ;
#87612=VECTOR ( 'NONE', #45719, 1000.000000000000000 ) ;
#87665=CIRCLE ( 'NONE', #103128, 4.000000000000000888 ) ;
#87672=ORIENTED_EDGE ( 'NONE', *, *, #92013, .T. ) ;
#87678=CARTESIAN_POINT ( 'NONE',  ( 5.947762761376476526, -4.378239541354671971, -5.416666666666665186 ) ) ;
#87698=( NAMED_UNIT ( * ) PLANE_ANGLE_UNIT ( ) SI_UNIT ( $, .RADIAN. ) );
#87706=AXIS2_PLACEMENT_3D ( 'NONE', #68514, #12376, #85216 ) ;
#87712=CARTESIAN_POINT ( 'NONE',  ( 18.58349330513380337, 1.593028355512270567E-15, 0.000000000000000000 ) ) ;
#87714=ADVANCED_FACE ( 'NONE', ( #51914 ), #100469, .T. ) ;
#87748=DIRECTION ( 'NONE',  ( 0.000000000000000000, 1.000000000000000000, 0.000000000000000000 ) ) ;
#87756=CARTESIAN_POINT ( 'NONE',  ( 32.61650669486618881, 1.474610560812782335E-15, 0.000000000000000000 ) ) ;
#87765=B_SPLINE_CURVE_WITH_KNOTS ( 'NONE', 3,
 ( #97632, #57175, #32943, #15134, #16192, #81977 ),
 .UNSPECIFIED., .F., .F.,
 ( 4, 2, 4 ),
 ( 0.003990927807053575027, 0.005983070073873390966, 0.007975212340693206906 ),
 .UNSPECIFIED. ) ;
#87767=CARTESIAN_POINT ( 'NONE',  ( 18.58349330513380337, 4.000000000000002665, 0.000000000000000000 ) ) ;
#87779=ORIENTED_EDGE ( 'NONE', *, *, #70250, .T. ) ;
#87797=CONICAL_SURFACE ( 'NONE', #80839, 4.000000000000001776, 0.9599310885968808105 ) ;
#87805=CARTESIAN_POINT ( 'NONE',  ( 13.09999999999999787, 1.533819458162526451E-15, 0.000000000000000000 ) ) ;
#87806=DIRECTION ( 'NONE',  ( 0.000000000000000000, -1.000000000000000000, 0.000000000000000000 ) ) ;
#87886=DIRECTION ( 'NONE',  ( -1.000000000000000000, -1.224606353822377258E-16, -0.000000000000000000 ) ) ;
#87920=CARTESIAN_POINT ( 'NONE',  ( 30.11650669486618881, 1.474610560812782335E-15, 0.000000000000000000 ) ) ;
#87952=CARTESIAN_POINT ( 'NONE',  ( 0.000000000000000000, -5.629165124598843661, 3.250000000000012879 ) ) ;
#87974=CARTESIAN_POINT ( 'NONE',  ( 19.83349330513379982, 1.593028355512270567E-15, 0.000000000000000000 ) ) ;
#88014=CARTESIAN_POINT ( 'NONE',  ( 5.980073869853586466, 2.767359234578507188, -6.499999999999999112 ) ) ;
#88022=EDGE_LOOP ( 'NONE', ( #24171, #26554, #39803, #48038, #45830 ) ) ;
#88044=ORIENTED_EDGE ( 'NONE', *, *, #97164, .T. ) ;
#88062=DIRECTION ( 'NONE',  ( 1.000000000000000000, 0.000000000000000000, -0.000000000000000000 ) ) ;
#88085=CARTESIAN_POINT ( 'NONE',  ( 0.000000000000000000, 0.000000000000000000, 0.000000000000000000 ) ) ;
#88121=AXIS2_PLACEMENT_3D ( 'NONE', #1864, #57980, #25673 ) ;
#88122=ORIENTED_EDGE ( 'NONE', *, *, #29529, .T. ) ;
#88160=CYLINDRICAL_SURFACE ( 'NONE', #63733, 4.000000000000000000 ) ;
#88164=SHAPE_REPRESENTATION ( 'hex flange bolt_din_DIN 6921 - M8 x 40 x 40-S', ( #10728 ), #33394 ) ;
#88180=CARTESIAN_POINT ( 'NONE',  ( 33.58349330513379982, 4.000000000000003553, 0.000000000000000000 ) ) ;
#88185=DIRECTION ( 'NONE',  ( 0.000000000000000000, -1.000000000000000000, 0.000000000000000000 ) ) ;
#88213=CARTESIAN_POINT ( 'NONE',  ( 11.84999999999999787, 1.533819458162526451E-15, 0.000000000000000000 ) ) ;
#88225=( NAMED_UNIT ( * ) SI_UNIT ( $, .STERADIAN. ) SOLID_ANGLE_UNIT ( ) );
#88256=AXIS2_PLACEMENT_3D ( 'NONE', #36152, #78673, #79217 ) ;
#88269=CARTESIAN_POINT ( 'NONE',  ( 0.000000000000000000, 0.000000000000000000, 0.000000000000000000 ) ) ;
#88284=ORIENTED_EDGE ( 'NONE', *, *, #64647, .F. ) ;
#88304=VERTEX_POINT ( 'NONE', #5253 ) ;
#88337=AXIS2_PLACEMENT_3D ( 'NONE', #94775, #85613, #102848 ) ;
#88348=DIRECTION ( 'NONE',  ( -1.000000000000000000, -1.224606353822377258E-16, -0.000000000000000000 ) ) ;
#88371=CYLINDRICAL_SURFACE ( 'NONE', #87191, 4.000000000000000000 ) ;
#88404=EDGE_LOOP ( 'NONE', ( #26667, #4000, #1220, #59699 ) ) ;
#88419=CARTESIAN_POINT ( 'NONE',  ( 28.58349330513380337, 1.593028355512270567E-15, 0.000000000000000000 ) ) ;
#88425=EDGE_LOOP ( 'NONE', ( #95050, #26406, #28049, #3570, #105326 ) ) ;
#88483=CARTESIAN_POINT ( 'NONE',  ( 0.4033376246892543260, -7.198601258566906580, 0.5316568767328693212 ) ) ;
#88488=ORIENTED_EDGE ( 'NONE', *, *, #33542, .T. ) ;
#88503=CARTESIAN_POINT ( 'NONE',  ( 36.36650669486618881, 1.474610560812782335E-15, 0.000000000000000000 ) ) ;
#88508=ORIENTED_EDGE ( 'NONE', *, *, #50073, .T. ) ;
#88519=CIRCLE ( 'NONE', #19658, 4.000000000000001776 ) ;
#88546=CARTESIAN_POINT ( 'NONE',  ( 16.08349330513380337, 1.593028355512270567E-15, 0.000000000000000000 ) ) ;
#88549=VERTEX_POINT ( 'NONE', #43875 ) ;
#88550=CARTESIAN_POINT ( 'NONE',  ( 35.11650669486618170, -3.851859888774471706E-31, 4.000000000000000888 ) ) ;
#88554=ADVANCED_BREP_SHAPE_REPRESENTATION ( '', ( #88996, #10728 ), #33394 ) ;
#88575=CIRCLE ( 'NONE', #55821, 3.309500000000001663 ) ;
#88585=CARTESIAN_POINT ( 'NONE',  ( 15.11650669486618881, 1.474610560812782335E-15, 0.000000000000000000 ) ) ;
#88588=AXIS2_PLACEMENT_3D ( 'NONE', #15523, #56503, #89950 ) ;
#88659=CARTESIAN_POINT ( 'NONE',  ( 33.58349330513379982, 1.593028355512270567E-15, 0.000000000000000000 ) ) ;
#88685=ORIENTED_EDGE ( 'NONE', *, *, #62568, .F. ) ;
#88699=CARTESIAN_POINT ( 'NONE',  ( 0.5805565836007654523, 7.505553499465140277, 2.211437577243512467E-16 ) ) ;
#88704=AXIS2_PLACEMENT_3D ( 'NONE', #979, #43089, #58749 ) ;
#88711=AXIS2_PLACEMENT_3D ( 'NONE', #19317, #103370, #102298 ) ;
#88722=EDGE_CURVE ( 'NONE', #64980, #66178, #50618, .T. ) ;
#88723=ORIENTED_EDGE ( 'NONE', *, *, #70293, .F. ) ;
#88736=PLANE ( 'NONE',  #104618 ) ;
#88765=AXIS2_PLACEMENT_3D ( 'NONE', #27098, #52384, #51853 ) ;
#88770=CARTESIAN_POINT ( 'NONE',  ( 23.86650669486618881, 1.474610560812782335E-15, 0.000000000000000000 ) ) ;
#88777=AXIS2_PLACEMENT_3D ( 'NONE', #20819, #4048, #69848 ) ;
#88780=CIRCLE ( 'NONE', #40580, 3.309500000000001663 ) ;
#88783=EDGE_LOOP ( 'NONE', ( #68695, #60604, #27967, #93764, #31880 ) ) ;
#88822=AXIS2_PLACEMENT_3D ( 'NONE', #74173, #41811, #83333 ) ;
#88829=EDGE_CURVE ( 'NONE', #25666, #16749, #35997, .T. ) ;
#88858=ORIENTED_EDGE ( 'NONE', *, *, #27024, .F. ) ;
#88901=VECTOR ( 'NONE', #20540, 1000.000000000000000 ) ;
#88908=ADVANCED_FACE ( 'NONE', ( #53723 ), #85582, .T. ) ;
#88914=CARTESIAN_POINT ( 'NONE',  ( 6.162888688655344005, 3.752776749732561257, -6.499999999999999112 ) ) ;
#88915=EDGE_CURVE ( 'NONE', #56862, #35387, #54471, .T. ) ;
#88956=ORIENTED_EDGE ( 'NONE', *, *, #105521, .F. ) ;
#88970=DIRECTION ( 'NONE',  ( 1.000000000000000000, 1.224606353822377258E-16, 0.000000000000000000 ) ) ;
#88996=MANIFOLD_SOLID_BREP ( 'ThdSchPat', #24018 ) ;
#89056=EDGE_CURVE ( 'NONE', #2115, #45306, #72283, .T. ) ;
#89064=AXIS2_PLACEMENT_3D ( 'NONE', #15716, #14636, #49131 ) ;
#89086=CARTESIAN_POINT ( 'NONE',  ( 40.59999999999999432, 3.309500000000003439, 4.052968581778167743E-16 ) ) ;
#89104=CIRCLE ( 'NONE', #44373, 4.000000000000000888 ) ;
#89108=DIRECTION ( 'NONE',  ( -1.000000000000000000, -0.000000000000000000, -0.000000000000000000 ) ) ;
#89129=DIRECTION ( 'NONE',  ( 0.000000000000000000, -1.000000000000000000, 0.000000000000000000 ) ) ;
#89149=AXIS2_PLACEMENT_3D ( 'NONE', #103548, #23179, #29698 ) ;
#89152=DIRECTION ( 'NONE',  ( 0.000000000000000000, -1.000000000000000000, 0.000000000000000000 ) ) ;
#89184=CARTESIAN_POINT ( 'NONE',  ( 18.58349330513380337, -4.000000000000000888, 4.898587196589416773E-16 ) ) ;
#89196=VERTEX_POINT ( 'NONE', #99207 ) ;
#89209=AXIS2_PLACEMENT_3D ( 'NONE', #88770, #14865, #38646 ) ;
#89234=CIRCLE ( 'NONE', #44427, 4.000000000000000888 ) ;
#89249=ORIENTED_EDGE ( 'NONE', *, *, #46719, .T. ) ;
#89279=DIRECTION ( 'NONE',  ( 0.000000000000000000, 0.000000000000000000, 1.000000000000000000 ) ) ;
#89281=DIRECTION ( 'NONE',  ( -1.000000000000000000, -1.224606353822377258E-16, -0.000000000000000000 ) ) ;
#89286=FILL_AREA_STYLE ('',( #5697 ) ) ;
#89298=ADVANCED_FACE ( 'NONE', ( #98154 ), #15449, .T. ) ;
#89299=ORIENTED_EDGE ( 'NONE', *, *, #35206, .T. ) ;
#89328=VECTOR ( 'NONE', #55208, 1000.000000000000000 ) ;
#89357=CARTESIAN_POINT ( 'NONE',  ( 46.36650669486618881, 4.898587196589411843E-16, -4.000000000000000888 ) ) ;
#89374=DIRECTION ( 'NONE',  ( 0.000000000000000000, 1.000000000000000000, 0.000000000000000000 ) ) ;
#89387=ORIENTED_EDGE ( 'NONE', *, *, #18377, .T. ) ;
#89407=ORIENTED_EDGE ( 'NONE', *, *, #89462, .T. ) ;
#89462=EDGE_CURVE ( 'NONE', #31692, #77337, #15225, .T. ) ;
#89470=EDGE_CURVE ( 'NONE', #77294, #103513, #25924, .T. ) ;
#89492=CARTESIAN_POINT ( 'NONE',  ( 47.33349330513379982, 1.593028355512270567E-15, 0.000000000000000000 ) ) ;
#89510=ORIENTED_EDGE ( 'NONE', *, *, #44294, .F. ) ;
#89528=CONICAL_SURFACE ( 'NONE', #44736, 3.309500000000001663, 0.9599310885968770357 ) ;
#89564=DIRECTION ( 'NONE',  ( 0.000000000000000000, 1.000000000000000000, 0.000000000000000000 ) ) ;
#89566=DIRECTION ( 'NONE',  ( -1.000000000000000000, -1.224606353822377258E-16, -0.000000000000000000 ) ) ;
#89598=EDGE_CURVE ( 'NONE', #85984, #89196, #21424, .T. ) ;
#89605=FACE_OUTER_BOUND ( 'NONE', #26195, .T. ) ;
#89629=EDGE_LOOP ( 'NONE', ( #40825, #12562, #61382, #17495, #22115 ) ) ;
#89669=CARTESIAN_POINT ( 'NONE',  ( 29.83349330513380337, 1.593028355512270567E-15, 0.000000000000000000 ) ) ;
#89670=ADVANCED_FACE ( 'NONE', ( #89944 ), #73801, .T. ) ;
#89677=ORIENTED_EDGE ( 'NONE', *, *, #59971, .T. ) ;
#89680=CARTESIAN_POINT ( 'NONE',  ( 42.61650669486618881, -3.851859888774471706E-31, 4.000000000000000888 ) ) ;
#89695=ORIENTED_EDGE ( 'NONE', *, *, #29602, .F. ) ;
#89733=AXIS2_PLACEMENT_3D ( 'NONE', #77735, #70167, #29226 ) ;
#89747=FACE_OUTER_BOUND ( 'NONE', #39787, .T. ) ;
#89751=DIRECTION ( 'NONE',  ( -1.000000000000000000, -1.224606353822377258E-16, -0.000000000000000000 ) ) ;
#89768=ORIENTED_EDGE ( 'NONE', *, *, #9474, .F. ) ;
#89797=VECTOR ( 'NONE', #52802, 1000.000000000000000 ) ;
#89818=ORIENTED_EDGE ( 'NONE', *, *, #20511, .F. ) ;
#89831=AXIS2_PLACEMENT_3D ( 'NONE', #21107, #63115, #12947 ) ;
#89840=DIRECTION ( 'NONE',  ( 0.000000000000000000, -1.000000000000000000, 0.000000000000000000 ) ) ;
#89854=LINE ( 'NONE', #264, #62373 ) ;
#89874=CIRCLE ( 'NONE', #88121, 4.000000000000001776 ) ;
#89910=CARTESIAN_POINT ( 'NONE',  ( 0.000000000000000000, 4.898587196589412829E-16, -4.000000000000000000 ) ) ;
#89919=ADVANCED_FACE ( 'NONE', ( #67282 ), #74806, .T. ) ;
#89931=DIRECTION ( 'NONE',  ( 0.000000000000000000, -1.000000000000000000, 0.000000000000000000 ) ) ;
#89944=FACE_OUTER_BOUND ( 'NONE', #47849, .T. ) ;
#89946=ORIENTED_EDGE ( 'NONE', *, *, #76903, .F. ) ;
#89950=DIRECTION ( 'NONE',  ( 0.000000000000000000, -1.000000000000000000, 0.000000000000000000 ) ) ;
#89958=VERTEX_POINT ( 'NONE', #67801 ) ;
#89976=CARTESIAN_POINT ( 'NONE',  ( 46.84999999999999432, 3.309500000000003439, 0.000000000000000000 ) ) ;
#89977=CARTESIAN_POINT ( 'NONE',  ( 45.59999999999999432, 3.309500000000003439, 0.000000000000000000 ) ) ;
#89989=DIRECTION ( 'NONE',  ( -1.000000000000000000, -0.000000000000000000, -0.000000000000000000 ) ) ;
#89999=EDGE_CURVE ( 'NONE', #60237, #32972, #102833, .T. ) ;
#90026=B_SPLINE_CURVE_WITH_KNOTS ( 'NONE', 3,
 ( #84052, #91625, #17735, #99155, #50594, #35003, #74872, #960, #26395, #9610 ),
 .UNSPECIFIED., .F., .F.,
 ( 4, 2, 2, 2, 4 ),
 ( 0.000000000000000000, 0.001993803085173304328, 0.003987606170346608657, 0.005981409255519911684, 0.007975212340693215579 ),
 .UNSPECIFIED. ) ;
#90035=DIRECTION ( 'NONE',  ( -1.000000000000000000, -1.224606353822377258E-16, -0.000000000000000000 ) ) ;
#90044=ORIENTED_EDGE ( 'NONE', *, *, #61958, .T. ) ;
#90066=EDGE_LOOP ( 'NONE', ( #25772, #88508, #38696, #9711, #31769, #19136 ) ) ;
#90070=DIRECTION ( 'NONE',  ( 0.000000000000000000, -1.000000000000000000, 0.000000000000000000 ) ) ;
#90088=AXIS2_PLACEMENT_3D ( 'NONE', #53756, #36559, #45155 ) ;
#90134=B_SPLINE_CURVE_WITH_KNOTS ( 'NONE', 3,
 ( #77634, #46848, #46331, #36685, #102974 ),
 .UNSPECIFIED., .F., .F.,
 ( 4, 1, 4 ),
 ( 0.000000000000000000, 0.003752776749732568331, 0.007505553499465136662 ),
 .UNSPECIFIED. ) ;
#90177=DIRECTION ( 'NONE',  ( -1.000000000000000000, -0.000000000000000000, -0.000000000000000000 ) ) ;
#90198=AXIS2_PLACEMENT_3D ( 'NONE', #67660, #16985, #8872 ) ;
#90244=FACE_OUTER_BOUND ( 'NONE', #79772, .T. ) ;
#90246=DIRECTION ( 'NONE',  ( -1.000000000000000000, -0.000000000000000000, -0.000000000000000000 ) ) ;
#90269=CARTESIAN_POINT ( 'NONE',  ( 48.10000000000000142, 0.000000000000000000, 3.309499999999999886 ) ) ;
#90327=ORIENTED_EDGE ( 'NONE', *, *, #98957, .T. ) ;
#90347=ORIENTED_EDGE ( 'NONE', *, *, #31090, .F. ) ;
#90398=CARTESIAN_POINT ( 'NONE',  ( 12.61650669486618881, -3.851859888774471706E-31, 4.000000000000000888 ) ) ;
#90410=CARTESIAN_POINT ( 'NONE',  ( 11.08349330513380160, 1.593028355512270567E-15, 0.000000000000000000 ) ) ;
#90428=CARTESIAN_POINT ( 'NONE',  ( 12.61650669486618881, 1.474610560812782335E-15, 0.000000000000000000 ) ) ;
#90438=ORIENTED_EDGE ( 'NONE', *, *, #91691, .T. ) ;
#90477=DIRECTION ( 'NONE',  ( -1.000000000000000000, -1.224606353822377258E-16, -0.000000000000000000 ) ) ;
#90482=CARTESIAN_POINT ( 'NONE',  ( 6.644028492724104673, 7.802520252160765502, -5.627655413974009852E-13 ) ) ;
#90499=VECTOR ( 'NONE', #66484, 1000.000000000000114 ) ;
#90508=FACE_OUTER_BOUND ( 'NONE', #75362, .T. ) ;
#90518=CARTESIAN_POINT ( 'NONE',  ( 0.000000000000000000, 0.000000000000000000, 0.000000000000000000 ) ) ;
#90520=DIRECTION ( 'NONE',  ( 0.000000000000000000, -1.000000000000000000, 0.000000000000000000 ) ) ;
#90571=CIRCLE ( 'NONE', #4420, 6.500000000000000888 ) ;
#90599=CONICAL_SURFACE ( 'NONE', #87217, 4.000000000000001776, 0.9599310885968808105 ) ;
#90609=CARTESIAN_POINT ( 'NONE',  ( 12.61650669486618881, 4.000000000000003553, 4.898587196589414801E-16 ) ) ;
#90618=AXIS2_PLACEMENT_3D ( 'NONE', #98791, #26561, #73992 ) ;
#90648=DIRECTION ( 'NONE',  ( -1.000000000000000000, -1.224606353822377258E-16, -0.000000000000000000 ) ) ;
#90662=DIRECTION ( 'NONE',  ( -1.000000000000000000, -1.224606353822377258E-16, -0.000000000000000000 ) ) ;
#90731=CIRCLE ( 'NONE', #94201, 3.309500000000001663 ) ;
#90735=ORIENTED_EDGE ( 'NONE', *, *, #18071, .F. ) ;
#90759=CARTESIAN_POINT ( 'NONE',  ( 47.40949999999999420, 0.000000000000000000, 0.000000000000000000 ) ) ;
#90765=VECTOR ( 'NONE', #86713, 1000.000000000000000 ) ;
#90766=CIRCLE ( 'NONE', #20220, 4.000000000000001776 ) ;
#90784=AXIS2_PLACEMENT_3D ( 'NONE', #88546, #105774, #41575 ) ;
#90807=CARTESIAN_POINT ( 'NONE',  ( 16.08349330513380337, 1.593028355512270567E-15, 0.000000000000000000 ) ) ;
#90821=ORIENTED_EDGE ( 'NONE', *, *, #67403, .F. ) ;
#90850=FACE_OUTER_BOUND ( 'NONE', #64081, .T. ) ;
#90857=ORIENTED_EDGE ( 'NONE', *, *, #93126, .T. ) ;
#90870=CARTESIAN_POINT ( 'NONE',  ( 6.222742520105472686, -3.584500230190552639, -6.791463481567638460 ) ) ;
#90894=EDGE_LOOP ( 'NONE', ( #14842, #36648, #61078, #90347, #67704, #58757 ) ) ;
#90903=DIRECTION ( 'NONE',  ( -1.000000000000000000, -1.224606353822377258E-16, -0.000000000000000000 ) ) ;
#90921=ADVANCED_FACE ( 'NONE', ( #43940 ), #89528, .T. ) ;
#90980=CYLINDRICAL_SURFACE ( 'NONE', #7447, 4.000000000000000000 ) ;
#90982=DIRECTION ( 'NONE',  ( -1.000000000000000000, -0.000000000000000000, -0.000000000000000000 ) ) ;
#90986=FACE_OUTER_BOUND ( 'NONE', #78536, .T. ) ;
#91004=VECTOR ( 'NONE', #17734, 1000.000000000000000 ) ;
#91021=CARTESIAN_POINT ( 'NONE',  ( 6.169949891408688103, 6.308465495019028424, -2.073417244830852990 ) ) ;
#91032=DIRECTION ( 'NONE',  ( 0.000000000000000000, -1.000000000000000000, 0.000000000000000000 ) ) ;
#91039=CARTESIAN_POINT ( 'NONE',  ( 33.09999999999999432, 1.533819458162526451E-15, 0.000000000000000000 ) ) ;
#91053=CONICAL_SURFACE ( 'NONE', #11798, 4.000000000000001776, 0.9599310885968808105 ) ;
#91105=DIRECTION ( 'NONE',  ( 0.5735764363510462704, 0.8191520442889915765, 0.000000000000000000 ) ) ;
#91112=DIRECTION ( 'NONE',  ( -1.000000000000000000, -1.224606353822377258E-16, -0.000000000000000000 ) ) ;
#91115=DIRECTION ( 'NONE',  ( -1.000000000000000000, -0.000000000000000000, -0.000000000000000000 ) ) ;
#91123=CARTESIAN_POINT ( 'NONE',  ( 34.35000000000000142, 1.533819458162526451E-15, 0.000000000000000000 ) ) ;
#91132=ORIENTED_EDGE ( 'NONE', *, *, #103254, .F. ) ;
#91136=EDGE_CURVE ( 'NONE', #99943, #65781, #60678, .T. ) ;
#91171=ORIENTED_EDGE ( 'NONE', *, *, #59351, .F. ) ;
#91175=VERTEX_POINT ( 'NONE', #13680 ) ;
#91177=CARTESIAN_POINT ( 'NONE',  ( 35.11650669486618170, 1.474610560812782335E-15, 0.000000000000000000 ) ) ;
#91203=CARTESIAN_POINT ( 'NONE',  ( 31.08349330513380337, 1.593028355512270567E-15, 0.000000000000000000 ) ) ;
#91220=ORIENTED_EDGE ( 'NONE', *, *, #29060, .F. ) ;
#91248=ORIENTED_EDGE ( 'NONE', *, *, #70494, .F. ) ;
#91268=CARTESIAN_POINT ( 'NONE',  ( 42.33349330513380693, 4.000000000000002665, 0.000000000000000000 ) ) ;
#91298=ORIENTED_EDGE ( 'NONE', *, *, #58100, .F. ) ;
#91299=DIRECTION ( 'NONE',  ( -1.000000000000000000, -1.224606353822377258E-16, -0.000000000000000000 ) ) ;
#91386=ORIENTED_EDGE ( 'NONE', *, *, #28814, .F. ) ;
#91403=VECTOR ( 'NONE', #51292, 1000.000000000000000 ) ;
#91405=ORIENTED_EDGE ( 'NONE', *, *, #97164, .F. ) ;
#91434=CARTESIAN_POINT ( 'NONE',  ( 6.162888688655350222, -7.505553499465148271, 0.000000000000000000 ) ) ;
#91481=CARTESIAN_POINT ( 'NONE',  ( 38.86650669486618881, 1.474610560812782335E-15, 0.000000000000000000 ) ) ;
#91497=CARTESIAN_POINT ( 'NONE',  ( 45.11650669486618881, -3.851859888774471706E-31, 4.000000000000000888 ) ) ;
#91530=ORIENTED_EDGE ( 'NONE', *, *, #106561, .T. ) ;
#91532=AXIS2_PLACEMENT_3D ( 'NONE', #48858, #66122, #106575 ) ;
#91549=CARTESIAN_POINT ( 'NONE',  ( 12.33349330513380337, 1.593028355512270567E-15, 0.000000000000000000 ) ) ;
#91594=DIRECTION ( 'NONE',  ( -1.000000000000000000, -0.000000000000000000, -0.000000000000000000 ) ) ;
#91603=CARTESIAN_POINT ( 'NONE',  ( 6.167866516170612989, -1.339763354879983215, -6.499999999999395150 ) ) ;
#91625=CARTESIAN_POINT ( 'NONE',  ( 6.562974947121713143, 7.579827465851455948, 0.5629870116737627495 ) ) ;
#91637=CARTESIAN_POINT ( 'NONE',  ( 0.000000000000000000, 0.000000000000000000, 0.000000000000000000 ) ) ;
#91651=EDGE_CURVE ( 'NONE', #79598, #29102, #94855, .T. ) ;
#91652=ORIENTED_EDGE ( 'NONE', *, *, #71134, .T. ) ;
#91691=EDGE_CURVE ( 'NONE', #101661, #1636, #61618, .T. ) ;
#91709=DIRECTION ( 'NONE',  ( -1.000000000000000000, -0.000000000000000000, -0.000000000000000000 ) ) ;
#91710=CARTESIAN_POINT ( 'NONE',  ( 9.349999999999997868, 3.309500000000003439, 4.052968581778167743E-16 ) ) ;
#91747=CARTESIAN_POINT ( 'NONE',  ( 6.936184427528457874, 0.000000000000000000, 0.000000000000000000 ) ) ;
#91799=CARTESIAN_POINT ( 'NONE',  ( 29.34999999999999787, -3.309499999999999886, 0.000000000000000000 ) ) ;
#91810=CIRCLE ( 'NONE', #76237, 4.000000000000001776 ) ;
#91860=ORIENTED_EDGE ( 'NONE', *, *, #94957, .F. ) ;
#91869=CARTESIAN_POINT ( 'NONE',  ( 0.000000000000000000, 0.000000000000000000, 4.000000000000000000 ) ) ;
#91889=CARTESIAN_POINT ( 'NONE',  ( 0.000000000000000000, -5.629165124598843661, 3.250000000000012879 ) ) ;
#91894=COLOUR_RGB ( '', 0.31764706, 0.68627451, 0.89019608) ;
#91901=ORIENTED_EDGE ( 'NONE', *, *, #57683, .F. ) ;
#91934=CIRCLE ( 'NONE', #50560, 0.5999999999999980904 ) ;
#91955=DIRECTION ( 'NONE',  ( -1.000000000000000000, -1.224606353822377258E-16, -0.000000000000000000 ) ) ;
#91961=ORIENTED_EDGE ( 'NONE', *, *, #45015, .F. ) ;
#91990=CARTESIAN_POINT ( 'NONE',  ( 18.58349330513380337, 1.593028355512270567E-15, 0.000000000000000000 ) ) ;
#91998=AXIS2_PLACEMENT_3D ( 'NONE', #13904, #5823, #14432 ) ;
#92013=EDGE_CURVE ( 'NONE', #81048, #78409, #84146, .T. ) ;
#92017=EDGE_LOOP ( 'NONE', ( #2248, #89299, #102951, #95990, #74147, #15088 ) ) ;
#92028=VERTEX_POINT ( 'NONE', #66905 ) ;
#92046=VERTEX_POINT ( 'NONE', #67959 ) ;
#92059=CARTESIAN_POINT ( 'NONE',  ( 5.691929483231185749, 1.734723475976807094E-15, 6.500000000000001776 ) ) ;
#92062=ORIENTED_EDGE ( 'NONE', *, *, #62421, .T. ) ;
#92065=DIRECTION ( 'NONE',  ( 0.000000000000000000, 0.000000000000000000, 1.000000000000000000 ) ) ;
#92076=CYLINDRICAL_SURFACE ( 'NONE', #96653, 4.000000000000000000 ) ;
#92107=CIRCLE ( 'NONE', #52536, 4.000000000000000888 ) ;
#92118=ORIENTED_EDGE ( 'NONE', *, *, #23714, .T. ) ;
#92128=LINE ( 'NONE', #82983, #44053 ) ;
#92131=EDGE_CURVE ( 'NONE', #83331, #59135, #86294, .T. ) ;
#92136=DIRECTION ( 'NONE',  ( 0.000000000000000000, -1.000000000000000000, 0.000000000000000000 ) ) ;
#92181=DIRECTION ( 'NONE',  ( -1.000000000000000000, -1.224606353822377258E-16, -0.000000000000000000 ) ) ;
#92184=ORIENTED_EDGE ( 'NONE', *, *, #66248, .F. ) ;
#92209=DIRECTION ( 'NONE',  ( 0.5735764363510462704, 0.8191520442889915765, 0.000000000000000000 ) ) ;
#92224=ORIENTED_EDGE ( 'NONE', *, *, #54946, .T. ) ;
#92234=CARTESIAN_POINT ( 'NONE',  ( 0.000000000000000000, 0.000000000000000000, 0.000000000000000000 ) ) ;
#92260=VERTEX_POINT ( 'NONE', #91497 ) ;
#92263=ORIENTED_EDGE ( 'NONE', *, *, #65093, .T. ) ;
#92266=DIRECTION ( 'NONE',  ( -1.000000000000000000, -0.000000000000000000, -0.000000000000000000 ) ) ;
#92272=CIRCLE ( 'NONE', #52703, 4.000000000000001776 ) ;
#92280=FACE_OUTER_BOUND ( 'NONE', #21968, .T. ) ;
#92301=DIRECTION ( 'NONE',  ( 1.000000000000000000, 1.224606353822377258E-16, 0.000000000000000000 ) ) ;
#92306=CARTESIAN_POINT ( 'NONE',  ( 6.445370176742116541, -4.584736124524379619, 5.738941594274989733 ) ) ;
#92307=CONICAL_SURFACE ( 'NONE', #44128, 4.000000000000001776, 0.9599310885968808105 ) ;
#92310=VERTEX_POINT ( 'NONE', #8954 ) ;
#92341=ORIENTED_EDGE ( 'NONE', *, *, #4977, .T. ) ;
#92344=DIRECTION ( 'NONE',  ( -1.000000000000000000, -0.000000000000000000, -0.000000000000000000 ) ) ;
#92354=DIRECTION ( 'NONE',  ( -1.000000000000000000, -1.224606353822377258E-16, -0.000000000000000000 ) ) ;
#92355=CONICAL_SURFACE ( 'NONE', #61364, 4.000000000000001776, 0.9599310885968808105 ) ;
#92365=CARTESIAN_POINT ( 'NONE',  ( 24.83349330513380337, -4.000000000000000000, 4.898587196589415787E-16 ) ) ;
#92380=ADVANCED_FACE ( 'NONE', ( #21879 ), #82816, .T. ) ;
#92408=DIRECTION ( 'NONE',  ( 0.000000000000000000, -1.000000000000000000, 0.000000000000000000 ) ) ;
#92417=ORIENTED_EDGE ( 'NONE', *, *, #64245, .T. ) ;
#92439=CARTESIAN_POINT ( 'NONE',  ( 6.222742520105476238, -7.673830019007169767, 0.2914634815676377388 ) ) ;
#92440=DIRECTION ( 'NONE',  ( 0.000000000000000000, -1.000000000000000000, 0.000000000000000000 ) ) ;
#92441=CARTESIAN_POINT ( 'NONE',  ( 31.84999999999999787, 1.533819458162526451E-15, 0.000000000000000000 ) ) ;
#92451=ORIENTED_EDGE ( 'NONE', *, *, #51467, .F. ) ;
#92459=EDGE_LOOP ( 'NONE', ( #93722, #16238, #96579, #93716, #52954 ) ) ;
#92462=ORIENTED_EDGE ( 'NONE', *, *, #67408, .F. ) ;
#92468=EDGE_CURVE ( 'NONE', #27527, #75440, #80067, .T. ) ;
#92510=CYLINDRICAL_SURFACE ( 'NONE', #23940, 4.000000000000000000 ) ;
#92519=AXIS2_PLACEMENT_3D ( 'NONE', #86461, #13048, #61104 ) ;
#92534=FACE_OUTER_BOUND ( 'NONE', #18446, .T. ) ;
#92550=ORIENTED_EDGE ( 'NONE', *, *, #105893, .T. ) ;
#92564=DIRECTION ( 'NONE',  ( 0.000000000000000000, 0.000000000000000000, 1.000000000000000000 ) ) ;
#92593=CARTESIAN_POINT ( 'NONE',  ( 0.000000000000000000, 0.000000000000000000, 0.000000000000000000 ) ) ;
#92597=DIRECTION ( 'NONE',  ( 0.000000000000000000, 1.000000000000000000, 0.000000000000000000 ) ) ;
#92602=ORIENTED_EDGE ( 'NONE', *, *, #51641, .T. ) ;
#92617=DIRECTION ( 'NONE',  ( -1.000000000000000000, -1.224606353822377258E-16, -0.000000000000000000 ) ) ;
#92618=LINE ( 'NONE', #3084, #66166 ) ;
#92619=LINE ( 'NONE', #59209, #20056 ) ;
#92622=ADVANCED_FACE ( 'NONE', ( #702 ), #72493, .T. ) ;
#92623=CONICAL_SURFACE ( 'NONE', #97774, 3.309500000000001663, 0.9599310885968770357 ) ;
#92625=DIRECTION ( 'NONE',  ( -1.000000000000000000, -0.000000000000000000, -0.000000000000000000 ) ) ;
#92649=CARTESIAN_POINT ( 'NONE',  ( 6.222802839579463452, -4.089658325571342345, -6.499999999999999112 ) ) ;
#92650=ORIENTED_EDGE ( 'NONE', *, *, #75812, .F. ) ;
#92652=CARTESIAN_POINT ( 'NONE',  ( 0.000000000000000000, 0.000000000000000000, 0.000000000000000000 ) ) ;
#92660=EDGE_CURVE ( 'NONE', #44939, #48427, #34216, .T. ) ;
#92664=ORIENTED_EDGE ( 'NONE', *, *, #79657, .T. ) ;
#92670=FACE_OUTER_BOUND ( 'NONE', #102049, .T. ) ;
#92674=DIRECTION ( 'NONE',  ( -1.000000000000000000, -0.000000000000000000, -0.000000000000000000 ) ) ;
#92678=DIRECTION ( 'NONE',  ( -1.000000000000000000, -1.224606353822377258E-16, -0.000000000000000000 ) ) ;
#92716=FACE_OUTER_BOUND ( 'NONE', #44695, .T. ) ;
#92729=FACE_OUTER_BOUND ( 'NONE', #16529, .T. ) ;
#92759=CONICAL_SURFACE ( 'NONE', #46271, 4.000000000000001776, 0.9599310885968808105 ) ;
#92763=LINE ( 'NONE', #3231, #88901 ) ;
#92790=FACE_OUTER_BOUND ( 'NONE', #43096, .T. ) ;
#92798=DIRECTION ( 'NONE',  ( 0.000000000000000000, -1.000000000000000000, 0.000000000000000000 ) ) ;
#92841=CARTESIAN_POINT ( 'NONE',  ( 44.83349330513380693, 1.593028355512270567E-15, 0.000000000000000000 ) ) ;
#92845=CARTESIAN_POINT ( 'NONE',  ( 6.333820801331439654, -6.982605850969140882, 0.9057718968901056211 ) ) ;
#92854=DIRECTION ( 'NONE',  ( -1.000000000000000000, -1.224606353822377258E-16, -0.000000000000000000 ) ) ;
#92858=CIRCLE ( 'NONE', #75614, 4.000000000000000888 ) ;
#92866=ORIENTED_EDGE ( 'NONE', *, *, #104539, .F. ) ;
#92875=EDGE_CURVE ( 'NONE', #70548, #77685, #29580, .T. ) ;
#92883=LINE ( 'NONE', #19047, #24229 ) ;
#92892=LINE ( 'NONE', #43285, #52633 ) ;
#92905=AXIS2_PLACEMENT_3D ( 'NONE', #91203, #33491, #65316 ) ;
#92918=DIRECTION ( 'NONE',  ( -1.000000000000000000, -0.000000000000000000, -0.000000000000000000 ) ) ;
#92943=ORIENTED_EDGE ( 'NONE', *, *, #863, .T. ) ;
#92966=ORIENTED_EDGE ( 'NONE', *, *, #3037, .F. ) ;
#92984=ORIENTED_EDGE ( 'NONE', *, *, #61426, .T. ) ;
#92987=CARTESIAN_POINT ( 'NONE',  ( 6.333820801330213968, -6.982605850969823891, -0.9057718968899813872 ) ) ;
#92995=EDGE_LOOP ( 'NONE', ( #91298, #45253, #80015, #63965, #15637, #30590 ) ) ;
#93001=EDGE_CURVE ( 'NONE', #49207, #98370, #83648, .T. ) ;
#93013=CONICAL_SURFACE ( 'NONE', #37917, 3.309500000000001663, 0.9599310885968770357 ) ;
#93028=CONICAL_SURFACE ( 'NONE', #49981, 4.000000000000001776, 0.9599310885968808105 ) ;
#93040=DIRECTION ( 'NONE',  ( 0.000000000000000000, -1.000000000000000000, 0.000000000000000000 ) ) ;
#93060=ADVANCED_FACE ( 'NONE', ( #79288 ), #98440, .T. ) ;
#93106=ORIENTED_EDGE ( 'NONE', *, *, #27307, .T. ) ;
#93109=AXIS2_PLACEMENT_3D ( 'NONE', #101078, #60649, #9936 ) ;
#93122=DIRECTION ( 'NONE',  ( 0.000000000000000000, 0.000000000000000000, 1.000000000000000000 ) ) ;
#93126=EDGE_CURVE ( 'NONE', #44793, #86259, #3683, .T. ) ;
#93136=ORIENTED_EDGE ( 'NONE', *, *, #13466, .F. ) ;
#93140=ADVANCED_FACE ( 'NONE', ( #63659 ), #95012, .T. ) ;
#93146=CARTESIAN_POINT ( 'NONE',  ( 0.000000000000000000, 0.000000000000000000, 0.000000000000000000 ) ) ;
#93174=DIRECTION ( 'NONE',  ( 0.5735764363510466035, -0.8191520442889914655, 1.003171929053524500E-16 ) ) ;
#93178=AXIS2_PLACEMENT_3D ( 'NONE', #19432, #61990, #44192 ) ;
#93179=ORIENTED_EDGE ( 'NONE', *, *, #25665, .T. ) ;
#93183=AXIS2_PLACEMENT_3D ( 'NONE', #70451, #86122, #37048 ) ;
#93193=CARTESIAN_POINT ( 'NONE',  ( 40.59999999999999432, -3.309499999999999886, 4.475777889183790779E-16 ) ) ;
#93195=EDGE_LOOP ( 'NONE', ( #100293, #1818, #57201, #91530, #97906 ) ) ;
#93237=DIRECTION ( 'NONE',  ( -1.000000000000000000, -1.224606353822377258E-16, -0.000000000000000000 ) ) ;
#93266=CIRCLE ( 'NONE', #14016, 4.000000000000000888 ) ;
#93276=B_SPLINE_CURVE_WITH_KNOTS ( 'NONE', 3,
 ( #39693, #55824, #97903, #47752, #105984, #6773, #24059, #56900 ),
 .UNSPECIFIED., .F., .F.,
 ( 4, 2, 2, 4 ),
 ( 0.003797433802554431997, 0.004743183970586230085, 0.005688934138618028172, 0.007580434474681626948 ),
 .UNSPECIFIED. ) ;
#93302=EDGE_CURVE ( 'NONE', #100266, #42587, #53637, .T. ) ;
#93310=DIRECTION ( 'NONE',  ( -1.000000000000000000, -1.224606353822377258E-16, -0.000000000000000000 ) ) ;
#93315=DIRECTION ( 'NONE',  ( -1.000000000000000000, -1.224606353822377258E-16, -0.000000000000000000 ) ) ;
#93339=EDGE_CURVE ( 'NONE', #45306, #2115, #46852, .T. ) ;
#93346=DIRECTION ( 'NONE',  ( 0.000000000000000000, -1.000000000000000000, 0.000000000000000000 ) ) ;
#93359=CARTESIAN_POINT ( 'NONE',  ( 5.691929483231184861, 5.629165124598850767, -3.250000000000000444 ) ) ;
#93387=EDGE_LOOP ( 'NONE', ( #81499, #39153, #8677, #50393, #92966 ) ) ;
#93426=EDGE_CURVE ( 'NONE', #81048, #9279, #74412, .T. ) ;
#93432=LINE ( 'NONE', #58938, #30443 ) ;
#93444=DIRECTION ( 'NONE',  ( -1.000000000000000000, -1.224606353822377258E-16, -0.000000000000000000 ) ) ;
#93446=AXIS2_PLACEMENT_3D ( 'NONE', #71638, #46843, #71121 ) ;
#93463=CIRCLE ( 'NONE', #46941, 4.000000000000000888 ) ;
#93465=DIRECTION ( 'NONE',  ( 0.000000000000000000, 0.000000000000000000, 1.000000000000000000 ) ) ;
#93467=ORIENTED_EDGE ( 'NONE', *, *, #61347, .F. ) ;
#93486=ORIENTED_EDGE ( 'NONE', *, *, #61492, .F. ) ;
#93508=VERTEX_POINT ( 'NONE', #56323 ) ;
#93513=ORIENTED_EDGE ( 'NONE', *, *, #4941, .T. ) ;
#93527=CIRCLE ( 'NONE', #72846, 4.000000000000000888 ) ;
#93546=VERTEX_POINT ( 'NONE', #72006 ) ;
#93583=CARTESIAN_POINT ( 'NONE',  ( 38.09999999999999432, -3.309499999999999886, 0.000000000000000000 ) ) ;
#93617=ORIENTED_EDGE ( 'NONE', *, *, #73094, .T. ) ;
#93644=EDGE_CURVE ( 'NONE', #58764, #33833, #19356, .T. ) ;
#93653=DIRECTION ( 'NONE',  ( 0.000000000000000000, -1.000000000000000000, 0.000000000000000000 ) ) ;
#93686=LINE ( 'NONE', #54787, #53988 ) ;
#93716=ORIENTED_EDGE ( 'NONE', *, *, #34746, .T. ) ;
#93722=ORIENTED_EDGE ( 'NONE', *, *, #78187, .F. ) ;
#93764=ORIENTED_EDGE ( 'NONE', *, *, #27938, .F. ) ;
#93778=CARTESIAN_POINT ( 'NONE',  ( 9.833493305133801599, 1.593028355512270567E-15, 0.000000000000000000 ) ) ;
#93779=ORIENTED_EDGE ( 'NONE', *, *, #68111, .T. ) ;
#93806=EDGE_CURVE ( 'NONE', #82046, #80206, #96844, .T. ) ;
#93808=EDGE_LOOP ( 'NONE', ( #16983, #92224, #39917, #61083 ) ) ;
#93839=FACE_OUTER_BOUND ( 'NONE', #48108, .T. ) ;
#93847=EDGE_CURVE ( 'NONE', #60121, #29715, #45189, .T. ) ;
#93856=DIRECTION ( 'NONE',  ( 0.000000000000000000, -1.000000000000000000, 0.000000000000000000 ) ) ;
#93860=ORIENTED_EDGE ( 'NONE', *, *, #87499, .T. ) ;
#93863=ORIENTED_EDGE ( 'NONE', *, *, #36643, .T. ) ;
#93864=ORIENTED_EDGE ( 'NONE', *, *, #106679, .T. ) ;
#93907=DIRECTION ( 'NONE',  ( 0.000000000000000000, 1.000000000000000000, 0.000000000000000000 ) ) ;
#93931=CARTESIAN_POINT ( 'NONE',  ( 46.08349330513379982, 1.593028355512270567E-15, 0.000000000000000000 ) ) ;
#93935=AXIS2_PLACEMENT_3D ( 'NONE', #80226, #95903, #72146 ) ;
#93938=CIRCLE ( 'NONE', #19913, 4.000000000000000888 ) ;
#93958=( NAMED_UNIT ( * ) SI_UNIT ( $, .STERADIAN. ) SOLID_ANGLE_UNIT ( ) );
#93985=VERTEX_POINT ( 'NONE', #82626 ) ;
#94005=ORIENTED_EDGE ( 'NONE', *, *, #77380, .T. ) ;
#94032=DIRECTION ( 'NONE',  ( 0.000000000000000000, -1.000000000000000000, 0.000000000000000000 ) ) ;
#94046=AXIS2_PLACEMENT_3D ( 'NONE', #32077, #71984, #63389 ) ;
#94084=AXIS2_PLACEMENT_3D ( 'NONE', #59169, #53717, #94736 ) ;
#94087=CIRCLE ( 'NONE', #21742, 4.000000000000000888 ) ;
#94111=VERTEX_POINT ( 'NONE', #91268 ) ;
#94136=AXIS2_PLACEMENT_3D ( 'NONE', #5602, #55200, #63332 ) ;
#94154=ORIENTED_EDGE ( 'NONE', *, *, #63635, .F. ) ;
#94172=CARTESIAN_POINT ( 'NONE',  ( 6.289692432696588398, 5.239086202714920759, 4.583616368337912306 ) ) ;
#94185=ORIENTED_EDGE ( 'NONE', *, *, #64924, .F. ) ;
#94190=CARTESIAN_POINT ( 'NONE',  ( 0.000000000000000000, 4.898587196589412829E-16, -4.000000000000000000 ) ) ;
#94201=AXIS2_PLACEMENT_3D ( 'NONE', #49822, #8299, #81637 ) ;
#94216=EDGE_CURVE ( 'NONE', #64733, #95564, #71031, .T. ) ;
#94224=CIRCLE ( 'NONE', #45943, 4.000000000000001776 ) ;
#94239=EDGE_CURVE ( 'NONE', #54290, #54096, #11915, .T. ) ;
#94257=ORIENTED_EDGE ( 'NONE', *, *, #41675, .F. ) ;
#94276=ORIENTED_EDGE ( 'NONE', *, *, #28804, .T. ) ;
#94287=EDGE_CURVE ( 'NONE', #72439, #9941, #64203, .T. ) ;
#94295=CARTESIAN_POINT ( 'NONE',  ( 30.59999999999999787, -3.309499999999999886, 0.000000000000000000 ) ) ;
#94298=CARTESIAN_POINT ( 'NONE',  ( 5.996380728650903436, 2.731133088746460658, 6.499999999999999112 ) ) ;
#94302=ORIENTED_EDGE ( 'NONE', *, *, #71134, .F. ) ;
#94311=FACE_OUTER_BOUND ( 'NONE', #45397, .T. ) ;
#94319=CONICAL_SURFACE ( 'NONE', #70128, 3.309500000000001663, 0.9599310885968770357 ) ;
#94329=CIRCLE ( 'NONE', #11681, 4.000000000000001776 ) ;
#94391=DIRECTION ( 'NONE',  ( 1.000000000000000000, 1.224606353822377258E-16, 0.000000000000000000 ) ) ;
#94431=CARTESIAN_POINT ( 'NONE',  ( 39.83349330513380693, -7.703719777548943412E-31, 4.000000000000001776 ) ) ;
#94436=DIRECTION ( 'NONE',  ( -1.000000000000000000, -1.224606353822377258E-16, -0.000000000000000000 ) ) ;
#94457=DIRECTION ( 'NONE',  ( 0.000000000000000000, -1.000000000000000000, 0.000000000000000000 ) ) ;
#94499=PRESENTATION_STYLE_ASSIGNMENT (( #102030 ) ) ;
#94505=CARTESIAN_POINT ( 'NONE',  ( 0.000000000000000000, 0.000000000000000000, 0.000000000000000000 ) ) ;
#94510=DIRECTION ( 'NONE',  ( -0.5735764363510497121, 0.8191520442889892450, 1.003171929053521665E-16 ) ) ;
#94516=FACE_OUTER_BOUND ( 'NONE', #42506, .T. ) ;
#94542=CARTESIAN_POINT ( 'NONE',  ( 31.36650669486618881, 1.474610560812782335E-15, 0.000000000000000000 ) ) ;
#94557=AXIS2_PLACEMENT_3D ( 'NONE', #99111, #106138, #24735 ) ;
#94568=DIRECTION ( 'NONE',  ( -1.000000000000000000, -1.224606353822377258E-16, -0.000000000000000000 ) ) ;
#94589=VECTOR ( 'NONE', #90246, 1000.000000000000000 ) ;
#94594=DIRECTION ( 'NONE',  ( 0.000000000000000000, -1.000000000000000000, 0.000000000000000000 ) ) ;
#94595=CARTESIAN_POINT ( 'NONE',  ( 0.000000000000000000, 0.000000000000000000, 0.000000000000000000 ) ) ;
#94609=DIRECTION ( 'NONE',  ( -1.000000000000000000, -1.224606353822377258E-16, -0.000000000000000000 ) ) ;
#94647=ORIENTED_EDGE ( 'NONE', *, *, #93339, .T. ) ;
#94667=CIRCLE ( 'NONE', #48123, 4.000000000000000888 ) ;
#94690=CARTESIAN_POINT ( 'NONE',  ( 27.61650669486618881, 1.474610560812782335E-15, 0.000000000000000000 ) ) ;
#94728=DIRECTION ( 'NONE',  ( -1.000000000000000000, -1.224606353822377258E-16, -0.000000000000000000 ) ) ;
#94736=DIRECTION ( 'NONE',  ( 0.000000000000000000, -1.000000000000000000, 0.000000000000000000 ) ) ;
#94765=CIRCLE ( 'NONE', #82653, 3.309500000000001663 ) ;
#94775=CARTESIAN_POINT ( 'NONE',  ( 8.099999999999999645, 7.505553499465140277, 0.000000000000000000 ) ) ;
#94813=VECTOR ( 'NONE', #38621, 1000.000000000000000 ) ;
#94815=ORIENTED_EDGE ( 'NONE', *, *, #57974, .F. ) ;
#94826=CARTESIAN_POINT ( 'NONE',  ( 6.162888688655344005, 3.752776749732561257, -6.499999999999999112 ) ) ;
#94837=FACE_OUTER_BOUND ( 'NONE', #45952, .T. ) ;
#94849=ORIENTED_EDGE ( 'NONE', *, *, #66504, .F. ) ;
#94852=EDGE_LOOP ( 'NONE', ( #96743, #43203, #20628, #34739 ) ) ;
#94854=LINE ( 'NONE', #104509, #9429 ) ;
#94855=CIRCLE ( 'NONE', #36294, 4.000000000000000888 ) ;
#94857=EDGE_CURVE ( 'NONE', #27527, #54223, #52239, .T. ) ;
#94916=EDGE_CURVE ( 'NONE', #77294, #35660, #75476, .T. ) ;
#94925=CARTESIAN_POINT ( 'NONE',  ( 8.866506694866188809, 1.474610560812782335E-15, 0.000000000000000000 ) ) ;
#94957=EDGE_CURVE ( 'NONE', #87415, #48427, #98722, .T. ) ;
#94974=CARTESIAN_POINT ( 'NONE',  ( 42.33349330513380693, 1.593028355512270567E-15, 0.000000000000000000 ) ) ;
#94976=VECTOR ( 'NONE', #55299, 1000.000000000000000 ) ;
#95000=DIRECTION ( 'NONE',  ( -1.000000000000000000, -1.224606353822377258E-16, -0.000000000000000000 ) ) ;
#95004=VECTOR ( 'NONE', #53662, 1000.000000000000000 ) ;
#95010=CARTESIAN_POINT ( 'NONE',  ( 44.83349330513380693, -4.000000000000000888, 4.898587196589416773E-16 ) ) ;
#95012=CONICAL_SURFACE ( 'NONE', #41543, 3.309500000000001663, 0.9599310885968770357 ) ;
#95016=FACE_OUTER_BOUND ( 'NONE', #34455, .T. ) ;
#95021=CARTESIAN_POINT ( 'NONE',  ( 46.08349330513379982, 4.898587196589405926E-16, -4.000000000000001776 ) ) ;
#95032=DIRECTION ( 'NONE',  ( 0.000000000000000000, -1.000000000000000000, 0.000000000000000000 ) ) ;
#95050=ORIENTED_EDGE ( 'NONE', *, *, #56927, .F. ) ;
#95103=EDGE_LOOP ( 'NONE', ( #88488, #100411, #51233, #79823, #94302 ) ) ;
#95108=ORIENTED_EDGE ( 'NONE', *, *, #24161, .T. ) ;
#95124=CARTESIAN_POINT ( 'NONE',  ( 0.5805565836007605673, -3.752776749732561257, 6.500000000000000000 ) ) ;
#95134=CONICAL_SURFACE ( 'NONE', #48580, 6.500000000000000000, 1.047197551196600296 ) ;
#95150=VECTOR ( 'NONE', #33331, 1000.000000000000000 ) ;
#95161=DIRECTION ( 'NONE',  ( 0.000000000000000000, 0.000000000000000000, 1.000000000000000000 ) ) ;
#95188=CONICAL_SURFACE ( 'NONE', #88256, 4.000000000000001776, 0.9599310885968808105 ) ;
#95242=EDGE_CURVE ( 'NONE', #74067, #103934, #35037, .T. ) ;
#95248=EDGE_CURVE ( 'NONE', #24986, #77591, #36742, .T. ) ;
#95250=VERTEX_POINT ( 'NONE', #50013 ) ;
#95255=DIRECTION ( 'NONE',  ( 0.5735764363510462704, 0.8191520442889915765, 0.000000000000000000 ) ) ;
#95264=ORIENTED_EDGE ( 'NONE', *, *, #32011, .T. ) ;
#95283=DIRECTION ( 'NONE',  ( -1.000000000000000000, -0.000000000000000000, -0.000000000000000000 ) ) ;
#95330=ORIENTED_EDGE ( 'NONE', *, *, #22675, .T. ) ;
#95335=EDGE_CURVE ( 'NONE', #70548, #77591, #55696, .T. ) ;
#95346=DIRECTION ( 'NONE',  ( 0.000000000000000000, -1.000000000000000000, 0.000000000000000000 ) ) ;
#95357=CARTESIAN_POINT ( 'NONE',  ( 43.58349330513380693, 1.593028355512270567E-15, 0.000000000000000000 ) ) ;
#95370=DIRECTION ( 'NONE',  ( -0.5735764363510494901, -0.8191520442889894671, 0.000000000000000000 ) ) ;
#95379=CARTESIAN_POINT ( 'NONE',  ( 6.222742520105469133, -3.584500230190538428, 6.791463481567636684 ) ) ;
#95434=ORIENTED_EDGE ( 'NONE', *, *, #84280, .F. ) ;
#95450=CARTESIAN_POINT ( 'NONE',  ( 29.34999999999999787, 1.533819458162526451E-15, 0.000000000000000000 ) ) ;
#95456=CARTESIAN_POINT ( 'NONE',  ( 42.33349330513380693, -4.000000000000000888, 4.898587196589416773E-16 ) ) ;
#95506=AXIS2_PLACEMENT_3D ( 'NONE', #40349, #51625, #34951 ) ;
#95510=ORIENTED_EDGE ( 'NONE', *, *, #4977, .F. ) ;
#95516=ORIENTED_EDGE ( 'NONE', *, *, #85584, .T. ) ;
#95557=DIRECTION ( 'NONE',  ( -1.000000000000000000, -0.000000000000000000, -0.000000000000000000 ) ) ;
#95558=DIRECTION ( 'NONE',  ( 0.000000000000000000, -1.000000000000000000, 0.000000000000000000 ) ) ;
#95562=CARTESIAN_POINT ( 'NONE',  ( 6.683837171061802529, 3.955946848495962787, 6.851900933636986935 ) ) ;
#95564=VERTEX_POINT ( 'NONE', #95021 ) ;
#95578=EDGE_CURVE ( 'NONE', #57692, #64733, #44330, .T. ) ;
#95611=CARTESIAN_POINT ( 'NONE',  ( 20.11650669486618881, 1.474610560812782335E-15, 0.000000000000000000 ) ) ;
#95617=CIRCLE ( 'NONE', #33642, 4.000000000000001776 ) ;
#95625=EDGE_CURVE ( 'NONE', #30642, #44793, #88519, .T. ) ;
#95647=DIRECTION ( 'NONE',  ( -1.000000000000000000, -0.000000000000000000, -0.000000000000000000 ) ) ;
#95657=DIRECTION ( 'NONE',  ( -1.000000000000000000, -1.224606353822377258E-16, -0.000000000000000000 ) ) ;
#95659=EDGE_LOOP ( 'NONE', ( #8475, #5235, #45050, #14485, #17923, #80115 ) ) ;
#95664=ORIENTED_EDGE ( 'NONE', *, *, #45147, .T. ) ;
#95698=EDGE_CURVE ( 'NONE', #25329, #1155, #100513, .T. ) ;
#95705=AXIS2_PLACEMENT_3D ( 'NONE', #15843, #48725, #81614 ) ;
#95736=DIRECTION ( 'NONE',  ( 1.000000000000000000, 0.000000000000000000, -0.000000000000000000 ) ) ;
#95848=CARTESIAN_POINT ( 'NONE',  ( 33.58349330513379982, -4.000000000000000888, 4.898587196589416773E-16 ) ) ;
#95855=VECTOR ( 'NONE', #57588, 1000.000000000000000 ) ;
#95856=VECTOR ( 'NONE', #60062, 1000.000000000000000 ) ;
#95887=DIRECTION ( 'NONE',  ( -1.000000000000000000, -1.224606353822377258E-16, -0.000000000000000000 ) ) ;
#95894=CARTESIAN_POINT ( 'NONE',  ( 7.500000000000001776, 0.000000000000000000, 0.000000000000000000 ) ) ;
#95901=ORIENTED_EDGE ( 'NONE', *, *, #63155, .F. ) ;
#95903=DIRECTION ( 'NONE',  ( 1.000000000000000000, 1.224606353822377258E-16, 0.000000000000000000 ) ) ;
#95917=CARTESIAN_POINT ( 'NONE',  ( 21.36650669486618881, 4.898587196589411843E-16, -4.000000000000000888 ) ) ;
#95932=CONICAL_SURFACE ( 'NONE', #11436, 4.000000000000001776, 0.9599310885968808105 ) ;
#95978=ORIENTED_EDGE ( 'NONE', *, *, #65392, .T. ) ;
#95990=ORIENTED_EDGE ( 'NONE', *, *, #11178, .T. ) ;
#95995=ORIENTED_EDGE ( 'NONE', *, *, #62542, .T. ) ;
#96002=AXIS2_PLACEMENT_3D ( 'NONE', #55619, #65336, #104727 ) ;
#96025=EDGE_CURVE ( 'NONE', #98395, #59135, #53854, .T. ) ;
#96035=CONICAL_SURFACE ( 'NONE', #3017, 4.000000000000001776, 0.9599310885968808105 ) ;
#96047=AXIS2_PLACEMENT_3D ( 'NONE', #47611, #72431, #57823 ) ;
#96063=VERTEX_POINT ( 'NONE', #63041 ) ;
#96088=CARTESIAN_POINT ( 'NONE',  ( 32.33349330513379982, 1.593028355512270567E-15, 0.000000000000000000 ) ) ;
#96098=ADVANCED_FACE ( 'NONE', ( #62001 ), #373, .T. ) ;
#96109=CONICAL_SURFACE ( 'NONE', #8327, 4.000000000000001776, 0.9599310885968808105 ) ;
#96135=CONICAL_SURFACE ( 'NONE', #66878, 4.000000000000001776, 0.9599310885968808105 ) ;
#96168=ORIENTED_EDGE ( 'NONE', *, *, #82254, .F. ) ;
#96172=CARTESIAN_POINT ( 'NONE',  ( 6.575918192882433289, -3.850883087735915922, -6.669925161966309801 ) ) ;
#96200=DIRECTION ( 'NONE',  ( -1.000000000000000000, -1.224606353822377258E-16, -0.000000000000000000 ) ) ;
#96214=CARTESIAN_POINT ( 'NONE',  ( 41.85000000000000142, 3.309500000000003439, 0.000000000000000000 ) ) ;
#96230=ORIENTED_EDGE ( 'NONE', *, *, #65217, .T. ) ;
#96265=AXIS2_PLACEMENT_3D ( 'NONE', #55459, #105618, #15008 ) ;
#96267=DIRECTION ( 'NONE',  ( 0.000000000000000000, -1.000000000000000000, 0.000000000000000000 ) ) ;
#96275=ORIENTED_EDGE ( 'NONE', *, *, #79657, .F. ) ;
#96283=CARTESIAN_POINT ( 'NONE',  ( 0.5805565836007643421, -3.752776749732575468, -6.499999999999999112 ) ) ;
#96314=CARTESIAN_POINT ( 'NONE',  ( 28.86650669486618881, 1.474610560812782335E-15, 0.000000000000000000 ) ) ;
#96317=DIRECTION ( 'NONE',  ( -1.000000000000000000, -0.000000000000000000, -0.000000000000000000 ) ) ;
#96337=ADVANCED_FACE ( 'NONE', ( #22355 ), #53621, .T. ) ;
#96405=DIRECTION ( 'NONE',  ( 0.000000000000000000, -1.000000000000000000, 0.000000000000000000 ) ) ;
#96465=FACE_OUTER_BOUND ( 'NONE', #70375, .T. ) ;
#96491=CARTESIAN_POINT ( 'NONE',  ( 40.59999999999999432, 3.309500000000003439, 0.000000000000000000 ) ) ;
#96504=ORIENTED_EDGE ( 'NONE', *, *, #15815, .F. ) ;
#96526=DIRECTION ( 'NONE',  ( -1.000000000000000000, -0.000000000000000000, -0.000000000000000000 ) ) ;
#96530=CARTESIAN_POINT ( 'NONE',  ( 6.162888688655344005, 3.752776749732565253, 6.499999999999997335 ) ) ;
#96547=CARTESIAN_POINT ( 'NONE',  ( 31.84999999999999787, 1.533819458162526451E-15, 0.000000000000000000 ) ) ;
#96558=CIRCLE ( 'NONE', #74128, 4.000000000000000888 ) ;
#96565=ORIENTED_EDGE ( 'NONE', *, *, #26899, .F. ) ;
#96577=CIRCLE ( 'NONE', #10392, 3.309500000000001663 ) ;
#96579=ORIENTED_EDGE ( 'NONE', *, *, #31336, .T. ) ;
#96601=ORIENTED_EDGE ( 'NONE', *, *, #55340, .F. ) ;
#96613=CIRCLE ( 'NONE', #72499, 4.000000000000000888 ) ;
#96625=DIRECTION ( 'NONE',  ( -0.5735764363510497121, 0.8191520442889892450, 1.003171929053521665E-16 ) ) ;
#96627=ORIENTED_EDGE ( 'NONE', *, *, #55340, .T. ) ;
#96645=DIRECTION ( 'NONE',  ( -1.000000000000000000, -1.224606353822377258E-16, -0.000000000000000000 ) ) ;
#96653=AXIS2_PLACEMENT_3D ( 'NONE', #68352, #41403, #99638 ) ;
#96668=DIRECTION ( 'NONE',  ( 0.000000000000000000, -1.000000000000000000, 0.000000000000000000 ) ) ;
#96701=FACE_OUTER_BOUND ( 'NONE', #30699, .T. ) ;
#96715=EDGE_CURVE ( 'NONE', #100006, #77685, #102320, .T. ) ;
#96739=CIRCLE ( 'NONE', #50215, 3.309500000000001663 ) ;
#96743=ORIENTED_EDGE ( 'NONE', *, *, #49034, .T. ) ;
#96789=FACE_OUTER_BOUND ( 'NONE', #66431, .T. ) ;
#96799=ORIENTED_EDGE ( 'NONE', *, *, #83544, .T. ) ;
#96813=DIRECTION ( 'NONE',  ( -1.000000000000000000, -0.000000000000000000, 0.000000000000000000 ) ) ;
#96829=ORIENTED_EDGE ( 'NONE', *, *, #41539, .F. ) ;
#96833=CARTESIAN_POINT ( 'NONE',  ( 8.099999999999999645, 7.505553499465140277, 3.755786496842903002E-16 ) ) ;
#96836=ORIENTED_EDGE ( 'NONE', *, *, #48836, .T. ) ;
#96840=DIRECTION ( 'NONE',  ( -1.000000000000000000, -0.000000000000000000, -0.000000000000000000 ) ) ;
#96844=CIRCLE ( 'NONE', #17619, 3.309500000000001663 ) ;
#96856=CARTESIAN_POINT ( 'NONE',  ( 8.099999999999999645, 0.000000000000000000, 0.000000000000000000 ) ) ;
#96902=EDGE_CURVE ( 'NONE', #21459, #101293, #59102, .T. ) ;
#96904=DIRECTION ( 'NONE',  ( -1.000000000000000000, -1.224606353822377258E-16, -0.000000000000000000 ) ) ;
#96907=EDGE_CURVE ( 'NONE', #27202, #77668, #79794, .T. ) ;
#96927=DIRECTION ( 'NONE',  ( 0.000000000000000000, 1.000000000000000000, 0.000000000000000000 ) ) ;
#96940=DIRECTION ( 'NONE',  ( -1.000000000000000000, -1.224606353822377258E-16, -0.000000000000000000 ) ) ;
#96965=DIRECTION ( 'NONE',  ( 0.5735764363510466035, -0.8191520442889914655, 1.003171929053524500E-16 ) ) ;
#96973=EDGE_CURVE ( 'NONE', #86927, #70548, #93527, .T. ) ;
#96992=ORIENTED_EDGE ( 'NONE', *, *, #30920, .F. ) ;
#97061=FACE_OUTER_BOUND ( 'NONE', #7889, .T. ) ;
#97090=EDGE_CURVE ( 'NONE', #77591, #93546, #67800, .T. ) ;
#97094=EDGE_CURVE ( 'NONE', #74232, #49696, #78005, .T. ) ;
#97119=VECTOR ( 'NONE', #69409, 1000.000000000000000 ) ;
#97140=FACE_OUTER_BOUND ( 'NONE', #10006, .T. ) ;
#97158=CARTESIAN_POINT ( 'NONE',  ( 17.33349330513380337, 4.000000000000003553, 0.000000000000000000 ) ) ;
#97159=DIRECTION ( 'NONE',  ( -1.000000000000000000, -1.224606353822377258E-16, -0.000000000000000000 ) ) ;
#97164=EDGE_CURVE ( 'NONE', #22876, #68944, #48826, .T. ) ;
#97168=ORIENTED_EDGE ( 'NONE', *, *, #93847, .F. ) ;
#97175=ORIENTED_EDGE ( 'NONE', *, *, #80694, .F. ) ;
#97178=VERTEX_POINT ( 'NONE', #66053 ) ;
#97181=EDGE_CURVE ( 'NONE', #48447, #31692, #72928, .T. ) ;
#97182=DIRECTION ( 'NONE',  ( -1.000000000000000000, -1.224606353822377258E-16, -0.000000000000000000 ) ) ;
#97214=LINE ( 'NONE', #21781, #97369 ) ;
#97236=DIRECTION ( 'NONE',  ( 0.000000000000000000, 1.000000000000000000, 0.000000000000000000 ) ) ;
#97237=EDGE_LOOP ( 'NONE', ( #79712, #36826, #95510, #5929, #72269 ) ) ;
#97240=ORIENTED_EDGE ( 'NONE', *, *, #97418, .F. ) ;
#97270=ADVANCED_FACE ( 'NONE', ( #28839 ), #57451, .T. ) ;
#97287=EDGE_CURVE ( 'NONE', #61806, #75040, #20755, .T. ) ;
#97306=AXIS2_PLACEMENT_3D ( 'NONE', #79117, #79641, #47790 ) ;
#97312=EDGE_CURVE ( 'NONE', #35387, #40315, #12586, .T. ) ;
#97343=EDGE_CURVE ( 'NONE', #2814, #21525, #33389, .T. ) ;
#97344=ORIENTED_EDGE ( 'NONE', *, *, #3115, .F. ) ;
#97352=SURFACE_STYLE_FILL_AREA ( #89286 ) ;
#97353=CARTESIAN_POINT ( 'NONE',  ( 12.61650669486618881, 1.474610560812782335E-15, 0.000000000000000000 ) ) ;
#97358=CARTESIAN_POINT ( 'NONE',  ( 29.83349330513380337, 1.593028355512270567E-15, 0.000000000000000000 ) ) ;
#97366=DIRECTION ( 'NONE',  ( 0.000000000000000000, 1.000000000000000000, 0.000000000000000000 ) ) ;
#97368=EDGE_CURVE ( 'NONE', #78785, #26898, #37982, .T. ) ;
#97369=VECTOR ( 'NONE', #87557, 1000.000000000000000 ) ;
#97383=DIRECTION ( 'NONE',  ( 0.000000000000000000, 0.000000000000000000, -1.000000000000000000 ) ) ;
#97418=EDGE_CURVE ( 'NONE', #92046, #673, #44448, .T. ) ;
#97447=CIRCLE ( 'NONE', #7910, 4.000000000000000888 ) ;
#97451=CARTESIAN_POINT ( 'NONE',  ( 0.4033376246892503292, 7.198601258566900363, -0.5316568767328675449 ) ) ;
#97499=ORIENTED_EDGE ( 'NONE', *, *, #98009, .T. ) ;
#97506=CIRCLE ( 'NONE', #51011, 4.000000000000000888 ) ;
#97525=CARTESIAN_POINT ( 'NONE',  ( 32.33349330513379982, -7.703719777548943412E-31, 4.000000000000001776 ) ) ;
#97548=EDGE_LOOP ( 'NONE', ( #30786, #105341, #100874, #79064, #35034 ) ) ;
#97562=DIRECTION ( 'NONE',  ( 0.000000000000000000, -1.000000000000000000, 0.000000000000000000 ) ) ;
#97567=VERTEX_POINT ( 'NONE', #41919 ) ;
#97588=CONICAL_SURFACE ( 'NONE', #56236, 3.309500000000001663, 0.9599310885968770357 ) ;
#97622=CARTESIAN_POINT ( 'NONE',  ( 38.58349330513380693, -4.000000000000000000, 4.898587196589415787E-16 ) ) ;
#97632=CARTESIAN_POINT ( 'NONE',  ( 6.289692432696784685, 1.244805614057421469E-13, 6.828989928337167115 ) ) ;
#97649=CIRCLE ( 'NONE', #73481, 4.000000000000000888 ) ;
#97660=CARTESIAN_POINT ( 'NONE',  ( 28.86650669486618881, 1.474610560812782335E-15, 0.000000000000000000 ) ) ;
#97687=CARTESIAN_POINT ( 'NONE',  ( 41.85000000000000142, 1.533819458162526451E-15, 0.000000000000000000 ) ) ;
#97695=ORIENTED_EDGE ( 'NONE', *, *, #15723, .F. ) ;
#97723=FACE_OUTER_BOUND ( 'NONE', #13128, .T. ) ;
#97756=AXIS2_PLACEMENT_3D ( 'NONE', #15041, #38300, #31273 ) ;
#97774=AXIS2_PLACEMENT_3D ( 'NONE', #103643, #29792, #55072 ) ;
#97778=DIRECTION ( 'NONE',  ( 0.000000000000000000, -1.000000000000000000, 0.000000000000000000 ) ) ;
#97786=EDGE_CURVE ( 'NONE', #79431, #45302, #47224, .T. ) ;
#97819=DIRECTION ( 'NONE',  ( 0.000000000000000000, -1.000000000000000000, 0.000000000000000000 ) ) ;
#97825=DIRECTION ( 'NONE',  ( 0.000000000000000000, -1.000000000000000000, 0.000000000000000000 ) ) ;
#97831=EDGE_CURVE ( 'NONE', #44258, #59773, #4135, .T. ) ;
#97841=AXIS2_PLACEMENT_3D ( 'NONE', #37601, #59722, #70463 ) ;
#97844=EDGE_LOOP ( 'NONE', ( #82555, #66404, #52664, #76253 ) ) ;
#97850=CARTESIAN_POINT ( 'NONE',  ( 6.463178677061754307, -2.643201791673488010, -6.839998497243178655 ) ) ;
#97869=LINE ( 'NONE', #31062, #20856 ) ;
#97896=DIRECTION ( 'NONE',  ( -1.000000000000000000, -1.224606353822377258E-16, -0.000000000000000000 ) ) ;
#97903=CARTESIAN_POINT ( 'NONE',  ( 0.01372220897662188889, -5.948365447239590154, -2.697128823393880825 ) ) ;
#97906=ORIENTED_EDGE ( 'NONE', *, *, #334, .F. ) ;
#97923=ORIENTED_EDGE ( 'NONE', *, *, #29060, .T. ) ;
#97949=CARTESIAN_POINT ( 'NONE',  ( 0.000000000000000000, -5.629165124598848990, -3.250000000000003553 ) ) ;
#97972=ORIENTED_EDGE ( 'NONE', *, *, #25289, .F. ) ;
#97998=DIRECTION ( 'NONE',  ( 0.000000000000000000, -1.000000000000000000, 0.000000000000000000 ) ) ;
#98009=EDGE_CURVE ( 'NONE', #76835, #22614, #93276, .T. ) ;
#98011=AXIS2_PLACEMENT_3D ( 'NONE', #3662, #77544, #5251 ) ;
#98068=AXIS2_PLACEMENT_3D ( 'NONE', #53059, #100529, #36905 ) ;
#98087=CARTESIAN_POINT ( 'NONE',  ( 33.86650669486618881, 1.474610560812782335E-15, 0.000000000000000000 ) ) ;
#98094=ORIENTED_EDGE ( 'NONE', *, *, #93302, .F. ) ;
#98101=CARTESIAN_POINT ( 'NONE',  ( 37.33349330513379982, 4.000000000000003553, 0.000000000000000000 ) ) ;
#98106=CONICAL_SURFACE ( 'NONE', #86143, 4.000000000000001776, 0.9599310885968808105 ) ;
#98140=DIRECTION ( 'NONE',  ( -1.000000000000000000, -1.224606353822377258E-16, -0.000000000000000000 ) ) ;
#98154=FACE_OUTER_BOUND ( 'NONE', #67343, .T. ) ;
#98167=EDGE_CURVE ( 'NONE', #40315, #12958, #104116, .T. ) ;
#98169=ORIENTED_EDGE ( 'NONE', *, *, #66298, .F. ) ;
#98224=EDGE_CURVE ( 'NONE', #25084, #22876, #36806, .T. ) ;
#98240=CIRCLE ( 'NONE', #5252, 3.309500000000001663 ) ;
#98270=CONICAL_SURFACE ( 'NONE', #67331, 3.309500000000001663, 0.9599310885968770357 ) ;
#98279=CARTESIAN_POINT ( 'NONE',  ( 0.000000000000000000, 0.000000000000000000, 0.000000000000000000 ) ) ;
#98318=ORIENTED_EDGE ( 'NONE', *, *, #96973, .F. ) ;
#98323=DIRECTION ( 'NONE',  ( 0.000000000000000000, 1.000000000000000000, 0.000000000000000000 ) ) ;
#98332=ORIENTED_EDGE ( 'NONE', *, *, #26697, .F. ) ;
#98339=VECTOR ( 'NONE', #65718, 1000.000000000000000 ) ;
#98342=CONICAL_SURFACE ( 'NONE', #51836, 3.309499999999999886, 0.7853981633974407295 ) ;
#98344=CONICAL_SURFACE ( 'NONE', #46610, 4.000000000000001776, 0.9599310885968808105 ) ;
#98370=VERTEX_POINT ( 'NONE', #57177 ) ;
#98395=VERTEX_POINT ( 'NONE', #80394 ) ;
#98404=CARTESIAN_POINT ( 'NONE',  ( 32.33349330513379982, 4.000000000000003553, 0.000000000000000000 ) ) ;
#98423=VERTEX_POINT ( 'NONE', #104680 ) ;
#98440=CONICAL_SURFACE ( 'NONE', #89831, 3.309500000000001663, 0.9599310885968770357 ) ;
#98442=CARTESIAN_POINT ( 'NONE',  ( 12.33349330513380337, -7.703719777548943412E-31, 4.000000000000001776 ) ) ;
#98444=LINE ( 'NONE', #101110, #29636 ) ;
#98458=EDGE_CURVE ( 'NONE', #52601, #14924, #5949, .T. ) ;
#98475=ADVANCED_FACE ( 'NONE', ( #39439 ), #81697, .T. ) ;
#98485=CARTESIAN_POINT ( 'NONE',  ( 42.61650669486618881, -3.999999999999998224, 0.000000000000000000 ) ) ;
#98522=CARTESIAN_POINT ( 'NONE',  ( 28.58349330513380337, 1.593028355512270567E-15, 0.000000000000000000 ) ) ;
#98525=ORIENTED_EDGE ( 'NONE', *, *, #83544, .F. ) ;
#98543=ORIENTED_EDGE ( 'NONE', *, *, #28814, .T. ) ;
#98558=CARTESIAN_POINT ( 'NONE',  ( 6.281178480976150169, 7.505553499465138501, 5.007024290797826235E-17 ) ) ;
#98571=ORIENTED_EDGE ( 'NONE', *, *, #81615, .T. ) ;
#98575=ORIENTED_EDGE ( 'NONE', *, *, #103217, .F. ) ;
#98577=CARTESIAN_POINT ( 'NONE',  ( 38.86650669486618881, -3.999999999999998224, 0.000000000000000000 ) ) ;
#98596=ORIENTED_EDGE ( 'NONE', *, *, #38606, .F. ) ;
#98605=EDGE_LOOP ( 'NONE', ( #4258, #8227, #31183, #26948, #68564 ) ) ;
#98610=CARTESIAN_POINT ( 'NONE',  ( 0.1061556211655344389, -4.836380039389415408, 4.623144047065558482 ) ) ;
#98611=LINE ( 'NONE', #62432, #81585 ) ;
#98617=ORIENTED_EDGE ( 'NONE', *, *, #102815, .F. ) ;
#98618=ORIENTED_EDGE ( 'NONE', *, *, #104539, .T. ) ;
#98625=DIRECTION ( 'NONE',  ( 0.000000000000000000, -1.000000000000000000, 0.000000000000000000 ) ) ;
#98645=DIRECTION ( 'NONE',  ( -1.000000000000000000, -1.224606353822377258E-16, -0.000000000000000000 ) ) ;
#98659=DIRECTION ( 'NONE',  ( 0.000000000000000000, -1.000000000000000000, 0.000000000000000000 ) ) ;
#98660=ORIENTED_EDGE ( 'NONE', *, *, #95698, .F. ) ;
#98685=AXIS2_PLACEMENT_3D ( 'NONE', #44144, #59805, #10686 ) ;
#98686=EDGE_LOOP ( 'NONE', ( #8300, #61672, #53934, #27262, #57888 ) ) ;
#98692=DIRECTION ( 'NONE',  ( 1.000000000000000000, 1.224606353822377258E-16, 0.000000000000000000 ) ) ;
#98693=CARTESIAN_POINT ( 'NONE',  ( 38.09999999999999432, 1.533819458162526451E-15, 0.000000000000000000 ) ) ;
#98697=CARTESIAN_POINT ( 'NONE',  ( 0.000000000000000000, 0.000000000000000000, 0.000000000000000000 ) ) ;
#98716=CARTESIAN_POINT ( 'NONE',  ( 41.85000000000000142, 1.533819458162526451E-15, 0.000000000000000000 ) ) ;
#98722=CIRCLE ( 'NONE', #79802, 4.000000000000000888 ) ;
#98741=VERTEX_POINT ( 'NONE', #12876 ) ;
#98743=EDGE_CURVE ( 'NONE', #89958, #44258, #92107, .T. ) ;
#98754=ORIENTED_EDGE ( 'NONE', *, *, #34710, .T. ) ;
#98755=DIRECTION ( 'NONE',  ( 0.000000000000000000, -1.000000000000000000, 0.000000000000000000 ) ) ;
#98763=ORIENTED_EDGE ( 'NONE', *, *, #104963, .F. ) ;
#98778=DIRECTION ( 'NONE',  ( -1.000000000000000000, -1.224606353822377258E-16, -0.000000000000000000 ) ) ;
#98791=CARTESIAN_POINT ( 'NONE',  ( 14.83349330513380337, 1.593028355512270567E-15, 0.000000000000000000 ) ) ;
#98796=DIRECTION ( 'NONE',  ( 0.000000000000000000, -1.000000000000000000, 0.000000000000000000 ) ) ;
#98826=DIRECTION ( 'NONE',  ( -1.000000000000000000, 0.000000000000000000, -0.000000000000000000 ) ) ;
#98829=EDGE_CURVE ( 'NONE', #40330, #82202, #65021, .T. ) ;
#98854=CARTESIAN_POINT ( 'NONE',  ( 26.08349330513380337, 1.593028355512270567E-15, 0.000000000000000000 ) ) ;
#98860=CIRCLE ( 'NONE', #5865, 3.309500000000001663 ) ;
#98865=DIRECTION ( 'NONE',  ( 0.000000000000000000, -1.000000000000000000, 0.000000000000000000 ) ) ;
#98868=CONICAL_SURFACE ( 'NONE', #81617, 4.000000000000001776, 0.9599310885968808105 ) ;
#98874=EDGE_CURVE ( 'NONE', #58778, #87270, #105885, .T. ) ;
#98906=ORIENTED_EDGE ( 'NONE', *, *, #50250, .T. ) ;
#98913=CIRCLE ( 'NONE', #5913, 4.000000000000001776 ) ;
#98953=CIRCLE ( 'NONE', #88588, 4.000000000000000888 ) ;
#98957=EDGE_CURVE ( 'NONE', #54096, #60365, #74847, .T. ) ;
#99001=EDGE_CURVE ( 'NONE', #16154, #103256, #42140, .T. ) ;
#99007=DIRECTION ( 'NONE',  ( -1.000000000000000000, -0.000000000000000000, -0.000000000000000000 ) ) ;
#99016=EDGE_CURVE ( 'NONE', #43396, #45302, #35351, .T. ) ;
#99040=CARTESIAN_POINT ( 'NONE',  ( 0.000000000000000000, 0.000000000000000000, 4.000000000000000000 ) ) ;
#99054=VERTEX_POINT ( 'NONE', #9969 ) ;
#99070=CARTESIAN_POINT ( 'NONE',  ( 6.445370176743034918, 7.262437273742029298, -1.101027156350743663 ) ) ;
#99080=EDGE_CURVE ( 'NONE', #100006, #60457, #34823, .T. ) ;
#99083=VERTEX_POINT ( 'NONE', #68770 ) ;
#99111=CARTESIAN_POINT ( 'NONE',  ( 0.000000000000000000, 0.000000000000000000, 0.000000000000000000 ) ) ;
#99116=AXIS2_PLACEMENT_3D ( 'NONE', #36308, #12492, #78300 ) ;
#99123=CARTESIAN_POINT ( 'NONE',  ( 0.000000000000000000, 0.000000000000000000, 0.000000000000000000 ) ) ;
#99126=VERTEX_POINT ( 'NONE', #36943 ) ;
#99136=CARTESIAN_POINT ( 'NONE',  ( 0.5805565836007605673, -3.752776749732561257, 6.500000000000000000 ) ) ;
#99139=CIRCLE ( 'NONE', #42336, 8.605212085995399107 ) ;
#99151=DIRECTION ( 'NONE',  ( -1.000000000000000000, -1.224606353822377258E-16, -0.000000000000000000 ) ) ;
#99155=CARTESIAN_POINT ( 'NONE',  ( 6.326592304916279552, 6.579439845142156074, 2.267162479624769134 ) ) ;
#99189=ORIENTED_EDGE ( 'NONE', *, *, #87050, .T. ) ;
#99207=CARTESIAN_POINT ( 'NONE',  ( 6.162888688655347558, 7.505553499465140277, 0.000000000000000000 ) ) ;
#99208=CIRCLE ( 'NONE', #9663, 4.000000000000000888 ) ;
#99225=DIRECTION ( 'NONE',  ( 0.000000000000000000, -1.000000000000000000, 0.000000000000000000 ) ) ;
#99232=DIRECTION ( 'NONE',  ( -1.000000000000000000, -0.000000000000000000, -0.000000000000000000 ) ) ;
#99238=DIRECTION ( 'NONE',  ( 0.000000000000000000, 0.000000000000000000, 1.000000000000000000 ) ) ;
#99256=CARTESIAN_POINT ( 'NONE',  ( 6.683837171061802529, 3.955946848495962787, 6.851900933636986935 ) ) ;
#99264=EDGE_LOOP ( 'NONE', ( #72966, #60996, #96799, #23828, #64562 ) ) ;
#99294=ORIENTED_EDGE ( 'NONE', *, *, #99001, .T. ) ;
#99336=CARTESIAN_POINT ( 'NONE',  ( 43.58349330513380693, 1.593028355512270567E-15, 0.000000000000000000 ) ) ;
#99345=CARTESIAN_POINT ( 'NONE',  ( 21.84999999999999787, 1.533819458162526451E-15, 0.000000000000000000 ) ) ;
#99352=ORIENTED_EDGE ( 'NONE', *, *, #96715, .T. ) ;
#99366=VECTOR ( 'NONE', #91105, 1000.000000000000114 ) ;
#99371=EDGE_CURVE ( 'NONE', #77299, #76326, #9297, .T. ) ;
#99372=CARTESIAN_POINT ( 'NONE',  ( 46.84999999999999432, 3.309500000000003439, 4.052968581778167743E-16 ) ) ;
#99373=AXIS2_PLACEMENT_3D ( 'NONE', #52993, #62686, #70239 ) ;
#99393=ORIENTED_EDGE ( 'NONE', *, *, #80978, .F. ) ;
#99416=AXIS2_PLACEMENT_3D ( 'NONE', #85893, #75641, #27140 ) ;
#99444=CIRCLE ( 'NONE', #83907, 4.000000000000001776 ) ;
#99448=DIRECTION ( 'NONE',  ( -1.000000000000000000, -1.224606353822377258E-16, -0.000000000000000000 ) ) ;
#99466=CARTESIAN_POINT ( 'NONE',  ( 5.975663821521009389, -7.000939006314210289, -0.8740179403730387042 ) ) ;
#99478=CARTESIAN_POINT ( 'NONE',  ( 8.866506694866188809, 4.898587196589411843E-16, -4.000000000000000888 ) ) ;
#99490=DIRECTION ( 'NONE',  ( -1.000000000000000000, -0.000000000000000000, -0.000000000000000000 ) ) ;
#99494=AXIS2_PLACEMENT_3D ( 'NONE', #51157, #84074, #50105 ) ;
#99509=DIRECTION ( 'NONE',  ( -1.000000000000000000, -1.224606353822377258E-16, -0.000000000000000000 ) ) ;
#99525=CIRCLE ( 'NONE', #8225, 4.000000000000001776 ) ;
#99526=CARTESIAN_POINT ( 'NONE',  ( 0.000000000000000000, 0.000000000000000000, 4.000000000000000000 ) ) ;
#99545=DIRECTION ( 'NONE',  ( 0.000000000000000000, -1.000000000000000000, 0.000000000000000000 ) ) ;
#99559=FACE_OUTER_BOUND ( 'NONE', #41187, .T. ) ;
#99574=AXIS2_PLACEMENT_3D ( 'NONE', #96314, #6201, #48251 ) ;
#99576=DIRECTION ( 'NONE',  ( -1.000000000000000000, -0.000000000000000000, -0.000000000000000000 ) ) ;
#99577=ORIENTED_EDGE ( 'NONE', *, *, #16066, .F. ) ;
#99596=ORIENTED_EDGE ( 'NONE', *, *, #9474, .T. ) ;
#99606=AXIS2_PLACEMENT_3D ( 'NONE', #5954, #63156, #36787 ) ;
#99609=ADVANCED_FACE ( 'NONE', ( #17298 ), #84144, .T. ) ;
#99614=CARTESIAN_POINT ( 'NONE',  ( 6.692588830498424457, 3.932766476276027046, -6.892929031562515796 ) ) ;
#99634=CIRCLE ( 'NONE', #72304, 3.309500000000001663 ) ;
#99638=DIRECTION ( 'NONE',  ( 0.000000000000000000, 0.000000000000000000, 1.000000000000000000 ) ) ;
#99662=CARTESIAN_POINT ( 'NONE',  ( 19.83349330513379982, 1.593028355512270567E-15, 0.000000000000000000 ) ) ;
#99663=CIRCLE ( 'NONE', #106515, 4.000000000000001776 ) ;
#99666=ORIENTED_EDGE ( 'NONE', *, *, #72556, .T. ) ;
#99674=CARTESIAN_POINT ( 'NONE',  ( 6.291746522141169251, 1.386194408037410231, -6.829127798246559244 ) ) ;
#99707=DIRECTION ( 'NONE',  ( 0.5735764363510462704, 0.8191520442889915765, 0.000000000000000000 ) ) ;
#99708=AXIS2_PLACEMENT_3D ( 'NONE', #43240, #75599, #42166 ) ;
#99749=DIRECTION ( 'NONE',  ( 0.000000000000000000, -1.000000000000000000, 0.000000000000000000 ) ) ;
#99758=DIRECTION ( 'NONE',  ( 1.000000000000000000, 1.224606353822377258E-16, 0.000000000000000000 ) ) ;
#99763=AXIS2_PLACEMENT_3D ( 'NONE', #5490, #54016, #29798 ) ;
#99770=EDGE_LOOP ( 'NONE', ( #6125, #43707, #36218, #33197, #21395, #48766 ) ) ;
#99865=ORIENTED_EDGE ( 'NONE', *, *, #92875, .T. ) ;
#99870=EDGE_CURVE ( 'NONE', #53830, #23893, #71621, .T. ) ;
#99878=EDGE_CURVE ( 'NONE', #9941, #20019, #78483, .T. ) ;
#99883=EDGE_LOOP ( 'NONE', ( #22233, #19280, #40614, #48660, #80533, #67862, #78596 ) ) ;
#99919=CARTESIAN_POINT ( 'NONE',  ( 22.33349330513380337, 1.593028355512270567E-15, 0.000000000000000000 ) ) ;
#99921=FACE_OUTER_BOUND ( 'NONE', #17331, .T. ) ;
#99928=VECTOR ( 'NONE', #84028, 1000.000000000000000 ) ;
#99943=VERTEX_POINT ( 'NONE', #26360 ) ;
#99954=CARTESIAN_POINT ( 'NONE',  ( 30.11650669486618881, -3.999999999999998224, 0.000000000000000000 ) ) ;
#99956=AXIS2_PLACEMENT_3D ( 'NONE', #13629, #21771, #37432 ) ;
#99966=AXIS2_PLACEMENT_3D ( 'NONE', #79792, #5387, #15048 ) ;
#99988=CIRCLE ( 'NONE', #68988, 4.000000000000001776 ) ;
#100000=ADVANCED_FACE ( 'NONE', ( #39105 ), #63021, .T. ) ;
#100006=VERTEX_POINT ( 'NONE', #54718 ) ;
#100014=CARTESIAN_POINT ( 'NONE',  ( 8.099999999999999645, 3.752776749732561257, -6.499999999999999112 ) ) ;
#100018=EDGE_LOOP ( 'NONE', ( #73573, #36528, #101424, #68873 ) ) ;
#100021=LINE ( 'NONE', #60137, #18395 ) ;
#100024=VERTEX_POINT ( 'NONE', #22410 ) ;
#100050=CARTESIAN_POINT ( 'NONE',  ( 17.61650669486618881, 1.474610560812782335E-15, 0.000000000000000000 ) ) ;
#100063=DIRECTION ( 'NONE',  ( 0.000000000000000000, -1.000000000000000000, 0.000000000000000000 ) ) ;
#100076=AXIS2_PLACEMENT_3D ( 'NONE', #51160, #26946, #20472 ) ;
#100087=CARTESIAN_POINT ( 'NONE',  ( 22.61650669486618526, -3.999999999999998224, 0.000000000000000000 ) ) ;
#100091=CARTESIAN_POINT ( 'NONE',  ( 44.83349330513380693, 4.000000000000002665, 0.000000000000000000 ) ) ;
#100095=AXIS2_PLACEMENT_3D ( 'NONE', #64356, #81034, #7150 ) ;
#100102=EDGE_CURVE ( 'NONE', #74232, #46481, #90571, .T. ) ;
#100107=ORIENTED_EDGE ( 'NONE', *, *, #85360, .T. ) ;
#100131=ADVANCED_FACE ( 'NONE', ( #82729 ), #75157, .T. ) ;
#100146=CARTESIAN_POINT ( 'NONE',  ( 8.866506694866188809, -3.999999999999998224, 0.000000000000000000 ) ) ;
#100165=DIRECTION ( 'NONE',  ( 0.000000000000000000, 1.000000000000000000, 0.000000000000000000 ) ) ;
#100201=LINE ( 'NONE', #74321, #82384 ) ;
#100211=AXIS2_PLACEMENT_3D ( 'NONE', #10696, #35560, #42011 ) ;
#100240=ORIENTED_EDGE ( 'NONE', *, *, #95335, .F. ) ;
#100266=VERTEX_POINT ( 'NONE', #20174 ) ;
#100278=FACE_OUTER_BOUND ( 'NONE', #79413, .T. ) ;
#100283=AXIS2_PLACEMENT_3D ( 'NONE', #59265, #92678, #35008 ) ;
#100293=ORIENTED_EDGE ( 'NONE', *, *, #71398, .F. ) ;
#100330=EDGE_LOOP ( 'NONE', ( #76530, #18858, #72725, #24358, #38635 ) ) ;
#100347=CYLINDRICAL_SURFACE ( 'NONE', #33826, 4.000000000000000000 ) ;
#100408=CARTESIAN_POINT ( 'NONE',  ( 6.585468679846627538, -7.640532685286905767, -0.2337908078075620621 ) ) ;
#100411=ORIENTED_EDGE ( 'NONE', *, *, #8547, .T. ) ;
#100432=LINE ( 'NONE', #76688, #12922 ) ;
#100437=EDGE_CURVE ( 'NONE', #45306, #70963, #76221, .T. ) ;
#100454=CARTESIAN_POINT ( 'NONE',  ( 20.59999999999999787, 3.309500000000003439, 0.000000000000000000 ) ) ;
#100469=CYLINDRICAL_SURFACE ( 'NONE', #64608, 4.000000000000000000 ) ;
#100478=FACE_OUTER_BOUND ( 'NONE', #23350, .T. ) ;
#100484=DIRECTION ( 'NONE',  ( 0.000000000000000000, -1.000000000000000000, 0.000000000000000000 ) ) ;
#100499=DIRECTION ( 'NONE',  ( 1.000000000000000000, 1.224606353822377258E-16, 0.000000000000000000 ) ) ;
#100508=ADVANCED_FACE ( 'NONE', ( #22274 ), #9634, .T. ) ;
#100513=CIRCLE ( 'NONE', #9273, 4.000000000000000888 ) ;
#100520=ORIENTED_EDGE ( 'NONE', *, *, #86784, .F. ) ;
#100529=DIRECTION ( 'NONE',  ( 1.000000000000000000, 1.224606353822377258E-16, 0.000000000000000000 ) ) ;
#100533=EDGE_CURVE ( 'NONE', #45302, #49899, #104424, .T. ) ;
#100553=ORIENTED_EDGE ( 'NONE', *, *, #63596, .F. ) ;
#100556=AXIS2_PLACEMENT_3D ( 'NONE', #52856, #77135, #85783 ) ;
#100583=CARTESIAN_POINT ( 'NONE',  ( 6.683837171061809634, -7.911893696991943337, -3.558927330633863411E-17 ) ) ;
#100590=DIRECTION ( 'NONE',  ( -1.000000000000000000, -1.224606353822377258E-16, -0.000000000000000000 ) ) ;
#100608=ORIENTED_EDGE ( 'NONE', *, *, #21037, .F. ) ;
#100627=ORIENTED_EDGE ( 'NONE', *, *, #106679, .F. ) ;
#100642=UNCERTAINTY_MEASURE_WITH_UNIT (LENGTH_MEASURE( 1.000000000000000082E-05 ), #62140, 'distance_accuracy_value', 'NONE');
#100652=CARTESIAN_POINT ( 'NONE',  ( 5.819846122303830249, 4.937269551422740044, 4.448398286273013369 ) ) ;
#100667=AXIS2_PLACEMENT_3D ( 'NONE', #69010, #34003, #101885 ) ;
#100682=ORIENTED_EDGE ( 'NONE', *, *, #93426, .T. ) ;
#100688=FACE_OUTER_BOUND ( 'NONE', #46151, .T. ) ;
#100695=FACE_OUTER_BOUND ( 'NONE', #86344, .T. ) ;
#100698=B_SPLINE_CURVE_WITH_KNOTS ( 'NONE', 3,
 ( #33678, #22939, #97850, #81132, #72515, #40149 ),
 .UNSPECIFIED., .F., .F.,
 ( 4, 2, 4 ),
 ( 0.000000000000000000, 0.001995463903526792284, 0.003990927807053584568 ),
 .UNSPECIFIED. ) ;
#100710=ADVANCED_FACE ( 'NONE', ( #106320 ), #34091, .T. ) ;
#100726=VERTEX_POINT ( 'NONE', #57241 ) ;
#100735=ORIENTED_EDGE ( 'NONE', *, *, #83369, .T. ) ;
#100745=ORIENTED_EDGE ( 'NONE', *, *, #58533, .F. ) ;
#100753=CARTESIAN_POINT ( 'NONE',  ( 41.36650669486618881, 1.474610560812782335E-15, 0.000000000000000000 ) ) ;
#100768=DIRECTION ( 'NONE',  ( 0.000000000000000000, 0.000000000000000000, 1.000000000000000000 ) ) ;
#100769=CIRCLE ( 'NONE', #52660, 4.000000000000000888 ) ;
#100770=CIRCLE ( 'NONE', #97306, 3.309500000000001663 ) ;
#100775=AXIS2_PLACEMENT_3D ( 'NONE', #91123, #65764, #83530 ) ;
#100816=CARTESIAN_POINT ( 'NONE',  ( 44.83349330513380693, 1.593028355512270567E-15, 0.000000000000000000 ) ) ;
#100820=CIRCLE ( 'NONE', #54297, 4.000000000000000888 ) ;
#100851=AXIS2_PLACEMENT_3D ( 'NONE', #95357, #87274, #13352 ) ;
#100867=DIRECTION ( 'NONE',  ( 0.3420201433256622736, 0.000000000000000000, -0.9396926207859106484 ) ) ;
#100874=ORIENTED_EDGE ( 'NONE', *, *, #334, .T. ) ;
#100878=DIRECTION ( 'NONE',  ( 0.000000000000000000, -1.000000000000000000, 0.000000000000000000 ) ) ;
#100911=CIRCLE ( 'NONE', #38945, 4.000000000000001776 ) ;
#100932=CIRCLE ( 'NONE', #54396, 4.000000000000000888 ) ;
#100934=FACE_OUTER_BOUND ( 'NONE', #106373, .T. ) ;
#100939=CARTESIAN_POINT ( 'NONE',  ( 6.585468679846619544, -3.617797563910806868, 6.733790807807553236 ) ) ;
#100976=DIRECTION ( 'NONE',  ( 0.000000000000000000, 0.000000000000000000, 1.000000000000000000 ) ) ;
#100990=AXIS2_PLACEMENT_3D ( 'NONE', #17025, #99509, #33218 ) ;
#101003=CARTESIAN_POINT ( 'NONE',  ( 0.000000000000000000, 4.898587196589412829E-16, -4.000000000000000000 ) ) ;
#101008=ORIENTED_EDGE ( 'NONE', *, *, #49935, .T. ) ;
#101074=ORIENTED_EDGE ( 'NONE', *, *, #27307, .F. ) ;
#101078=CARTESIAN_POINT ( 'NONE',  ( 26.36650669486618881, 1.474610560812782335E-15, 0.000000000000000000 ) ) ;
#101085=DIRECTION ( 'NONE',  ( -0.5735764363510497121, 0.8191520442889892450, 1.003171929053521665E-16 ) ) ;
#101110=CARTESIAN_POINT ( 'NONE',  ( 0.000000000000000000, 0.000000000000000000, 4.000000000000000000 ) ) ;
#101119=DIRECTION ( 'NONE',  ( -1.000000000000000000, -1.224606353822377258E-16, -0.000000000000000000 ) ) ;
#101130=CARTESIAN_POINT ( 'NONE',  ( 46.08349330513379982, 1.593028355512270567E-15, 0.000000000000000000 ) ) ;
#101146=EDGE_LOOP ( 'NONE', ( #101074, #16567, #28517, #97168, #6531 ) ) ;
#101182=ORIENTED_EDGE ( 'NONE', *, *, #24425, .T. ) ;
#101187=CARTESIAN_POINT ( 'NONE',  ( 0.000000000000000000, 0.000000000000000000, 0.000000000000000000 ) ) ;
#101231=DIRECTION ( 'NONE',  ( -1.000000000000000000, -0.000000000000000000, -0.000000000000000000 ) ) ;
#101251=DIRECTION ( 'NONE',  ( 0.000000000000000000, 0.000000000000000000, 1.000000000000000000 ) ) ;
#101285=CIRCLE ( 'NONE', #22075, 4.000000000000000888 ) ;
#101292=DIRECTION ( 'NONE',  ( 1.000000000000000000, 1.224606353822377258E-16, 0.000000000000000000 ) ) ;
#101293=VERTEX_POINT ( 'NONE', #63550 ) ;
#101303=DIRECTION ( 'NONE',  ( 0.000000000000000000, -1.000000000000000000, 0.000000000000000000 ) ) ;
#101304=DIRECTION ( 'NONE',  ( 0.000000000000000000, -1.000000000000000000, 0.000000000000000000 ) ) ;
#101311=CONICAL_SURFACE ( 'NONE', #20382, 4.000000000000001776, 0.9599310885968808105 ) ;
#101336=EDGE_LOOP ( 'NONE', ( #87521, #37806, #58293, #20593, #18124 ) ) ;
#101350=CARTESIAN_POINT ( 'NONE',  ( 6.692428679880670472, -4.002209756868618129, 6.852332176615682613 ) ) ;
#101358=CARTESIAN_POINT ( 'NONE',  ( 33.09999999999999432, 1.533819458162526451E-15, 0.000000000000000000 ) ) ;
#101380=EDGE_CURVE ( 'NONE', #96063, #52601, #35720, .T. ) ;
#101418=CARTESIAN_POINT ( 'NONE',  ( 46.36650669486618881, 4.000000000000003553, 4.898587196589414801E-16 ) ) ;
#101424=ORIENTED_EDGE ( 'NONE', *, *, #97312, .T. ) ;
#101473=DIRECTION ( 'NONE',  ( 0.000000000000000000, -1.000000000000000000, 0.000000000000000000 ) ) ;
#101572=ORIENTED_EDGE ( 'NONE', *, *, #42553, .F. ) ;
#101574=EDGE_LOOP ( 'NONE', ( #39855, #66725, #51050, #14167, #66243 ) ) ;
#101588=CONICAL_SURFACE ( 'NONE', #10254, 4.000000000000001776, 0.9599310885968808105 ) ;
#101608=CARTESIAN_POINT ( 'NONE',  ( 15.59999999999999787, 3.309500000000003439, 4.052968581778167743E-16 ) ) ;
#101632=CARTESIAN_POINT ( 'NONE',  ( 35.59999999999999432, 3.309500000000003439, 4.052968581778167743E-16 ) ) ;
#101640=ORIENTED_EDGE ( 'NONE', *, *, #36564, .T. ) ;
#101641=AXIS2_PLACEMENT_3D ( 'NONE', #20455, #79681, #13873 ) ;
#101661=VERTEX_POINT ( 'NONE', #83833 ) ;
#101672=AXIS2_PLACEMENT_3D ( 'NONE', #25739, #9480, #58594 ) ;
#101722=CARTESIAN_POINT ( 'NONE',  ( 6.692588830498428898, 7.935834885954428763, -0.04058884017440173020 ) ) ;
#101744=ORIENTED_EDGE ( 'NONE', *, *, #89056, .T. ) ;
#101763=CYLINDRICAL_SURFACE ( 'NONE', #29543, 4.000000000000000000 ) ;
#101777=CARTESIAN_POINT ( 'NONE',  ( 13.86650669486618881, 1.474610560812782335E-15, 0.000000000000000000 ) ) ;
#101783=FACE_OUTER_BOUND ( 'NONE', #31587, .T. ) ;
#101797=AXIS2_PLACEMENT_3D ( 'NONE', #15381, #72554, #39152 ) ;
#101803=CARTESIAN_POINT ( 'NONE',  ( 20.59999999999999787, 1.533819458162526451E-15, 0.000000000000000000 ) ) ;
#101811=FACE_OUTER_BOUND ( 'NONE', #61949, .T. ) ;
#101815=EDGE_CURVE ( 'NONE', #478, #70516, #85997, .T. ) ;
#101825=AXIS2_PLACEMENT_3D ( 'NONE', #73672, #82840, #40253 ) ;
#101836=CARTESIAN_POINT ( 'NONE',  ( 34.83349330513379982, 4.000000000000002665, 0.000000000000000000 ) ) ;
#101856=ORIENTED_EDGE ( 'NONE', *, *, #63976, .F. ) ;
#101872=CARTESIAN_POINT ( 'NONE',  ( 6.449804269883600227, -2.701269212709792367, 6.840189325177430391 ) ) ;
#101873=CONICAL_SURFACE ( 'NONE', #27865, 4.000000000000001776, 0.9599310885968808105 ) ;
#101884=CARTESIAN_POINT ( 'NONE',  ( 33.86650669486618881, 1.474610560812782335E-15, 0.000000000000000000 ) ) ;
#101885=DIRECTION ( 'NONE',  ( 0.000000000000000000, -1.000000000000000000, 0.000000000000000000 ) ) ;
#101900=ADVANCED_FACE ( 'NONE', ( #32534 ), #48669, .T. ) ;
#101929=FACE_OUTER_BOUND ( 'NONE', #88425, .T. ) ;
#101981=AXIS2_PLACEMENT_3D ( 'NONE', #18287, #76486, #82462 ) ;
#101987=VECTOR ( 'NONE', #66641, 1000.000000000000000 ) ;
#101990=DIRECTION ( 'NONE',  ( -1.000000000000000000, -1.224606353822377258E-16, -0.000000000000000000 ) ) ;
#102019=ORIENTED_EDGE ( 'NONE', *, *, #40608, .T. ) ;
#102023=DIRECTION ( 'NONE',  ( -1.000000000000000000, -0.000000000000000000, -0.000000000000000000 ) ) ;
#102030=SURFACE_STYLE_USAGE ( .BOTH. , #85329 ) ;
#102033=DIRECTION ( 'NONE',  ( 0.000000000000000000, -1.000000000000000000, 0.000000000000000000 ) ) ;
#102040=DIRECTION ( 'NONE',  ( -1.000000000000000000, -1.224606353822377258E-16, -0.000000000000000000 ) ) ;
#102049=EDGE_LOOP ( 'NONE', ( #104142, #47437, #87013, #76262, #94849 ) ) ;
#102070=CARTESIAN_POINT ( 'NONE',  ( 32.33349330513379982, 4.000000000000002665, 0.000000000000000000 ) ) ;
#102080=ORIENTED_EDGE ( 'NONE', *, *, #26631, .F. ) ;
#102088=CIRCLE ( 'NONE', #98685, 4.000000000000001776 ) ;
#102092=ORIENTED_EDGE ( 'NONE', *, *, #85360, .F. ) ;
#102129=VECTOR ( 'NONE', #61349, 1000.000000000000000 ) ;
#102139=DIRECTION ( 'NONE',  ( -1.000000000000000000, -0.000000000000000000, -0.000000000000000000 ) ) ;
#102153=EDGE_CURVE ( 'NONE', #57881, #84797, #53674, .T. ) ;
#102198=CIRCLE ( 'NONE', #45404, 4.000000000000000000 ) ;
#102223=CARTESIAN_POINT ( 'NONE',  ( 40.11650669486618881, 4.000000000000003553, 4.898587196589414801E-16 ) ) ;
#102240=ORIENTED_EDGE ( 'NONE', *, *, #9605, .T. ) ;
#102271=CARTESIAN_POINT ( 'NONE',  ( 26.36650669486618881, 1.474610560812782335E-15, 0.000000000000000000 ) ) ;
#102272=CARTESIAN_POINT ( 'NONE',  ( 36.36650669486618881, -3.999999999999998224, 0.000000000000000000 ) ) ;
#102298=DIRECTION ( 'NONE',  ( 0.000000000000000000, 0.000000000000000000, 1.000000000000000000 ) ) ;
#102310=LINE ( 'NONE', #60806, #24597 ) ;
#102320=LINE ( 'NONE', #28471, #102129 ) ;
#102357=DIRECTION ( 'NONE',  ( -1.000000000000000000, -1.224606353822377258E-16, -0.000000000000000000 ) ) ;
#102367=DIRECTION ( 'NONE',  ( -1.000000000000000000, -1.224606353822377258E-16, -0.000000000000000000 ) ) ;
#102391=VERTEX_POINT ( 'NONE', #70674 ) ;
#102406=AXIS2_PLACEMENT_3D ( 'NONE', #16925, #7742, #32595 ) ;
#102429=ORIENTED_EDGE ( 'NONE', *, *, #50073, .F. ) ;
#102438=DIRECTION ( 'NONE',  ( -1.000000000000000000, -1.224606353822377258E-16, -0.000000000000000000 ) ) ;
#102440=AXIS2_PLACEMENT_3D ( 'NONE', #42873, #91955, #76296 ) ;
#102457=ORIENTED_EDGE ( 'NONE', *, *, #96025, .T. ) ;
#102472=AXIS2_PLACEMENT_3D ( 'NONE', #9207, #8687, #18405 ) ;
#102474=ORIENTED_EDGE ( 'NONE', *, *, #99878, .F. ) ;
#102477=AXIS2_PLACEMENT_3D ( 'NONE', #95450, #37789, #70650 ) ;
#102484=ORIENTED_EDGE ( 'NONE', *, *, #68492, .T. ) ;
#102497=LINE ( 'NONE', #10800, #1404 ) ;
#102509=DIRECTION ( 'NONE',  ( 0.000000000000000000, 0.000000000000000000, 1.000000000000000000 ) ) ;
#102519=DIRECTION ( 'NONE',  ( 0.000000000000000000, -1.000000000000000000, 0.000000000000000000 ) ) ;
#102521=DIRECTION ( 'NONE',  ( 1.000000000000000000, 1.224606353822377258E-16, 0.000000000000000000 ) ) ;
#102531=ORIENTED_EDGE ( 'NONE', *, *, #35079, .T. ) ;
#102532=DIRECTION ( 'NONE',  ( -1.000000000000000000, -1.224606353822377258E-16, -0.000000000000000000 ) ) ;
#102540=VECTOR ( 'NONE', #56798, 1000.000000000000000 ) ;
#102541=DIRECTION ( 'NONE',  ( 0.000000000000000000, -1.000000000000000000, 0.000000000000000000 ) ) ;
#102549=B_SPLINE_CURVE_WITH_KNOTS ( 'NONE', 3,
 ( #7465, #80834, #48988, #8541, #98610, #24761, #66254, #99136 ),
 .UNSPECIFIED., .F., .F.,
 ( 4, 2, 2, 4 ),
 ( 0.003797433802554463656, 0.004743183970586255238, 0.005688934138618048121, 0.007580434474681636489 ),
 .UNSPECIFIED. ) ;
#102550=DIRECTION ( 'NONE',  ( 0.000000000000000000, 1.000000000000000000, 0.000000000000000000 ) ) ;
#102556=AXIS2_PLACEMENT_3D ( 'NONE', #8322, #41226, #66035 ) ;
#102566=ORIENTED_EDGE ( 'NONE', *, *, #40335, .T. ) ;
#102597=ADVANCED_FACE ( 'NONE', ( #1820 ), #48085, .T. ) ;
#102610=ORIENTED_EDGE ( 'NONE', *, *, #50404, .T. ) ;
#102623=ORIENTED_EDGE ( 'NONE', *, *, #21610, .T. ) ;
#102628=VECTOR ( 'NONE', #80720, 1000.000000000000114 ) ;
#102635=DIRECTION ( 'NONE',  ( 0.5735764363510466035, -0.8191520442889914655, 1.003171929053524500E-16 ) ) ;
#102647=EDGE_CURVE ( 'NONE', #77299, #59177, #68726, .T. ) ;
#102649=ORIENTED_EDGE ( 'NONE', *, *, #64245, .F. ) ;
#102655=ORIENTED_EDGE ( 'NONE', *, *, #53722, .T. ) ;
#102662=DIRECTION ( 'NONE',  ( -1.000000000000000000, -1.224606353822377258E-16, -0.000000000000000000 ) ) ;
#102668=CARTESIAN_POINT ( 'NONE',  ( 5.947762761376479190, -6.880090707843049103, 1.083333333333333259 ) ) ;
#102693=ORIENTED_EDGE ( 'NONE', *, *, #39102, .T. ) ;
#102703=DIRECTION ( 'NONE',  ( 0.000000000000000000, 1.000000000000000000, 0.000000000000000000 ) ) ;
#102718=CIRCLE ( 'NONE', #50954, 4.000000000000001776 ) ;
#102743=CARTESIAN_POINT ( 'NONE',  ( 0.000000000000000000, 0.000000000000000000, 0.000000000000000000 ) ) ;
#102748=CARTESIAN_POINT ( 'NONE',  ( 33.86650669486618881, -3.999999999999998224, 0.000000000000000000 ) ) ;
#102788=CIRCLE ( 'NONE', #73418, 3.309500000000001663 ) ;
#102815=EDGE_CURVE ( 'NONE', #78081, #58076, #44663, .T. ) ;
#102833=LINE ( 'NONE', #46706, #78974 ) ;
#102848=DIRECTION ( 'NONE',  ( 0.000000000000000000, 0.5000000000000008882, -0.8660254037844381525 ) ) ;
#102854=CIRCLE ( 'NONE', #56313, 4.000000000000001776 ) ;
#102858=EDGE_CURVE ( 'NONE', #103547, #29512, #99988, .T. ) ;
#102912=AXIS2_PLACEMENT_3D ( 'NONE', #33229, #17574, #57460 ) ;
#102922=CARTESIAN_POINT ( 'NONE',  ( 16.36650669486618881, -3.851859888774471706E-31, 4.000000000000000888 ) ) ;
#102933=ORIENTED_EDGE ( 'NONE', *, *, #82254, .T. ) ;
#102940=CONICAL_SURFACE ( 'NONE', #9911, 3.309500000000001663, 0.9599310885968770357 ) ;
#102951=ORIENTED_EDGE ( 'NONE', *, *, #95698, .T. ) ;
#102963=ORIENTED_EDGE ( 'NONE', *, *, #60099, .F. ) ;
#102974=CARTESIAN_POINT ( 'NONE',  ( 6.162888688655346670, -3.752776749732575468, -6.499999999999999112 ) ) ;
#102994=DIRECTION ( 'NONE',  ( 0.000000000000000000, 1.000000000000000000, 0.000000000000000000 ) ) ;
#103001=VECTOR ( 'NONE', #40930, 1000.000000000000114 ) ;
#103028=CARTESIAN_POINT ( 'NONE',  ( 10.59999999999999609, 1.533819458162526451E-15, 0.000000000000000000 ) ) ;
#103062=ORIENTED_EDGE ( 'NONE', *, *, #57003, .T. ) ;
#103067=ORIENTED_EDGE ( 'NONE', *, *, #82819, .T. ) ;
#103070=CARTESIAN_POINT ( 'NONE',  ( 16.84999999999999787, 1.533819458162526451E-15, 0.000000000000000000 ) ) ;
#103073=DIRECTION ( 'NONE',  ( 0.000000000000000000, -1.000000000000000000, 0.000000000000000000 ) ) ;
#103110=DIRECTION ( 'NONE',  ( -1.000000000000000000, -1.224606353822377258E-16, -0.000000000000000000 ) ) ;
#103112=CYLINDRICAL_SURFACE ( 'NONE', #84418, 4.000000000000000000 ) ;
#103120=ORIENTED_EDGE ( 'NONE', *, *, #25695, .T. ) ;
#103127=ORIENTED_EDGE ( 'NONE', *, *, #97786, .F. ) ;
#103128=AXIS2_PLACEMENT_3D ( 'NONE', #87451, #63171, #13532 ) ;
#103194=FACE_OUTER_BOUND ( 'NONE', #4712, .T. ) ;
#103197=DIRECTION ( 'NONE',  ( 0.000000000000000000, -1.000000000000000000, 0.000000000000000000 ) ) ;
#103203=DIRECTION ( 'NONE',  ( -1.000000000000000000, -0.000000000000000000, -0.000000000000000000 ) ) ;
#103217=EDGE_CURVE ( 'NONE', #40330, #3694, #64605, .T. ) ;
#103254=EDGE_CURVE ( 'NONE', #86482, #31074, #56487, .T. ) ;
#103256=VERTEX_POINT ( 'NONE', #105064 ) ;
#103351=EDGE_LOOP ( 'NONE', ( #73584, #7131, #98618, #97175, #11134 ) ) ;
#103363=CIRCLE ( 'NONE', #77494, 3.309499999999999886 ) ;
#103370=DIRECTION ( 'NONE',  ( -1.000000000000000000, -0.000000000000000000, -0.000000000000000000 ) ) ;
#103382=CARTESIAN_POINT ( 'NONE',  ( 29.83349330513380337, -4.000000000000000888, 4.898587196589416773E-16 ) ) ;
#103407=DIRECTION ( 'NONE',  ( -1.000000000000000000, -0.000000000000000000, -0.000000000000000000 ) ) ;
#103453=ORIENTED_EDGE ( 'NONE', *, *, #19513, .F. ) ;
#103455=CARTESIAN_POINT ( 'NONE',  ( 36.84999999999999432, 1.533819458162526451E-15, 0.000000000000000000 ) ) ;
#103460=VERTEX_POINT ( 'NONE', #42443 ) ;
#103470=CARTESIAN_POINT ( 'NONE',  ( 25.59999999999999787, -3.309499999999999886, 0.000000000000000000 ) ) ;
#103484=DIRECTION ( 'NONE',  ( -1.000000000000000000, -0.000000000000000000, -0.000000000000000000 ) ) ;
#103513=VERTEX_POINT ( 'NONE', #34396 ) ;
#103522=CARTESIAN_POINT ( 'NONE',  ( 44.83349330513380693, 1.593028355512270567E-15, 0.000000000000000000 ) ) ;
#103529=FACE_OUTER_BOUND ( 'NONE', #58853, .T. ) ;
#103541=EDGE_CURVE ( 'NONE', #86259, #81954, #17402, .T. ) ;
#103547=VERTEX_POINT ( 'NONE', #104391 ) ;
#103548=CARTESIAN_POINT ( 'NONE',  ( 19.34999999999999787, 1.533819458162526451E-15, 0.000000000000000000 ) ) ;
#103582=AXIS2_PLACEMENT_3D ( 'NONE', #37667, #11732, #29569 ) ;
#103597=DIRECTION ( 'NONE',  ( 0.000000000000000000, -1.000000000000000000, 0.000000000000000000 ) ) ;
#103598=EDGE_CURVE ( 'NONE', #47451, #89958, #96613, .T. ) ;
#103628=( NAMED_UNIT ( * ) SI_UNIT ( $, .STERADIAN. ) SOLID_ANGLE_UNIT ( ) );
#103643=CARTESIAN_POINT ( 'NONE',  ( 33.09999999999999432, 1.533819458162526451E-15, 0.000000000000000000 ) ) ;
#103690=ORIENTED_EDGE ( 'NONE', *, *, #24932, .F. ) ;
#103715=CYLINDRICAL_SURFACE ( 'NONE', #30276, 4.000000000000000000 ) ;
#103720=DIRECTION ( 'NONE',  ( -1.000000000000000000, -1.224606353822377258E-16, -0.000000000000000000 ) ) ;
#103727=CARTESIAN_POINT ( 'NONE',  ( 0.000000000000000000, 4.898587196589412829E-16, -4.000000000000000000 ) ) ;
#103732=ORIENTED_EDGE ( 'NONE', *, *, #70473, .T. ) ;
#103733=DIRECTION ( 'NONE',  ( 0.000000000000000000, -1.000000000000000000, 0.000000000000000000 ) ) ;
#103755=ADVANCED_FACE ( 'NONE', ( #39156 ), #44969, .T. ) ;
#103768=EDGE_CURVE ( 'NONE', #76086, #97178, #69056, .T. ) ;
#103824=CARTESIAN_POINT ( 'NONE',  ( 11.08349330513380160, 1.593028355512270567E-15, 0.000000000000000000 ) ) ;
#103852=ORIENTED_EDGE ( 'NONE', *, *, #76182, .T. ) ;
#103853=VERTEX_POINT ( 'NONE', #9946 ) ;
#103858=LINE ( 'NONE', #22455, #94976 ) ;
#103866=CARTESIAN_POINT ( 'NONE',  ( 6.289572920342629381, -5.584521518880467106, -3.985288806461540823 ) ) ;
#103911=ORIENTED_EDGE ( 'NONE', *, *, #63635, .T. ) ;
#103934=VERTEX_POINT ( 'NONE', #74142 ) ;
#103940=CARTESIAN_POINT ( 'NONE',  ( 48.10000000000000142, 4.475777889183788807E-16, -3.309499999999999886 ) ) ;
#103979=DIRECTION ( 'NONE',  ( -1.000000000000000000, -1.224606353822377258E-16, -0.000000000000000000 ) ) ;
#103992=ORIENTED_EDGE ( 'NONE', *, *, #13536, .T. ) ;
#104019=ORIENTED_EDGE ( 'NONE', *, *, #25665, .F. ) ;
#104021=CARTESIAN_POINT ( 'NONE',  ( 36.08349330513379982, 1.593028355512270567E-15, 0.000000000000000000 ) ) ;
#104042=ORIENTED_EDGE ( 'NONE', *, *, #87050, .F. ) ;
#104091=DIRECTION ( 'NONE',  ( 0.000000000000000000, -1.000000000000000000, 0.000000000000000000 ) ) ;
#104105=ORIENTED_EDGE ( 'NONE', *, *, #60303, .F. ) ;
#104107=DIRECTION ( 'NONE',  ( 0.000000000000000000, -1.000000000000000000, 0.000000000000000000 ) ) ;
#104111=CARTESIAN_POINT ( 'NONE',  ( 44.35000000000000142, 1.533819458162526451E-15, 0.000000000000000000 ) ) ;
#104116=CIRCLE ( 'NONE', #50666, 4.000000000000000000 ) ;
#104142=ORIENTED_EDGE ( 'NONE', *, *, #64563, .F. ) ;
#104183=ORIENTED_EDGE ( 'NONE', *, *, #37711, .F. ) ;
#104186=ORIENTED_EDGE ( 'NONE', *, *, #94287, .F. ) ;
#104221=DIRECTION ( 'NONE',  ( 0.000000000000000000, -1.000000000000000000, 0.000000000000000000 ) ) ;
#104230=ORIENTED_EDGE ( 'NONE', *, *, #3920, .T. ) ;
#104231=CARTESIAN_POINT ( 'NONE',  ( 8.099999999999999645, -3.752776749732575468, -6.499999999999999112 ) ) ;
#104242=AXIS2_PLACEMENT_3D ( 'NONE', #90807, #32593, #98865 ) ;
#104246=CARTESIAN_POINT ( 'NONE',  ( 0.2565376335216122961, -2.516992571280024737, 6.500000000000000888 ) ) ;
#104266=CARTESIAN_POINT ( 'NONE',  ( 24.34999999999999787, -3.309499999999999886, 0.000000000000000000 ) ) ;
#104288=VECTOR ( 'NONE', #95557, 1000.000000000000000 ) ;
#104303=EDGE_CURVE ( 'NONE', #44258, #13998, #84673, .T. ) ;
#104331=VERTEX_POINT ( 'NONE', #9049 ) ;
#104361=ORIENTED_EDGE ( 'NONE', *, *, #24425, .F. ) ;
#104382=LINE ( 'NONE', #28419, #11442 ) ;
#104387=CARTESIAN_POINT ( 'NONE',  ( 6.326445470157511686, -6.578717624163894939, 2.268395195563513767 ) ) ;
#104390=ORIENTED_EDGE ( 'NONE', *, *, #4968, .F. ) ;
#104391=CARTESIAN_POINT ( 'NONE',  ( 39.83349330513380693, -4.000000000000000888, 4.898587196589416773E-16 ) ) ;
#104393=AXIS2_PLACEMENT_3D ( 'NONE', #47461, #72279, #104107 ) ;
#104403=DIRECTION ( 'NONE',  ( 0.000000000000000000, -1.000000000000000000, 0.000000000000000000 ) ) ;
#104424=CIRCLE ( 'NONE', #45844, 4.000000000000001776 ) ;
#104431=EDGE_CURVE ( 'NONE', #46114, #79431, #30587, .T. ) ;
#104459=CIRCLE ( 'NONE', #83743, 4.000000000000000888 ) ;
#104472=ADVANCED_FACE ( 'NONE', ( #29540 ), #10657, .T. ) ;
#104489=EDGE_CURVE ( 'NONE', #77149, #54299, #89854, .T. ) ;
#104507=ORIENTED_EDGE ( 'NONE', *, *, #105893, .F. ) ;
#104509=CARTESIAN_POINT ( 'NONE',  ( 20.59999999999999787, -3.309499999999999886, 0.000000000000000000 ) ) ;
#104539=EDGE_CURVE ( 'NONE', #82046, #10704, #15963, .T. ) ;
#104542=CIRCLE ( 'NONE', #71808, 4.000000000000001776 ) ;
#104559=EDGE_CURVE ( 'NONE', #27202, #78767, #48314, .T. ) ;
#104589=CONICAL_SURFACE ( 'NONE', #66734, 3.309500000000001663, 0.9599310885968770357 ) ;
#104596=DIRECTION ( 'NONE',  ( -1.000000000000000000, -0.000000000000000000, -0.000000000000000000 ) ) ;
#104606=CONICAL_SURFACE ( 'NONE', #21956, 3.309500000000001663, 0.9599310885968770357 ) ;
#104613=CARTESIAN_POINT ( 'NONE',  ( 0.000000000000000000, 0.000000000000000000, 4.000000000000000000 ) ) ;
#104618=AXIS2_PLACEMENT_3D ( 'NONE', #96833, #71474, #47198 ) ;
#104640=ORIENTED_EDGE ( 'NONE', *, *, #64914, .T. ) ;
#104668=EDGE_CURVE ( 'NONE', #34171, #6924, #59093, .T. ) ;
#104680=CARTESIAN_POINT ( 'NONE',  ( 13.58349330513380160, -4.000000000000000888, 4.898587196589416773E-16 ) ) ;
#104686=EDGE_LOOP ( 'NONE', ( #39372, #100682, #46944, #67039, #73370 ) ) ;
#104722=ORIENTED_EDGE ( 'NONE', *, *, #11957, .T. ) ;
#104727=DIRECTION ( 'NONE',  ( 0.000000000000000000, -1.000000000000000000, 0.000000000000000000 ) ) ;
#104746=VECTOR ( 'NONE', #99232, 1000.000000000000000 ) ;
#104760=CARTESIAN_POINT ( 'NONE',  ( 0.000000000000000000, 7.505553499465140277, 3.755786496842903002E-16 ) ) ;
#104785=CARTESIAN_POINT ( 'NONE',  ( 6.162888688655344005, -3.752776749732561257, 6.500000000000000000 ) ) ;
#104792=ORIENTED_EDGE ( 'NONE', *, *, #69262, .F. ) ;
#104840=ORIENTED_EDGE ( 'NONE', *, *, #64647, .T. ) ;
#104843=CARTESIAN_POINT ( 'NONE',  ( 38.58349330513380693, 1.593028355512270567E-15, 0.000000000000000000 ) ) ;
#104873=DIRECTION ( 'NONE',  ( -1.000000000000000000, -0.000000000000000000, -0.000000000000000000 ) ) ;
#104889=DIRECTION ( 'NONE',  ( -1.000000000000000000, -1.224606353822377258E-16, -0.000000000000000000 ) ) ;
#104915=ORIENTED_EDGE ( 'NONE', *, *, #73533, .F. ) ;
#104922=CARTESIAN_POINT ( 'NONE',  ( 30.59999999999999787, -3.309499999999999886, 4.475777889183790779E-16 ) ) ;
#104935=CARTESIAN_POINT ( 'NONE',  ( 41.36650669486618881, 1.474610560812782335E-15, 0.000000000000000000 ) ) ;
#104956=ORIENTED_EDGE ( 'NONE', *, *, #81711, .T. ) ;
#104963=EDGE_CURVE ( 'NONE', #13998, #47451, #29513, .T. ) ;
#104964=CIRCLE ( 'NONE', #34400, 4.000000000000001776 ) ;
#104975=CIRCLE ( 'NONE', #42915, 4.000000000000001776 ) ;
#105027=DIRECTION ( 'NONE',  ( 0.000000000000000000, -1.000000000000000000, 0.000000000000000000 ) ) ;
#105050=CIRCLE ( 'NONE', #41284, 4.000000000000000888 ) ;
#105053=AXIS2_PLACEMENT_3D ( 'NONE', #62785, #13676, #97778 ) ;
#105058=CARTESIAN_POINT ( 'NONE',  ( 33.58349330513379982, 1.593028355512270567E-15, 0.000000000000000000 ) ) ;
#105064=CARTESIAN_POINT ( 'NONE',  ( 13.86650669486618881, -3.851859888774471706E-31, 4.000000000000000888 ) ) ;
#105080=EDGE_LOOP ( 'NONE', ( #52774, #59727, #39818, #16109, #65642, #56005 ) ) ;
#105083=CARTESIAN_POINT ( 'NONE',  ( 9.833493305133801599, 1.593028355512270567E-15, 0.000000000000000000 ) ) ;
#105122=ORIENTED_EDGE ( 'NONE', *, *, #104963, .T. ) ;
#105131=CARTESIAN_POINT ( 'NONE',  ( 0.000000000000000000, 0.000000000000000000, 0.000000000000000000 ) ) ;
#105144=LINE ( 'NONE', #40403, #14995 ) ;
#105161=CARTESIAN_POINT ( 'NONE',  ( 0.000000000000000000, 0.000000000000000000, 0.000000000000000000 ) ) ;
#105203=CARTESIAN_POINT ( 'NONE',  ( 9.833493305133801599, 1.593028355512270567E-15, 0.000000000000000000 ) ) ;
#105220=CARTESIAN_POINT ( 'NONE',  ( 30.11650669486618881, 4.898587196589411843E-16, -4.000000000000000888 ) ) ;
#105228=ADVANCED_FACE ( 'NONE', ( #89605 ), #31418, .T. ) ;
#105231=AXIS2_PLACEMENT_3D ( 'NONE', #72038, #72560, #31604 ) ;
#105260=AXIS2_PLACEMENT_3D ( 'NONE', #83565, #43124, #67927 ) ;
#105269=AXIS2_PLACEMENT_3D ( 'NONE', #16001, #7361, #55893 ) ;
#105270=EDGE_CURVE ( 'NONE', #59177, #31781, #83054, .T. ) ;
#105282=ORIENTED_EDGE ( 'NONE', *, *, #87004, .F. ) ;
#105288=CARTESIAN_POINT ( 'NONE',  ( 41.36650669486618881, 1.474610560812782335E-15, 0.000000000000000000 ) ) ;
#105314=FACE_OUTER_BOUND ( 'NONE', #29041, .T. ) ;
#105315=DIRECTION ( 'NONE',  ( 0.000000000000000000, -1.000000000000000000, 0.000000000000000000 ) ) ;
#105326=ORIENTED_EDGE ( 'NONE', *, *, #77990, .F. ) ;
#105330=CYLINDRICAL_SURFACE ( 'NONE', #100095, 4.000000000000000000 ) ;
#105341=ORIENTED_EDGE ( 'NONE', *, *, #35063, .F. ) ;
#105357=EDGE_CURVE ( 'NONE', #54223, #69803, #42636, .T. ) ;
#105389=ORIENTED_EDGE ( 'NONE', *, *, #68925, .F. ) ;
#105396=CYLINDRICAL_SURFACE ( 'NONE', #46198, 4.000000000000000000 ) ;
#105463=ORIENTED_EDGE ( 'NONE', *, *, #65246, .F. ) ;
#105489=ORIENTED_EDGE ( 'NONE', *, *, #30725, .F. ) ;
#105512=CARTESIAN_POINT ( 'NONE',  ( 26.84999999999999787, 3.309500000000003439, 0.000000000000000000 ) ) ;
#105515=LINE ( 'NONE', #46231, #76525 ) ;
#105521=EDGE_CURVE ( 'NONE', #52776, #55265, #13961, .T. ) ;
#105556=EDGE_CURVE ( 'NONE', #34171, #43396, #157, .T. ) ;
#105572=CARTESIAN_POINT ( 'NONE',  ( 16.08349330513380337, -7.703719777548943412E-31, 4.000000000000001776 ) ) ;
#105618=DIRECTION ( 'NONE',  ( -1.000000000000000000, -1.224606353822377258E-16, -0.000000000000000000 ) ) ;
#105638=CARTESIAN_POINT ( 'NONE',  ( 18.86650669486618881, 4.000000000000003553, 4.898587196589414801E-16 ) ) ;
#105650=VERTEX_POINT ( 'NONE', #40780 ) ;
#105675=EDGE_CURVE ( 'NONE', #6993, #43441, #65652, .T. ) ;
#105682=LINE ( 'NONE', #49031, #66921 ) ;
#105688=AXIS2_PLACEMENT_3D ( 'NONE', #80462, #97182, #96668 ) ;
#105753=VERTEX_POINT ( 'NONE', #12659 ) ;
#105762=DIRECTION ( 'NONE',  ( -1.000000000000000000, -1.224606353822377258E-16, -0.000000000000000000 ) ) ;
#105765=EDGE_CURVE ( 'NONE', #80889, #103547, #63371, .T. ) ;
#105774=DIRECTION ( 'NONE',  ( -1.000000000000000000, -1.224606353822377258E-16, -0.000000000000000000 ) ) ;
#105783=ORIENTED_EDGE ( 'NONE', *, *, #16953, .F. ) ;
#105804=ORIENTED_EDGE ( 'NONE', *, *, #104559, .T. ) ;
#105812=AXIS2_PLACEMENT_3D ( 'NONE', #40473, #72314, #23798 ) ;
#105827=CARTESIAN_POINT ( 'NONE',  ( 46.08349330513379982, 1.593028355512270567E-15, 0.000000000000000000 ) ) ;
#105853=AXIS2_PLACEMENT_3D ( 'NONE', #96856, #22982, #54773 ) ;
#105879=DIRECTION ( 'NONE',  ( 0.000000000000000000, 0.000000000000000000, 1.000000000000000000 ) ) ;
#105885=CIRCLE ( 'NONE', #49056, 8.605212085995399107 ) ;
#105893=EDGE_CURVE ( 'NONE', #103460, #106458, #76029, .T. ) ;
#105925=CONICAL_SURFACE ( 'NONE', #47407, 6.500000000000000000, 1.047197551196600296 ) ;
#105946=VERTEX_POINT ( 'NONE', #72364 ) ;
#105972=DIRECTION ( 'NONE',  ( -0.5735764363510494901, -0.8191520442889894671, 0.000000000000000000 ) ) ;
#105984=CARTESIAN_POINT ( 'NONE',  ( 0.1061556211655389909, -6.421950209808288790, -1.876855952934451510 ) ) ;
#105988=ORIENTED_EDGE ( 'NONE', *, *, #27017, .T. ) ;
#106057=CARTESIAN_POINT ( 'NONE',  ( 16.08349330513380337, 1.593028355512270567E-15, 0.000000000000000000 ) ) ;
#106071=CARTESIAN_POINT ( 'NONE',  ( 0.000000000000000000, 5.629165124598847214, -3.250000000000007550 ) ) ;
#106087=ORIENTED_EDGE ( 'NONE', *, *, #72083, .T. ) ;
#106093=ORIENTED_EDGE ( 'NONE', *, *, #62908, .F. ) ;
#106115=FACE_OUTER_BOUND ( 'NONE', #76567, .T. ) ;
#106138=DIRECTION ( 'NONE',  ( -1.000000000000000000, -0.000000000000000000, -0.000000000000000000 ) ) ;
#106139=AXIS2_PLACEMENT_3D ( 'NONE', #98279, #31974, #31456 ) ;
#106142=DIRECTION ( 'NONE',  ( 0.000000000000000000, -1.000000000000000000, 0.000000000000000000 ) ) ;
#106152=CARTESIAN_POINT ( 'NONE',  ( 17.33349330513380337, 4.000000000000002665, 0.000000000000000000 ) ) ;
#106173=ORIENTED_EDGE ( 'NONE', *, *, #93847, .T. ) ;
#106176=CARTESIAN_POINT ( 'NONE',  ( 18.09999999999999787, 1.533819458162526451E-15, 0.000000000000000000 ) ) ;
#106187=DIRECTION ( 'NONE',  ( -1.000000000000000000, -1.224606353822377258E-16, -0.000000000000000000 ) ) ;
#106207=VECTOR ( 'NONE', #27026, 1000.000000000000000 ) ;
#106228=CIRCLE ( 'NONE', #90784, 4.000000000000001776 ) ;
#106290=DIRECTION ( 'NONE',  ( -1.000000000000000000, -1.224606353822377258E-16, -0.000000000000000000 ) ) ;
#106295=ORIENTED_EDGE ( 'NONE', *, *, #64000, .T. ) ;
#106301=DIRECTION ( 'NONE',  ( 0.5735764363510462704, 0.8191520442889915765, 0.000000000000000000 ) ) ;
#106302=CARTESIAN_POINT ( 'NONE',  ( 16.08349330513380337, 1.593028355512270567E-15, 0.000000000000000000 ) ) ;
#106320=FACE_OUTER_BOUND ( 'NONE', #52527, .T. ) ;
#106342=ORIENTED_EDGE ( 'NONE', *, *, #29778, .F. ) ;
#106344=CIRCLE ( 'NONE', #80553, 4.000000000000001776 ) ;
#106373=EDGE_LOOP ( 'NONE', ( #34248, #30520, #19249, #73492, #7474 ) ) ;
#106385=DIRECTION ( 'NONE',  ( 0.000000000000000000, -1.000000000000000000, 0.000000000000000000 ) ) ;
#106402=AXIS2_PLACEMENT_3D ( 'NONE', #104231, #79432, #79953 ) ;
#106436=CYLINDRICAL_SURFACE ( 'NONE', #102406, 4.000000000000000000 ) ;
#106439=CARTESIAN_POINT ( 'NONE',  ( 6.563035550597769330, 3.302680408004402324, -6.845819698387219709 ) ) ;
#106458=VERTEX_POINT ( 'NONE', #80317 ) ;
#106484=EDGE_CURVE ( 'NONE', #82046, #25659, #81378, .T. ) ;
#106495=EDGE_CURVE ( 'NONE', #478, #104331, #52010, .T. ) ;
#106515=AXIS2_PLACEMENT_3D ( 'NONE', #32872, #83514, #92136 ) ;
#106537=B_SPLINE_CURVE_WITH_KNOTS ( 'NONE', 3,
 ( #76461, #60318, #77542, #35519, #52186, #34984 ),
 .UNSPECIFIED., .F., .F.,
 ( 4, 2, 4 ),
 ( 0.01067228061038544978, 0.01257272967564229335, 0.01447317874089913692 ),
 .UNSPECIFIED. ) ;
#106547=CARTESIAN_POINT ( 'NONE',  ( 39.83349330513380693, 4.898587196589405926E-16, -4.000000000000001776 ) ) ;
#106553=CARTESIAN_POINT ( 'NONE',  ( 16.84999999999999787, -3.309499999999999886, 4.475777889183790779E-16 ) ) ;
#106554=CARTESIAN_POINT ( 'NONE',  ( 32.61650669486618881, 4.000000000000003553, 4.898587196589414801E-16 ) ) ;
#106561=EDGE_CURVE ( 'NONE', #54371, #93985, #15903, .T. ) ;
#106569=EDGE_LOOP ( 'NONE', ( #104361, #16173, #85662, #52715, #103911 ) ) ;
#106575=DIRECTION ( 'NONE',  ( 0.000000000000000000, -1.000000000000000000, 0.000000000000000000 ) ) ;
#106610=VERTEX_POINT ( 'NONE', #75427 ) ;
#106643=CIRCLE ( 'NONE', #1530, 4.000000000000001776 ) ;
#106647=DIRECTION ( 'NONE',  ( 0.000000000000000000, -1.000000000000000000, 0.000000000000000000 ) ) ;
#106670=CARTESIAN_POINT ( 'NONE',  ( 25.11650669486618881, 1.474610560812782335E-15, 0.000000000000000000 ) ) ;
#106679=EDGE_CURVE ( 'NONE', #76929, #42491, #36586, .T. ) ;
#106691=LINE ( 'NONE', #32841, #98339 ) ;
#106729=ADVANCED_FACE ( 'NONE', ( #60861 ), #55455, .T. ) ;
#106737=ORIENTED_EDGE ( 'NONE', *, *, #82665, .T. ) ;
#106784=FACE_OUTER_BOUND ( 'NONE', #8006, .T. ) ;
ENDSEC;
END-ISO-10303-21;
